ISO-10303-21;
HEADER;
/* Generated by software containing ST-Developer
 * from STEP Tools, Inc. (www.steptools.com) 
 */

FILE_DESCRIPTION(
/* description */ ('Independent eighteen-tube parallel-flow evaporator geometry. Repeated
 machined headers and gasketed service covers, eighteen copper tubes, 
twenty-nine punched fins, threaded hose connections and bolted mountin
g feet. Native editable features and instanced parts. Braze details, w
orking fluid, pressure and thermal ratings require engineering selecti
on.'),
/* implementation_level */ '2;1');

FILE_NAME(
/* name */ 'Socket head cap screw M4x12.step',
/* time_stamp */ '2026-11-08T20:53:59-08:00',
/* author */ (''),
/* organization */ (''),
/* preprocessor_version */ 'ST-DEVELOPER v20.2',
/* originating_system */ 'Autodesk Translation Framework v15.17.0.0',
/* authorisation */ '');

FILE_SCHEMA (('AUTOMOTIVE_DESIGN { 1 0 10303 214 3 1 1 }'));
ENDSEC;

DATA;
#10=MECHANICAL_DESIGN_GEOMETRIC_PRESENTATION_REPRESENTATION('',(#339),#42620);
#311=CONICAL_SURFACE('',#11096,1.5,0.785398163397449);
#319=SHAPE_REPRESENTATION_RELATIONSHIP('SRR','None',#42729,#329);
#329=ADVANCED_BREP_SHAPE_REPRESENTATION('',(#349),#42616);
#339=STYLED_ITEM('',(#42784),#349);
#349=MANIFOLD_SOLID_BREP('Body1',#10389);
#471=FACE_BOUND('',#1722,.T.);
#472=FACE_BOUND('',#1725,.T.);
#547=PLANE('',#11102);
#548=PLANE('',#11103);
#549=PLANE('',#11104);
#550=PLANE('',#11105);
#551=PLANE('',#11106);
#552=PLANE('',#11107);
#553=PLANE('',#11108);
#554=PLANE('',#11109);
#555=PLANE('',#11113);
#556=PLANE('',#11114);
#597=B_SPLINE_SURFACE_WITH_KNOTS('',3,3,((#36638,#36639,#36640,#36641,#36642,
#36643,#36644,#36645,#36646,#36647,#36648,#36649,#36650,#36651,#36652,#36653,
#36654,#36655,#36656,#36657,#36658,#36659,#36660,#36661,#36662,#36663,#36664,
#36665,#36666,#36667,#36668,#36669,#36670,#36671,#36672,#36673,#36674,#36675,
#36676,#36677,#36678,#36679,#36680,#36681,#36682,#36683,#36684,#36685,#36686,
#36687,#36688,#36689,#36690,#36691,#36692,#36693,#36694,#36695,#36696,#36697,
#36698,#36699,#36700,#36701,#36702,#36703,#36704,#36705,#36706,#36707,#36708,
#36709,#36710,#36711,#36712,#36713,#36714,#36715,#36716,#36717,#36718,#36719,
#36720,#36721,#36722,#36723,#36724,#36725,#36726,#36727,#36728,#36729,#36730,
#36731,#36732,#36733,#36734,#36735,#36736,#36737,#36738,#36739,#36740,#36741,
#36742,#36743),(#36744,#36745,#36746,#36747,#36748,#36749,#36750,#36751,
#36752,#36753,#36754,#36755,#36756,#36757,#36758,#36759,#36760,#36761,#36762,
#36763,#36764,#36765,#36766,#36767,#36768,#36769,#36770,#36771,#36772,#36773,
#36774,#36775,#36776,#36777,#36778,#36779,#36780,#36781,#36782,#36783,#36784,
#36785,#36786,#36787,#36788,#36789,#36790,#36791,#36792,#36793,#36794,#36795,
#36796,#36797,#36798,#36799,#36800,#36801,#36802,#36803,#36804,#36805,#36806,
#36807,#36808,#36809,#36810,#36811,#36812,#36813,#36814,#36815,#36816,#36817,
#36818,#36819,#36820,#36821,#36822,#36823,#36824,#36825,#36826,#36827,#36828,
#36829,#36830,#36831,#36832,#36833,#36834,#36835,#36836,#36837,#36838,#36839,
#36840,#36841,#36842,#36843,#36844,#36845,#36846,#36847,#36848,#36849),
(#36850,#36851,#36852,#36853,#36854,#36855,#36856,#36857,#36858,#36859,
#36860,#36861,#36862,#36863,#36864,#36865,#36866,#36867,#36868,#36869,#36870,
#36871,#36872,#36873,#36874,#36875,#36876,#36877,#36878,#36879,#36880,#36881,
#36882,#36883,#36884,#36885,#36886,#36887,#36888,#36889,#36890,#36891,#36892,
#36893,#36894,#36895,#36896,#36897,#36898,#36899,#36900,#36901,#36902,#36903,
#36904,#36905,#36906,#36907,#36908,#36909,#36910,#36911,#36912,#36913,#36914,
#36915,#36916,#36917,#36918,#36919,#36920,#36921,#36922,#36923,#36924,#36925,
#36926,#36927,#36928,#36929,#36930,#36931,#36932,#36933,#36934,#36935,#36936,
#36937,#36938,#36939,#36940,#36941,#36942,#36943,#36944,#36945,#36946,#36947,
#36948,#36949,#36950,#36951,#36952,#36953,#36954,#36955),(#36956,#36957,
#36958,#36959,#36960,#36961,#36962,#36963,#36964,#36965,#36966,#36967,#36968,
#36969,#36970,#36971,#36972,#36973,#36974,#36975,#36976,#36977,#36978,#36979,
#36980,#36981,#36982,#36983,#36984,#36985,#36986,#36987,#36988,#36989,#36990,
#36991,#36992,#36993,#36994,#36995,#36996,#36997,#36998,#36999,#37000,#37001,
#37002,#37003,#37004,#37005,#37006,#37007,#37008,#37009,#37010,#37011,#37012,
#37013,#37014,#37015,#37016,#37017,#37018,#37019,#37020,#37021,#37022,#37023,
#37024,#37025,#37026,#37027,#37028,#37029,#37030,#37031,#37032,#37033,#37034,
#37035,#37036,#37037,#37038,#37039,#37040,#37041,#37042,#37043,#37044,#37045,
#37046,#37047,#37048,#37049,#37050,#37051,#37052,#37053,#37054,#37055,#37056,
#37057,#37058,#37059,#37060,#37061)),.UNSPECIFIED.,.F.,.F.,.F.,(4,4),(4,
1,1,1,1,1,1,1,1,1,1,1,1,1,1,1,1,1,1,1,1,1,1,1,1,1,1,1,1,1,1,1,1,1,1,1,1,
1,1,1,1,1,1,1,1,1,1,1,1,1,1,1,1,1,1,1,1,1,1,1,1,1,1,1,1,1,1,1,1,1,1,1,1,
1,1,1,1,1,1,1,1,1,1,1,1,1,1,1,1,1,1,1,1,1,1,1,1,1,1,1,1,1,1,4),(0.,0.0460148164544132),
(11.6154215191105,12.6127573616628,13.610093204215,14.6074290467673,15.6047648893195,
16.6021007318718,17.599436574424,18.5967724169762,19.5941082595285,20.5914441020807,
21.588779944633,22.5861157871852,23.5834516297375,24.5807874722897,25.5781233148419,
26.5754591573942,27.5727949999464,28.5701308424987,29.5674666850509,30.5648025276032,
31.5621383701554,32.5594742127077,33.5568100552599,34.5541458978121,35.5514817403644,
36.5488175829166,37.5461534254689,38.5434892680211,39.5408251105734,40.5381609531256,
41.5354967956779,42.5328326382301,43.5301684807823,44.5275043233346,45.5248401658868,
46.5221760084391,47.5195118509913,48.5168476935436,49.5141835360958,50.5115193786481,
51.5088552212003,52.5061910637525,53.5035269063048,54.500862748857,55.4981985914093,
56.4955344339615,57.4928702765138,58.490206119066,59.4875419616182,60.4848778041705,
61.4822136467227,62.479549489275,63.4768853318272,64.4742211743795,65.4715570169317,
66.468892859484,67.4662287020362,68.4635645445884,69.4609003871407,70.4582362296929,
71.4555720722452,72.4529079147974,73.4502437573497,74.4475795999019,75.4449154424541,
76.4422512850064,77.4395871275586,78.4369229701109,79.4342588126631,80.4315946552154,
81.4289304977676,82.4262663403199,83.4236021828721,84.4209380254243,85.4182738679766,
86.4156097105288,87.4129455530811,88.4102813956333,89.4076172381856,90.4049530807378,
91.4022889232901,92.3996247658423,93.3969606083945,94.3942964509468,95.391632293499,
96.3889681360513,97.3863039786035,98.3836398211558,99.380975663708,100.37831150626,
101.375647348812,102.372983191365,103.370319033917,104.367654876469,105.364990719021,
106.362326561574,107.359662404126,108.356998246678,109.35433408923,110.351669931783,
111.349005774335,112.346341616887,113.343677459439,114.341013301992),
 .UNSPECIFIED.);
#598=B_SPLINE_SURFACE_WITH_KNOTS('',3,3,((#37181,#37182,#37183,#37184,#37185,
#37186,#37187,#37188,#37189,#37190,#37191,#37192,#37193,#37194,#37195,#37196,
#37197,#37198,#37199,#37200,#37201,#37202,#37203,#37204,#37205,#37206,#37207,
#37208,#37209,#37210,#37211,#37212,#37213,#37214,#37215,#37216,#37217,#37218,
#37219,#37220,#37221,#37222,#37223,#37224,#37225,#37226,#37227,#37228,#37229,
#37230,#37231,#37232,#37233,#37234,#37235,#37236,#37237,#37238,#37239,#37240,
#37241,#37242,#37243,#37244,#37245,#37246,#37247,#37248,#37249,#37250,#37251,
#37252,#37253,#37254,#37255,#37256,#37257,#37258,#37259,#37260,#37261,#37262,
#37263,#37264,#37265,#37266,#37267,#37268,#37269,#37270,#37271,#37272,#37273,
#37274,#37275,#37276,#37277,#37278,#37279,#37280,#37281,#37282,#37283,#37284,
#37285,#37286,#37287,#37288),(#37289,#37290,#37291,#37292,#37293,#37294,
#37295,#37296,#37297,#37298,#37299,#37300,#37301,#37302,#37303,#37304,#37305,
#37306,#37307,#37308,#37309,#37310,#37311,#37312,#37313,#37314,#37315,#37316,
#37317,#37318,#37319,#37320,#37321,#37322,#37323,#37324,#37325,#37326,#37327,
#37328,#37329,#37330,#37331,#37332,#37333,#37334,#37335,#37336,#37337,#37338,
#37339,#37340,#37341,#37342,#37343,#37344,#37345,#37346,#37347,#37348,#37349,
#37350,#37351,#37352,#37353,#37354,#37355,#37356,#37357,#37358,#37359,#37360,
#37361,#37362,#37363,#37364,#37365,#37366,#37367,#37368,#37369,#37370,#37371,
#37372,#37373,#37374,#37375,#37376,#37377,#37378,#37379,#37380,#37381,#37382,
#37383,#37384,#37385,#37386,#37387,#37388,#37389,#37390,#37391,#37392,#37393,
#37394,#37395,#37396),(#37397,#37398,#37399,#37400,#37401,#37402,#37403,
#37404,#37405,#37406,#37407,#37408,#37409,#37410,#37411,#37412,#37413,#37414,
#37415,#37416,#37417,#37418,#37419,#37420,#37421,#37422,#37423,#37424,#37425,
#37426,#37427,#37428,#37429,#37430,#37431,#37432,#37433,#37434,#37435,#37436,
#37437,#37438,#37439,#37440,#37441,#37442,#37443,#37444,#37445,#37446,#37447,
#37448,#37449,#37450,#37451,#37452,#37453,#37454,#37455,#37456,#37457,#37458,
#37459,#37460,#37461,#37462,#37463,#37464,#37465,#37466,#37467,#37468,#37469,
#37470,#37471,#37472,#37473,#37474,#37475,#37476,#37477,#37478,#37479,#37480,
#37481,#37482,#37483,#37484,#37485,#37486,#37487,#37488,#37489,#37490,#37491,
#37492,#37493,#37494,#37495,#37496,#37497,#37498,#37499,#37500,#37501,#37502,
#37503,#37504),(#37505,#37506,#37507,#37508,#37509,#37510,#37511,#37512,
#37513,#37514,#37515,#37516,#37517,#37518,#37519,#37520,#37521,#37522,#37523,
#37524,#37525,#37526,#37527,#37528,#37529,#37530,#37531,#37532,#37533,#37534,
#37535,#37536,#37537,#37538,#37539,#37540,#37541,#37542,#37543,#37544,#37545,
#37546,#37547,#37548,#37549,#37550,#37551,#37552,#37553,#37554,#37555,#37556,
#37557,#37558,#37559,#37560,#37561,#37562,#37563,#37564,#37565,#37566,#37567,
#37568,#37569,#37570,#37571,#37572,#37573,#37574,#37575,#37576,#37577,#37578,
#37579,#37580,#37581,#37582,#37583,#37584,#37585,#37586,#37587,#37588,#37589,
#37590,#37591,#37592,#37593,#37594,#37595,#37596,#37597,#37598,#37599,#37600,
#37601,#37602,#37603,#37604,#37605,#37606,#37607,#37608,#37609,#37610,#37611,
#37612)),.UNSPECIFIED.,.F.,.F.,.F.,(4,4),(4,1,1,1,1,1,1,1,1,1,1,1,1,1,1,
1,1,1,1,1,1,1,1,1,1,1,1,1,1,1,1,1,1,1,1,1,1,1,1,1,1,1,1,1,1,1,1,1,1,1,1,
1,1,1,1,1,1,1,1,1,1,1,1,1,1,1,1,1,1,1,1,1,1,1,1,1,1,1,1,1,1,1,1,1,1,1,1,
1,1,1,1,1,1,1,1,1,1,1,1,1,1,1,1,1,1,4),(0.,0.0460148164544132),(8.31058692273969,
9.30859389336977,10.3066008639999,11.30460783463,12.30261480526,13.3006217758901,
14.2986287465202,15.2966357171503,16.2946426877804,17.2926496584105,18.2906566290406,
19.2886635996707,20.2866705703008,21.2846775409308,22.2826845115609,23.280691482191,
24.2786984528211,25.2767054234512,26.2747123940813,27.2727193647114,28.2707263353415,
29.2687333059716,30.2667402766016,31.2647472472317,32.2627542178618,33.2607611884919,
34.258768159122,35.2567751297521,36.2547821003822,37.2527890710123,38.2507960416424,
39.2488030122724,40.2468099829025,41.2448169535326,42.2428239241627,43.2408308947928,
44.2388378654229,45.236844836053,46.2348518066831,47.2328587773132,48.2308657479432,
49.2288727185733,50.2268796892034,51.2248866598335,52.2228936304636,53.2209006010937,
54.2189075717238,55.2169145423539,56.214921512984,57.212928483614,58.2109354542441,
59.2089424248742,60.2069493955043,61.2049563661344,62.2029633367645,63.2009703073946,
64.1989772780247,65.1969842486548,66.1949912192848,67.1929981899149,68.191005160545,
69.1890121311751,70.1870191018052,71.1850260724353,72.1830330430654,73.1810400136955,
74.1790469843256,75.1770539549557,76.1750609255857,77.1730678962158,78.1710748668459,
79.169081837476,80.1670888081061,81.1650957787362,82.1631027493663,83.1611097199964,
84.1591166906264,85.1571236612565,86.1551306318866,87.1531376025167,88.1511445731468,
89.1491515437769,90.147158514407,91.1451654850371,92.1431724556672,93.1411794262973,
94.1391863969273,95.1371933675574,96.1352003381875,97.1332073088176,98.1312142794477,
99.1292212500778,100.127228220708,101.125235191338,102.123242161968,103.121249132598,
104.119256103228,105.117263073858,106.115270044488,107.113277015118,108.111283985749,
109.109290956379,110.107297927009,111.105304897639,112.103311868269,113.101318838899),
 .UNSPECIFIED.);
#1015=FACE_OUTER_BOUND('',#1677,.T.);
#1016=FACE_OUTER_BOUND('',#1678,.T.);
#1017=FACE_OUTER_BOUND('',#1679,.T.);
#1018=FACE_OUTER_BOUND('',#1680,.T.);
#1019=FACE_OUTER_BOUND('',#1681,.T.);
#1020=FACE_OUTER_BOUND('',#1682,.T.);
#1021=FACE_OUTER_BOUND('',#1683,.T.);
#1022=FACE_OUTER_BOUND('',#1684,.T.);
#1023=FACE_OUTER_BOUND('',#1685,.T.);
#1024=FACE_OUTER_BOUND('',#1686,.T.);
#1025=FACE_OUTER_BOUND('',#1687,.T.);
#1026=FACE_OUTER_BOUND('',#1688,.T.);
#1027=FACE_OUTER_BOUND('',#1689,.T.);
#1028=FACE_OUTER_BOUND('',#1690,.T.);
#1029=FACE_OUTER_BOUND('',#1691,.T.);
#1030=FACE_OUTER_BOUND('',#1692,.T.);
#1031=FACE_OUTER_BOUND('',#1693,.T.);
#1032=FACE_OUTER_BOUND('',#1694,.T.);
#1033=FACE_OUTER_BOUND('',#1695,.T.);
#1034=FACE_OUTER_BOUND('',#1696,.T.);
#1035=FACE_OUTER_BOUND('',#1697,.T.);
#1036=FACE_OUTER_BOUND('',#1698,.T.);
#1037=FACE_OUTER_BOUND('',#1699,.T.);
#1038=FACE_OUTER_BOUND('',#1700,.T.);
#1039=FACE_OUTER_BOUND('',#1701,.T.);
#1040=FACE_OUTER_BOUND('',#1702,.T.);
#1041=FACE_OUTER_BOUND('',#1703,.T.);
#1042=FACE_OUTER_BOUND('',#1704,.T.);
#1043=FACE_OUTER_BOUND('',#1705,.T.);
#1044=FACE_OUTER_BOUND('',#1706,.T.);
#1045=FACE_OUTER_BOUND('',#1707,.T.);
#1046=FACE_OUTER_BOUND('',#1708,.T.);
#1047=FACE_OUTER_BOUND('',#1709,.T.);
#1048=FACE_OUTER_BOUND('',#1710,.T.);
#1049=FACE_OUTER_BOUND('',#1711,.T.);
#1050=FACE_OUTER_BOUND('',#1712,.T.);
#1051=FACE_OUTER_BOUND('',#1713,.T.);
#1052=FACE_OUTER_BOUND('',#1714,.T.);
#1053=FACE_OUTER_BOUND('',#1715,.T.);
#1054=FACE_OUTER_BOUND('',#1716,.T.);
#1055=FACE_OUTER_BOUND('',#1717,.T.);
#1056=FACE_OUTER_BOUND('',#1718,.T.);
#1057=FACE_OUTER_BOUND('',#1719,.T.);
#1058=FACE_OUTER_BOUND('',#1720,.T.);
#1059=FACE_OUTER_BOUND('',#1721,.T.);
#1060=FACE_OUTER_BOUND('',#1723,.T.);
#1061=FACE_OUTER_BOUND('',#1724,.T.);
#1062=FACE_OUTER_BOUND('',#1726,.T.);
#1677=EDGE_LOOP('',(#8741,#8742,#8743,#8744));
#1678=EDGE_LOOP('',(#8745,#8746,#8747,#8748));
#1679=EDGE_LOOP('',(#8749,#8750,#8751,#8752));
#1680=EDGE_LOOP('',(#8753,#8754,#8755,#8756));
#1681=EDGE_LOOP('',(#8757,#8758,#8759,#8760));
#1682=EDGE_LOOP('',(#8761,#8762,#8763,#8764));
#1683=EDGE_LOOP('',(#8765,#8766,#8767,#8768));
#1684=EDGE_LOOP('',(#8769,#8770,#8771,#8772));
#1685=EDGE_LOOP('',(#8773,#8774,#8775,#8776));
#1686=EDGE_LOOP('',(#8777,#8778,#8779,#8780));
#1687=EDGE_LOOP('',(#8781,#8782,#8783,#8784));
#1688=EDGE_LOOP('',(#8785,#8786,#8787,#8788));
#1689=EDGE_LOOP('',(#8789,#8790,#8791,#8792));
#1690=EDGE_LOOP('',(#8793,#8794,#8795,#8796));
#1691=EDGE_LOOP('',(#8797,#8798,#8799,#8800));
#1692=EDGE_LOOP('',(#8801,#8802,#8803,#8804));
#1693=EDGE_LOOP('',(#8805,#8806,#8807,#8808));
#1694=EDGE_LOOP('',(#8809,#8810,#8811,#8812));
#1695=EDGE_LOOP('',(#8813,#8814,#8815,#8816));
#1696=EDGE_LOOP('',(#8817,#8818,#8819,#8820));
#1697=EDGE_LOOP('',(#8821,#8822,#8823,#8824));
#1698=EDGE_LOOP('',(#8825,#8826,#8827,#8828));
#1699=EDGE_LOOP('',(#8829,#8830,#8831,#8832));
#1700=EDGE_LOOP('',(#8833,#8834,#8835,#8836));
#1701=EDGE_LOOP('',(#8837,#8838,#8839,#8840));
#1702=EDGE_LOOP('',(#8841,#8842,#8843,#8844));
#1703=EDGE_LOOP('',(#8845,#8846,#8847,#8848));
#1704=EDGE_LOOP('',(#8849,#8850,#8851,#8852));
#1705=EDGE_LOOP('',(#8853,#8854,#8855,#8856));
#1706=EDGE_LOOP('',(#8857,#8858,#8859,#8860));
#1707=EDGE_LOOP('',(#8861,#8862,#8863,#8864));
#1708=EDGE_LOOP('',(#8865,#8866,#8867,#8868));
#1709=EDGE_LOOP('',(#8869,#8870,#8871,#8872,#8873,#8874,#8875,#8876));
#1710=EDGE_LOOP('',(#8877,#8878,#8879,#8880,#8881,#8882,#8883,#8884,#8885,
#8886,#8887,#8888,#8889,#8890,#8891,#8892,#8893,#8894,#8895,#8896,#8897,
#8898,#8899,#8900,#8901,#8902,#8903,#8904,#8905,#8906,#8907,#8908,#8909,
#8910,#8911,#8912));
#1711=EDGE_LOOP('',(#8913,#8914,#8915,#8916));
#1712=EDGE_LOOP('',(#8917,#8918,#8919,#8920,#8921,#8922,#8923,#8924,#8925,
#8926,#8927,#8928,#8929,#8930,#8931,#8932,#8933,#8934,#8935,#8936,#8937,
#8938,#8939,#8940,#8941,#8942,#8943,#8944,#8945,#8946,#8947,#8948,#8949,
#8950,#8951,#8952,#8953));
#1713=EDGE_LOOP('',(#8954,#8955,#8956,#8957));
#1714=EDGE_LOOP('',(#8958,#8959,#8960,#8961));
#1715=EDGE_LOOP('',(#8962,#8963,#8964,#8965));
#1716=EDGE_LOOP('',(#8966,#8967,#8968,#8969));
#1717=EDGE_LOOP('',(#8970,#8971,#8972,#8973));
#1718=EDGE_LOOP('',(#8974,#8975,#8976,#8977));
#1719=EDGE_LOOP('',(#8978,#8979,#8980,#8981));
#1720=EDGE_LOOP('',(#8982,#8983,#8984,#8985,#8986,#8987));
#1721=EDGE_LOOP('',(#8988));
#1722=EDGE_LOOP('',(#8989,#8990,#8991,#8992));
#1723=EDGE_LOOP('',(#8993,#8994,#8995,#8996));
#1724=EDGE_LOOP('',(#8997));
#1725=EDGE_LOOP('',(#8998,#8999,#9000,#9001,#9002,#9003));
#1726=EDGE_LOOP('',(#9004));
#1981=CIRCLE('',#11063,1.954);
#1982=CIRCLE('',#11080,1.5555);
#1983=CIRCLE('',#11097,1.954);
#1984=CIRCLE('',#11098,1.);
#1985=CIRCLE('',#11100,1.5555);
#1986=CIRCLE('',#11110,3.5);
#1987=CIRCLE('',#11112,3.5);
#2627=B_SPLINE_CURVE_WITH_KNOTS('',3,(#35189,#35190,#35191,#35192,#35193,
#35194,#35195,#35196,#35197,#35198),.UNSPECIFIED.,.F.,.F.,(4,3,3,4),(-4.09254174883833,
-3.98934337020898,-2.99200752765673,-2.06514013327813),.UNSPECIFIED.);
#2628=B_SPLINE_CURVE_WITH_KNOTS('',3,(#35201,#35202,#35203,#35204,#35205,
#35206,#35207),.UNSPECIFIED.,.F.,.F.,(4,3,4),(0.,0.998006970630082,1.11419103802948),
 .UNSPECIFIED.);
#2629=B_SPLINE_CURVE_WITH_KNOTS('',3,(#35212,#35213,#35214,#35215,#35216,
#35217,#35218,#35219,#35220,#35221,#35222,#35223,#35224,#35225,#35226,#35227,
#35228,#35229,#35230,#35231,#35232,#35233),.UNSPECIFIED.,.F.,.F.,(4,3,3,
3,3,3,3,4),(-10.3757270560179,-9.97335842552244,-8.9760225829702,-7.97868674041795,
-6.9813508978657,-5.98401505531347,-4.98667921276122,-4.09254174883833),
 .UNSPECIFIED.);
#2630=B_SPLINE_CURVE_WITH_KNOTS('',3,(#35234,#35235,#35236,#35237,#35238,
#35239,#35240,#35241,#35242,#35243,#35244,#35245,#35246,#35247,#35248,#35249,
#35250,#35251,#35252,#35253,#35254,#35255),.UNSPECIFIED.,.F.,.F.,(4,3,3,
3,3,3,3,4),(1.11419103802948,1.99601394126018,2.99402091189026,3.99202788252035,
4.99003485315045,5.98804182378054,6.98604879441062,7.39737634520907),
 .UNSPECIFIED.);
#2631=B_SPLINE_CURVE_WITH_KNOTS('',3,(#35260,#35261,#35262,#35263,#35264,
#35265,#35266,#35267,#35268,#35269,#35270,#35271,#35272,#35273,#35274,#35275,
#35276,#35277,#35278,#35279,#35280,#35281),.UNSPECIFIED.,.F.,.F.,(4,3,3,
3,3,3,3,4),(-16.6589123631975,-15.9573734808359,-14.9600376382837,-13.9627017957314,
-12.9653659531792,-11.9680301106269,-10.9706942680747,-10.3757270560179),
 .UNSPECIFIED.);
#2632=B_SPLINE_CURVE_WITH_KNOTS('',3,(#35282,#35283,#35284,#35285,#35286,
#35287,#35288,#35289,#35290,#35291,#35292,#35293,#35294,#35295,#35296,#35297,
#35298,#35299,#35300,#35301,#35302,#35303),.UNSPECIFIED.,.F.,.F.,(4,3,3,
3,3,3,3,4),(7.39737634520907,7.98405576504071,8.9820627356708,9.98006970630089,
10.978076676931,11.9760836475611,12.9740906181912,13.6805616523887),
 .UNSPECIFIED.);
#2633=B_SPLINE_CURVE_WITH_KNOTS('',3,(#35308,#35309,#35310,#35311,#35312,
#35313,#35314,#35315,#35316,#35317,#35318,#35319,#35320,#35321,#35322,#35323,
#35324,#35325,#35326,#35327,#35328,#35329,#35330,#35331,#35332),
 .UNSPECIFIED.,.F.,.F.,(4,3,3,3,3,3,3,3,4),(-22.9420976703771,-22.9387243787016,
-21.9413885361494,-20.9440526935971,-19.9467168510449,-18.9493810084926,
-17.9520451659404,-16.9547093233881,-16.6589123631975),.UNSPECIFIED.);
#2634=B_SPLINE_CURVE_WITH_KNOTS('',3,(#35333,#35334,#35335,#35336,#35337,
#35338,#35339,#35340,#35341,#35342,#35343,#35344,#35345,#35346,#35347,#35348,
#35349,#35350,#35351,#35352,#35353,#35354,#35355,#35356,#35357),
 .UNSPECIFIED.,.F.,.F.,(4,3,3,3,3,3,3,3,4),(13.6805616523887,13.9720975888212,
14.9701045594513,15.9681115300814,16.9661185007115,17.9641254713416,18.9621324419717,
19.9601394126018,19.9637469595682),.UNSPECIFIED.);
#2635=B_SPLINE_CURVE_WITH_KNOTS('',3,(#35362,#35363,#35364,#35365,#35366,
#35367,#35368,#35369,#35370,#35371,#35372,#35373,#35374,#35375,#35376,#35377,
#35378,#35379,#35380,#35381,#35382,#35383),.UNSPECIFIED.,.F.,.F.,(4,3,3,
3,3,3,3,4),(-29.2252829775567,-28.9227394340151,-27.9254035914628,-26.9280677489106,
-25.9307319063583,-24.9333960638061,-23.9360602212539,-22.9420976703771),
 .UNSPECIFIED.);
#2636=B_SPLINE_CURVE_WITH_KNOTS('',3,(#35384,#35385,#35386,#35387,#35388,
#35389,#35390,#35391,#35392,#35393,#35394,#35395,#35396,#35397,#35398,#35399,
#35400,#35401,#35402,#35403,#35404,#35405),.UNSPECIFIED.,.F.,.F.,(4,3,3,
3,3,3,3,4),(19.9637469595682,20.9581463832319,21.956153353862,22.954160324492,
23.9521672951221,24.9501742657522,25.9481812363823,26.2469322667478),
 .UNSPECIFIED.);
#2637=B_SPLINE_CURVE_WITH_KNOTS('',3,(#35410,#35411,#35412,#35413,#35414,
#35415,#35416,#35417,#35418,#35419,#35420,#35421,#35422,#35423,#35424,#35425,
#35426,#35427,#35428,#35429,#35430,#35431),.UNSPECIFIED.,.F.,.F.,(4,3,3,
3,3,3,3,4),(-35.5084682847363,-34.9067544893285,-33.9094186467763,-32.9120828042241,
-31.9147469616718,-30.9174111191196,-29.9200752765673,-29.2252829775567),
 .UNSPECIFIED.);
#2638=B_SPLINE_CURVE_WITH_KNOTS('',3,(#35432,#35433,#35434,#35435,#35436,
#35437,#35438,#35439,#35440,#35441,#35442,#35443,#35444,#35445,#35446,#35447,
#35448,#35449,#35450,#35451,#35452,#35453),.UNSPECIFIED.,.F.,.F.,(4,3,3,
3,3,3,3,4),(26.2469322667478,26.9461882070124,27.9441951776425,28.9422021482726,
29.9402091189027,30.9382160895327,31.9362230601628,32.5301175739274),
 .UNSPECIFIED.);
#2639=B_SPLINE_CURVE_WITH_KNOTS('',3,(#35458,#35459,#35460,#35461,#35462,
#35463,#35464,#35465,#35466,#35467,#35468,#35469,#35470,#35471,#35472,#35473,
#35474,#35475,#35476,#35477,#35478,#35479),.UNSPECIFIED.,.F.,.F.,(4,3,3,
3,3,3,3,4),(-41.7916535919159,-40.890769544642,-39.8934337020898,-38.8960978595375,
-37.8987620169853,-36.901426174433,-35.9040903318808,-35.5084682847363),
 .UNSPECIFIED.);
#2640=B_SPLINE_CURVE_WITH_KNOTS('',3,(#35480,#35481,#35482,#35483,#35484,
#35485,#35486,#35487,#35488,#35489,#35490,#35491,#35492,#35493,#35494,#35495,
#35496,#35497,#35498,#35499,#35500,#35501),.UNSPECIFIED.,.F.,.F.,(4,3,3,
3,3,3,3,4),(32.5301175739274,32.9342300307929,33.932237001423,34.9302439720531,
35.9282509426832,36.9262579133133,37.9242648839434,38.813302881107),
 .UNSPECIFIED.);
#2641=B_SPLINE_CURVE_WITH_KNOTS('',3,(#35506,#35507,#35508,#35509,#35510,
#35511,#35512,#35513,#35514,#35515,#35516,#35517,#35518,#35519,#35520,#35521,
#35522,#35523,#35524,#35525,#35526,#35527,#35528,#35529,#35530),
 .UNSPECIFIED.,.F.,.F.,(4,3,3,3,3,3,3,3,4),(-48.0748388990955,-47.8721204425077,
-46.8747845999555,-45.8774487574032,-44.880112914851,-43.8827770722987,
-42.8854412297465,-41.8881053871943,-41.7916535919159),.UNSPECIFIED.);
#2642=B_SPLINE_CURVE_WITH_KNOTS('',3,(#35531,#35532,#35533,#35534,#35535,
#35536,#35537,#35538,#35539,#35540,#35541,#35542,#35543,#35544,#35545,#35546,
#35547,#35548,#35549,#35550,#35551,#35552,#35553,#35554,#35555),
 .UNSPECIFIED.,.F.,.F.,(4,3,3,3,3,3,3,3,4),(38.813302881107,38.9222718545735,
39.9202788252036,40.9182857958337,41.9162927664637,42.9142997370938,43.9123067077239,
44.910313678354,45.0964881882866),.UNSPECIFIED.);
#2643=B_SPLINE_CURVE_WITH_KNOTS('',3,(#35560,#35561,#35562,#35563,#35564,
#35565,#35566,#35567,#35568,#35569,#35570,#35571,#35572,#35573,#35574,#35575,
#35576,#35577,#35578,#35579,#35580,#35581),.UNSPECIFIED.,.F.,.F.,(4,3,3,
3,3,3,3,4),(-54.3580242062751,-53.8561354978212,-52.8587996552689,-51.8614638127167,
-50.8641279701645,-49.8667921276122,-48.86945628506,-48.0748388990955),
 .UNSPECIFIED.);
#2644=B_SPLINE_CURVE_WITH_KNOTS('',3,(#35582,#35583,#35584,#35585,#35586,
#35587,#35588,#35589,#35590,#35591,#35592,#35593,#35594,#35595,#35596,#35597,
#35598,#35599,#35600,#35601,#35602,#35603),.UNSPECIFIED.,.F.,.F.,(4,3,3,
3,3,3,3,4),(45.0964881882866,45.9083206489841,46.9063276196142,47.9043345902443,
48.9023415608744,49.9003485315045,50.8983555021345,51.3796734954662),
 .UNSPECIFIED.);
#2645=B_SPLINE_CURVE_WITH_KNOTS('',3,(#35608,#35609,#35610,#35611,#35612,
#35613,#35614,#35615,#35616,#35617,#35618,#35619,#35620,#35621,#35622,#35623,
#35624,#35625,#35626,#35627,#35628,#35629),.UNSPECIFIED.,.F.,.F.,(4,3,3,
3,3,3,3,4),(-60.6412095134546,-59.8401505531347,-58.8428147105824,-57.8454788680302,
-56.8481430254779,-55.8508071829257,-54.8534713403734,-54.3580242062751),
 .UNSPECIFIED.);
#2646=B_SPLINE_CURVE_WITH_KNOTS('',3,(#35630,#35631,#35632,#35633,#35634,
#35635,#35636,#35637,#35638,#35639,#35640,#35641,#35642,#35643,#35644,#35645,
#35646,#35647,#35648,#35649,#35650,#35651),.UNSPECIFIED.,.F.,.F.,(4,3,3,
3,3,3,3,4),(51.3796734954662,51.8963624727646,52.8943694433947,53.8923764140248,
54.8903833846549,55.888390355285,56.8863973259151,57.6628588026458),
 .UNSPECIFIED.);
#2647=B_SPLINE_CURVE_WITH_KNOTS('',3,(#35656,#35657,#35658,#35659,#35660,
#35661,#35662,#35663,#35664,#35665,#35666,#35667,#35668,#35669,#35670,#35671,
#35672,#35673,#35674,#35675,#35676,#35677,#35678,#35679,#35680),
 .UNSPECIFIED.,.F.,.F.,(4,3,3,3,3,3,3,3,4),(-66.9243948206342,-66.8215014510004,
-65.8241656084481,-64.8268297658959,-63.8294939233436,-62.8321580807914,
-61.8348222382391,-60.8374863956869,-60.6412095134546),.UNSPECIFIED.);
#2648=B_SPLINE_CURVE_WITH_KNOTS('',3,(#35681,#35682,#35683,#35684,#35685,
#35686,#35687,#35688,#35689,#35690,#35691,#35692,#35693,#35694,#35695,#35696,
#35697,#35698,#35699,#35700,#35701,#35702,#35703,#35704,#35705),
 .UNSPECIFIED.,.F.,.F.,(4,3,3,3,3,3,3,3,4),(57.6628588026458,57.8844042965452,
58.8824112671752,59.8804182378054,60.8784252084354,61.8764321790655,62.8744391496956,
63.8724461203257,63.9460441098254),.UNSPECIFIED.);
#2649=B_SPLINE_CURVE_WITH_KNOTS('',3,(#35710,#35711,#35712,#35713,#35714,
#35715,#35716,#35717,#35718,#35719,#35720,#35721,#35722,#35723,#35724,#35725,
#35726,#35727,#35728,#35729,#35730,#35731),.UNSPECIFIED.,.F.,.F.,(4,3,3,
3,3,3,3,4),(-73.2075801278138,-72.8055165063138,-71.8081806637616,-70.8108448212093,
-69.8135089786571,-68.8161731361048,-67.8188372935526,-66.9243948206342),
 .UNSPECIFIED.);
#2650=B_SPLINE_CURVE_WITH_KNOTS('',3,(#35732,#35733,#35734,#35735,#35736,
#35737,#35738,#35739,#35740,#35741,#35742,#35743,#35744,#35745,#35746,#35747,
#35748,#35749,#35750,#35751,#35752,#35753),.UNSPECIFIED.,.F.,.F.,(4,3,3,
3,3,3,3,4),(63.9460441098254,64.8704530909558,65.8684600615859,66.866467032216,
67.8644740028461,68.8624809734761,69.8604879441062,70.229229417005),
 .UNSPECIFIED.);
#2651=B_SPLINE_CURVE_WITH_KNOTS('',3,(#35758,#35759,#35760,#35761,#35762,
#35763,#35764,#35765,#35766,#35767,#35768,#35769,#35770,#35771,#35772,#35773,
#35774,#35775,#35776,#35777,#35778,#35779),.UNSPECIFIED.,.F.,.F.,(4,3,3,
3,3,3,3,4),(-79.4907654349934,-78.7895315616273,-77.792195719075,-76.7948598765228,
-75.7975240339705,-74.8001881914183,-73.802852348866,-73.2075801278138),
 .UNSPECIFIED.);
#2652=B_SPLINE_CURVE_WITH_KNOTS('',3,(#35780,#35781,#35782,#35783,#35784,
#35785,#35786,#35787,#35788,#35789,#35790,#35791,#35792,#35793,#35794,#35795,
#35796,#35797,#35798,#35799,#35800,#35801),.UNSPECIFIED.,.F.,.F.,(4,3,3,
3,3,3,3,4),(70.229229417005,70.8584949147363,71.8565018853664,72.8545088559965,
73.8525158266266,74.8505227972567,75.8485297678868,76.5124147241846),
 .UNSPECIFIED.);
#2653=B_SPLINE_CURVE_WITH_KNOTS('',3,(#35806,#35807,#35808,#35809,#35810,
#35811,#35812,#35813,#35814,#35815,#35816,#35817,#35818,#35819,#35820,#35821,
#35822,#35823,#35824,#35825,#35826,#35827,#35828,#35829,#35830),
 .UNSPECIFIED.,.F.,.F.,(4,3,3,3,3,3,3,3,4),(-85.773950742173,-85.770882459493,
-84.7735466169407,-83.7762107743885,-82.7788749318363,-81.781539089284,
-80.7842032467318,-79.7868674041795,-79.4907654349934),.UNSPECIFIED.);
#2654=B_SPLINE_CURVE_WITH_KNOTS('',3,(#35831,#35832,#35833,#35834,#35835,
#35836,#35837,#35838,#35839,#35840,#35841,#35842,#35843,#35844,#35845,#35846,
#35847,#35848,#35849,#35850,#35851,#35852),.UNSPECIFIED.,.F.,.F.,(4,3,3,
3,3,3,3,4),(76.5124147241846,76.8465367385169,77.8445437091469,78.842550679777,
79.8405576504071,80.8385646210372,81.8365715916673,82.7956000313642),
 .UNSPECIFIED.);
#2655=B_SPLINE_CURVE_WITH_KNOTS('',3,(#35857,#35858,#35859,#35860,#35861,
#35862,#35863,#35864,#35865,#35866,#35867,#35868,#35869,#35870,#35871,#35872,
#35873,#35874,#35875,#35876,#35877,#35878),.UNSPECIFIED.,.F.,.F.,(4,3,3,
3,3,3,3,4),(-92.0571360493526,-91.7548975148065,-90.7575616722542,-89.760225829702,
-88.7628899871497,-87.7655541445975,-86.7682183020452,-85.773950742173),
 .UNSPECIFIED.);
#2656=B_SPLINE_CURVE_WITH_KNOTS('',3,(#35879,#35880,#35881,#35882,#35883,
#35884,#35885,#35886,#35887,#35888,#35889,#35890,#35891,#35892,#35893,#35894,
#35895,#35896,#35897,#35898,#35899,#35900,#35901,#35902,#35903),
 .UNSPECIFIED.,.F.,.F.,(4,3,3,3,3,3,3,3,4),(82.7956000313642,82.8345785622974,
83.8325855329275,84.8305925035576,85.8285994741877,86.8266064448178,87.8246134154479,
88.822620386078,89.0787853385438),.UNSPECIFIED.);
#2657=B_SPLINE_CURVE_WITH_KNOTS('',3,(#35908,#35909,#35910,#35911,#35912,
#35913,#35914,#35915,#35916,#35917,#35918,#35919,#35920,#35921,#35922,#35923,
#35924,#35925,#35926,#35927,#35928,#35929),.UNSPECIFIED.,.F.,.F.,(4,3,3,
3,3,3,3,4),(-98.3403213565322,-97.7389125701199,-96.7415767275677,-95.7442408850154,
-94.7469050424632,-93.7495691999109,-92.7522333573587,-92.0571360493526),
 .UNSPECIFIED.);
#2658=B_SPLINE_CURVE_WITH_KNOTS('',3,(#35930,#35931,#35932,#35933,#35934,
#35935,#35936,#35937,#35938,#35939,#35940,#35941,#35942,#35943,#35944,#35945,
#35946,#35947,#35948,#35949,#35950,#35951),.UNSPECIFIED.,.F.,.F.,(4,3,3,
3,3,3,3,4),(89.0787853385438,89.820627356708,90.8186343273381,91.8166412979682,
92.8146482685983,93.8126552392284,94.8106622098585,95.3619706457233),
 .UNSPECIFIED.);
#2659=B_SPLINE_CURVE_WITH_KNOTS('',3,(#35957,#35958,#35959,#35960,#35961,
#35962,#35963,#35964),.UNSPECIFIED.,.F.,.F.,(4,1,1,1,1,4),(109.955742875643,
110.351669931783,111.349005774335,112.346341616887,113.343677459439,114.341013301992),
 .UNSPECIFIED.);
#2660=B_SPLINE_CURVE_WITH_KNOTS('',3,(#35967,#35968,#35969,#35970,#35971,
#35972,#35973),.UNSPECIFIED.,.F.,.F.,(4,1,1,1,4),(109.955742875643,110.107297927009,
111.105304897639,112.103311868269,113.101318838899),.UNSPECIFIED.);
#2661=B_SPLINE_CURVE_WITH_KNOTS('',3,(#35978,#35979,#35980,#35981,#35982,
#35983,#35984,#35985,#35986,#35987),.UNSPECIFIED.,.F.,.F.,(4,1,1,1,1,1,
1,4),(103.672557568463,104.367654876469,105.364990719021,106.362326561574,
107.359662404126,108.356998246678,109.35433408923,109.955742875643),
 .UNSPECIFIED.);
#2662=B_SPLINE_CURVE_WITH_KNOTS('',3,(#35988,#35989,#35990,#35991,#35992,
#35993,#35994,#35995,#35996,#35997),.UNSPECIFIED.,.F.,.F.,(4,1,1,1,1,1,
1,4),(103.672557568463,104.119256103228,105.117263073858,106.115270044488,
107.113277015118,108.111283985749,109.109290956379,109.955742875643),
 .UNSPECIFIED.);
#2663=B_SPLINE_CURVE_WITH_KNOTS('',3,(#36002,#36003,#36004,#36005,#36006,
#36007,#36008,#36009,#36010,#36011),.UNSPECIFIED.,.F.,.F.,(4,1,1,1,1,1,
1,4),(97.3893722612836,98.3836398211558,99.380975663708,100.37831150626,
101.375647348812,102.372983191365,103.370319033917,103.672557568463),
 .UNSPECIFIED.);
#2664=B_SPLINE_CURVE_WITH_KNOTS('',3,(#36012,#36013,#36014,#36015,#36016,
#36017,#36018,#36019,#36020,#36021),.UNSPECIFIED.,.F.,.F.,(4,1,1,1,1,1,
1,4),(97.3893722612836,98.1312142794477,99.1292212500778,100.127228220708,
101.125235191338,102.123242161968,103.121249132598,103.672557568463),
 .UNSPECIFIED.);
#2665=B_SPLINE_CURVE_WITH_KNOTS('',3,(#36026,#36027,#36028,#36029,#36030,
#36031,#36032,#36033,#36034,#36035,#36036),.UNSPECIFIED.,.F.,.F.,(4,1,1,
1,1,1,1,1,4),(91.106186954104,91.4022889232901,92.3996247658423,93.3969606083945,
94.3942964509468,95.391632293499,96.3889681360513,97.3863039786035,97.3893722612836),
 .UNSPECIFIED.);
#2666=B_SPLINE_CURVE_WITH_KNOTS('',3,(#36037,#36038,#36039,#36040,#36041,
#36042,#36043,#36044,#36045,#36046,#36047),.UNSPECIFIED.,.F.,.F.,(4,1,1,
1,1,1,1,1,4),(91.106186954104,91.1451654850371,92.1431724556672,93.1411794262973,
94.1391863969273,95.1371933675574,96.1352003381875,97.1332073088176,97.3893722612836),
 .UNSPECIFIED.);
#2667=B_SPLINE_CURVE_WITH_KNOTS('',3,(#36052,#36053,#36054,#36055,#36056,
#36057,#36058,#36059,#36060,#36061),.UNSPECIFIED.,.F.,.F.,(4,1,1,1,1,1,
1,4),(84.8230016469244,85.4182738679766,86.4156097105288,87.4129455530811,
88.4102813956333,89.4076172381856,90.4049530807378,91.106186954104),
 .UNSPECIFIED.);
#2668=B_SPLINE_CURVE_WITH_KNOTS('',3,(#36062,#36063,#36064,#36065,#36066,
#36067,#36068,#36069,#36070,#36071),.UNSPECIFIED.,.F.,.F.,(4,1,1,1,1,1,
1,4),(84.8230016469244,85.1571236612565,86.1551306318866,87.1531376025167,
88.1511445731468,89.1491515437769,90.147158514407,91.106186954104),
 .UNSPECIFIED.);
#2669=B_SPLINE_CURVE_WITH_KNOTS('',3,(#36076,#36077,#36078,#36079,#36080,
#36081,#36082,#36083,#36084,#36085),.UNSPECIFIED.,.F.,.F.,(4,1,1,1,1,1,
1,4),(78.5398163397448,79.4342588126631,80.4315946552154,81.4289304977676,
82.4262663403199,83.4236021828721,84.4209380254243,84.8230016469244),
 .UNSPECIFIED.);
#2670=B_SPLINE_CURVE_WITH_KNOTS('',3,(#36086,#36087,#36088,#36089,#36090,
#36091,#36092,#36093,#36094,#36095),.UNSPECIFIED.,.F.,.F.,(4,1,1,1,1,1,
1,4),(78.5398163397448,79.169081837476,80.1670888081061,81.1650957787362,
82.1631027493663,83.1611097199964,84.1591166906264,84.8230016469244),
 .UNSPECIFIED.);
#2671=B_SPLINE_CURVE_WITH_KNOTS('',3,(#36100,#36101,#36102,#36103,#36104,
#36105,#36106,#36107,#36108,#36109,#36110),.UNSPECIFIED.,.F.,.F.,(4,1,1,
1,1,1,1,1,4),(72.2566310325652,72.4529079147974,73.4502437573497,74.4475795999019,
75.4449154424541,76.4422512850064,77.4395871275586,78.4369229701109,78.5398163397448),
 .UNSPECIFIED.);
#2672=B_SPLINE_CURVE_WITH_KNOTS('',3,(#36111,#36112,#36113,#36114,#36115,
#36116,#36117,#36118,#36119,#36120),.UNSPECIFIED.,.F.,.F.,(4,1,1,1,1,1,
1,4),(72.2566310325652,73.1810400136955,74.1790469843256,75.1770539549557,
76.1750609255857,77.1730678962158,78.1710748668459,78.5398163397448),
 .UNSPECIFIED.);
#2673=B_SPLINE_CURVE_WITH_KNOTS('',3,(#36125,#36126,#36127,#36128,#36129,
#36130,#36131,#36132,#36133,#36134),.UNSPECIFIED.,.F.,.F.,(4,1,1,1,1,1,
1,4),(65.9734457253856,66.468892859484,67.4662287020362,68.4635645445884,
69.4609003871407,70.4582362296929,71.4555720722452,72.2566310325652),
 .UNSPECIFIED.);
#2674=B_SPLINE_CURVE_WITH_KNOTS('',3,(#36135,#36136,#36137,#36138,#36139,
#36140,#36141,#36142,#36143,#36144,#36145),.UNSPECIFIED.,.F.,.F.,(4,1,1,
1,1,1,1,1,4),(65.9734457253856,66.1949912192848,67.1929981899149,68.191005160545,
69.1890121311751,70.1870191018052,71.1850260724353,72.1830330430654,72.2566310325652),
 .UNSPECIFIED.);
#2675=B_SPLINE_CURVE_WITH_KNOTS('',3,(#36150,#36151,#36152,#36153,#36154,
#36155,#36156,#36157,#36158,#36159),.UNSPECIFIED.,.F.,.F.,(4,1,1,1,1,1,
1,4),(59.690260418206,60.4848778041705,61.4822136467227,62.479549489275,
63.4768853318272,64.4742211743795,65.4715570169317,65.9734457253856),
 .UNSPECIFIED.);
#2676=B_SPLINE_CURVE_WITH_KNOTS('',3,(#36160,#36161,#36162,#36163,#36164,
#36165,#36166,#36167,#36168,#36169),.UNSPECIFIED.,.F.,.F.,(4,1,1,1,1,1,
1,4),(59.690260418206,60.2069493955043,61.2049563661344,62.2029633367645,
63.2009703073946,64.1989772780247,65.1969842486548,65.9734457253856),
 .UNSPECIFIED.);
#2677=B_SPLINE_CURVE_WITH_KNOTS('',3,(#36174,#36175,#36176,#36177,#36178,
#36179,#36180,#36181,#36182,#36183,#36184),.UNSPECIFIED.,.F.,.F.,(4,1,1,
1,1,1,1,1,4),(53.4070751110265,53.5035269063048,54.500862748857,55.4981985914093,
56.4955344339615,57.4928702765138,58.490206119066,59.4875419616182,59.690260418206),
 .UNSPECIFIED.);
#2678=B_SPLINE_CURVE_WITH_KNOTS('',3,(#36185,#36186,#36187,#36188,#36189,
#36190,#36191,#36192,#36193,#36194),.UNSPECIFIED.,.F.,.F.,(4,1,1,1,1,1,
1,4),(53.4070751110264,54.2189075717238,55.2169145423539,56.214921512984,
57.212928483614,58.2109354542441,59.2089424248742,59.690260418206),
 .UNSPECIFIED.);
#2679=B_SPLINE_CURVE_WITH_KNOTS('',3,(#36199,#36200,#36201,#36202,#36203,
#36204,#36205,#36206,#36207,#36208),.UNSPECIFIED.,.F.,.F.,(4,1,1,1,1,1,
1,4),(47.1238898038469,47.5195118509913,48.5168476935436,49.5141835360958,
50.5115193786481,51.5088552212003,52.5061910637525,53.4070751110265),
 .UNSPECIFIED.);
#2680=B_SPLINE_CURVE_WITH_KNOTS('',3,(#36209,#36210,#36211,#36212,#36213,
#36214,#36215,#36216,#36217,#36218,#36219),.UNSPECIFIED.,.F.,.F.,(4,1,1,
1,1,1,1,1,4),(47.1238898038468,47.2328587773132,48.2308657479432,49.2288727185733,
50.2268796892034,51.2248866598335,52.2228936304636,53.2209006010937,53.4070751110264),
 .UNSPECIFIED.);
#2681=B_SPLINE_CURVE_WITH_KNOTS('',3,(#36224,#36225,#36226,#36227,#36228,
#36229,#36230,#36231,#36232,#36233),.UNSPECIFIED.,.F.,.F.,(4,1,1,1,1,1,
1,4),(40.8407044966673,41.5354967956779,42.5328326382301,43.5301684807823,
44.5275043233346,45.5248401658868,46.5221760084391,47.1238898038469),
 .UNSPECIFIED.);
#2682=B_SPLINE_CURVE_WITH_KNOTS('',3,(#36234,#36235,#36236,#36237,#36238,
#36239,#36240,#36241,#36242,#36243),.UNSPECIFIED.,.F.,.F.,(4,1,1,1,1,1,
1,4),(40.8407044966672,41.2448169535326,42.2428239241627,43.2408308947928,
44.2388378654229,45.236844836053,46.2348518066831,47.1238898038468),
 .UNSPECIFIED.);
#2683=B_SPLINE_CURVE_WITH_KNOTS('',3,(#36248,#36249,#36250,#36251,#36252,
#36253,#36254,#36255,#36256,#36257),.UNSPECIFIED.,.F.,.F.,(4,1,1,1,1,1,
1,4),(34.5575191894877,35.5514817403644,36.5488175829166,37.5461534254689,
38.5434892680211,39.5408251105734,40.5381609531256,40.8407044966673),
 .UNSPECIFIED.);
#2684=B_SPLINE_CURVE_WITH_KNOTS('',3,(#36258,#36259,#36260,#36261,#36262,
#36263,#36264,#36265,#36266,#36267),.UNSPECIFIED.,.F.,.F.,(4,1,1,1,1,1,
1,4),(34.5575191894876,35.2567751297521,36.2547821003822,37.2527890710123,
38.2507960416424,39.2488030122724,40.2468099829025,40.8407044966672),
 .UNSPECIFIED.);
#2685=B_SPLINE_CURVE_WITH_KNOTS('',3,(#36272,#36273,#36274,#36275,#36276,
#36277,#36278,#36279,#36280,#36281,#36282),.UNSPECIFIED.,.F.,.F.,(4,1,1,
1,1,1,1,1,4),(28.2743338823081,28.5701308424987,29.5674666850509,30.5648025276032,
31.5621383701554,32.5594742127077,33.5568100552599,34.5541458978121,34.5575191894877),
 .UNSPECIFIED.);
#2686=B_SPLINE_CURVE_WITH_KNOTS('',3,(#36283,#36284,#36285,#36286,#36287,
#36288,#36289,#36290,#36291,#36292),.UNSPECIFIED.,.F.,.F.,(4,1,1,1,1,1,
1,4),(28.274333882308,29.2687333059716,30.2667402766016,31.2647472472317,
32.2627542178618,33.2607611884919,34.258768159122,34.5575191894876),
 .UNSPECIFIED.);
#2687=B_SPLINE_CURVE_WITH_KNOTS('',3,(#36297,#36298,#36299,#36300,#36301,
#36302,#36303,#36304,#36305,#36306),.UNSPECIFIED.,.F.,.F.,(4,1,1,1,1,1,
1,4),(21.9911485751285,22.5861157871852,23.5834516297375,24.5807874722897,
25.5781233148419,26.5754591573942,27.5727949999464,28.2743338823081),
 .UNSPECIFIED.);
#2688=B_SPLINE_CURVE_WITH_KNOTS('',3,(#36307,#36308,#36309,#36310,#36311,
#36312,#36313,#36314,#36315,#36316,#36317),.UNSPECIFIED.,.F.,.F.,(4,1,1,
1,1,1,1,1,4),(21.9911485751285,22.2826845115609,23.280691482191,24.2786984528211,
25.2767054234512,26.2747123940813,27.2727193647114,28.2707263353415,28.274333882308),
 .UNSPECIFIED.);
#2689=B_SPLINE_CURVE_WITH_KNOTS('',3,(#36322,#36323,#36324,#36325,#36326,
#36327,#36328,#36329,#36330,#36331),.UNSPECIFIED.,.F.,.F.,(4,1,1,1,1,1,
1,4),(15.7079632679489,16.6021007318718,17.599436574424,18.5967724169762,
19.5941082595285,20.5914441020807,21.588779944633,21.9911485751285),
 .UNSPECIFIED.);
#2690=B_SPLINE_CURVE_WITH_KNOTS('',3,(#36332,#36333,#36334,#36335,#36336,
#36337,#36338,#36339,#36340,#36341),.UNSPECIFIED.,.F.,.F.,(4,1,1,1,1,1,
1,4),(15.7079632679489,16.2946426877804,17.2926496584105,18.2906566290406,
19.2886635996707,20.2866705703008,21.2846775409308,21.9911485751285),
 .UNSPECIFIED.);
#2691=B_SPLINE_CURVE_WITH_KNOTS('',3,(#36344,#36345,#36346,#36347,#36348,
#36349,#36350,#36351,#36352,#36353,#36354,#36355,#36356,#36357,#36358,#36359,
#36360,#36361,#36362,#36363,#36364,#36365,#36366,#36367,#36368,#36369,#36370,
#36371,#36372,#36373,#36374,#36375,#36376,#36377,#36378,#36379,#36380,#36381,
#36382,#36383,#36384,#36385,#36386,#36387,#36388,#36389,#36390,#36391,#36392,
#36393,#36394,#36395,#36396,#36397,#36398,#36399,#36400,#36401,#36402,#36403,
#36404,#36405,#36406,#36407,#36408,#36409,#36410,#36411,#36412,#36413,#36414,
#36415,#36416,#36417,#36418,#36419,#36420,#36421,#36422,#36423,#36424,#36425,
#36426,#36427,#36428,#36429,#36430,#36431,#36432,#36433,#36434,#36435,#36436,
#36437,#36438,#36439,#36440,#36441,#36442,#36443,#36444,#36445,#36446,#36447,
#36448,#36449,#36450,#36451,#36452,#36453,#36454,#36455,#36456,#36457,#36458,
#36459,#36460,#36461,#36462,#36463,#36464,#36465,#36466,#36467,#36468,#36469,
#36470),.UNSPECIFIED.,.F.,.F.,(4,3,3,3,3,3,3,3,3,3,3,3,3,3,3,3,3,3,3,3,
3,3,3,3,3,3,3,3,3,3,3,3,3,3,3,3,3,3,3,3,3,3,4),(-0.996917990983956,-0.978871588953361,
-0.96111138213616,-0.951572166884024,-0.94788730271085,-0.928958746515757,
-0.909876465942473,-0.904936500084987,-0.901848009849201,-0.882541837721487,
-0.863353532865677,-0.850071733640713,-0.842096384739765,-0.838733342910066,
-0.836789934415749,-0.818254783653573,-0.798902591036692,-0.782735584954257,
-0.778204258927876,-0.774298497031817,-0.75473106557298,-0.734923369072796,
-0.7185841623989,-0.712646708603056,-0.709110058221935,-0.689189804001172,
-0.669566542377212,-0.649891129487148,-0.644972000047888,-0.641670824784499,
-0.621885476350888,-0.601705353300825,-0.588427767916722,-0.579820295317846,
-0.575107459303169,-0.554609906499435,-0.53420632583291,-0.514845498030454,
-0.510394870356688,-0.506773348856668,-0.495484670227998,-0.475532816008266,
-0.468408511919796),.UNSPECIFIED.);
#2692=B_SPLINE_CURVE_WITH_KNOTS('',3,(#36472,#36473,#36474,#36475,#36476,
#36477,#36478,#36479,#36480,#36481,#36482,#36483,#36484,#36485,#36486,#36487,
#36488,#36489,#36490,#36491,#36492,#36493,#36494,#36495,#36496,#36497,#36498,
#36499,#36500,#36501,#36502,#36503,#36504,#36505,#36506,#36507,#36508,#36509,
#36510,#36511,#36512,#36513,#36514,#36515,#36516,#36517,#36518,#36519,#36520,
#36521,#36522,#36523,#36524,#36525,#36526,#36527,#36528,#36529),
 .UNSPECIFIED.,.F.,.F.,(4,3,3,3,3,3,3,3,3,3,3,3,3,3,3,3,3,3,3,4),(-0.271362855059921,
-0.249815156703991,-0.228817954605844,-0.214757059032555,-0.202695986178297,
-0.199258382274391,-0.179079040584676,-0.172574372312687,-0.151002575773601,
-0.132127253801901,-0.128545223737615,-0.108660382312346,-0.0889046320299183,
-0.0695673553379917,-0.0643976613730527,-0.0611873083345303,-0.0424332578302701,
-0.0240014673407122,-0.00610701619818059,0.),.UNSPECIFIED.);
#2693=B_SPLINE_CURVE_WITH_KNOTS('',3,(#36532,#36533,#36534,#36535,#36536,
#36537,#36538,#36539,#36540,#36541,#36542,#36543,#36544,#36545,#36546,#36547,
#36548,#36549,#36550,#36551,#36552,#36553,#36554,#36555,#36556,#36557,#36558,
#36559,#36560,#36561,#36562,#36563,#36564,#36565,#36566,#36567,#36568,#36569,
#36570,#36571,#36572,#36573,#36574,#36575,#36576,#36577,#36578,#36579,#36580,
#36581,#36582,#36583,#36584,#36585,#36586,#36587,#36588,#36589,#36590,#36591,
#36592,#36593,#36594,#36595,#36596,#36597,#36598,#36599,#36600,#36601,#36602,
#36603,#36604,#36605,#36606,#36607,#36608,#36609,#36610,#36611,#36612,#36613,
#36614,#36615,#36616,#36617,#36618,#36619,#36620,#36621,#36622,#36623,#36624,
#36625,#36626,#36627,#36628,#36629,#36630,#36631,#36632,#36633,#36634),
 .UNSPECIFIED.,.F.,.F.,(4,3,3,3,3,3,3,3,3,3,3,3,3,3,3,3,3,3,3,3,3,3,3,3,
3,3,3,3,3,3,3,3,3,3,4),(-0.468408511919796,-0.449159592277506,-0.442679572366002,
-0.439139523917826,-0.418501747794262,-0.397540534942074,-0.376759689901926,
-0.369408338867191,-0.366188435771172,-0.344993296658329,-0.324164935680159,
-0.314417154781481,-0.302674036643168,-0.298303152413865,-0.294792657786698,
-0.273759483634418,-0.252453791079512,-0.23671297526563,-0.228622459040654,
-0.22484613779528,-0.221071692886511,-0.199520974492535,-0.177947952659577,
-0.156760757052952,-0.151824997028116,-0.148277425274246,-0.12652726456846,
-0.105236270462937,-0.0835127492652271,-0.0784406535722348,-0.0733870619889256,
-0.0516031153801045,-0.029512914496819,-0.0074997402847098,0.),
 .UNSPECIFIED.);
#2694=B_SPLINE_CURVE_WITH_KNOTS('',3,(#37063,#37064,#37065,#37066,#37067,
#37068,#37069,#37070),.UNSPECIFIED.,.F.,.F.,(4,1,1,1,1,4),(11.6154215191105,
12.6127573616628,13.610093204215,14.6074290467673,15.6047648893195,15.7079632679489),
 .UNSPECIFIED.);
#2695=B_SPLINE_CURVE_WITH_KNOTS('',3,(#37071,#37072,#37073,#37074,#37075,
#37076,#37077,#37078,#37079,#37080,#37081,#37082,#37083,#37084,#37085,#37086,
#37087,#37088,#37089,#37090,#37091,#37092,#37093,#37094,#37095,#37096,#37097,
#37098,#37099,#37100,#37101,#37102,#37103,#37104,#37105,#37106,#37107,#37108,
#37109,#37110,#37111,#37112,#37113,#37114,#37115,#37116,#37117,#37118,#37119,
#37120,#37121,#37122,#37123,#37124,#37125,#37126,#37127,#37128,#37129,#37130,
#37131,#37132,#37133,#37134,#37135,#37136,#37137,#37138,#37139,#37140,#37141,
#37142,#37143,#37144,#37145,#37146,#37147,#37148,#37149,#37150,#37151,#37152,
#37153,#37154,#37155),.UNSPECIFIED.,.F.,.F.,(4,3,3,3,3,3,3,3,3,3,3,3,3,
3,3,3,3,3,3,3,3,3,3,3,3,3,3,3,4),(-0.364629307890661,-0.350885759085945,
-0.329296488089375,-0.318978386270927,-0.313741431878983,-0.309365163672801,
-0.288042901568511,-0.272809238661881,-0.264006177467146,-0.26029818106468,
-0.239567096461013,-0.219346880276472,-0.206053559786221,-0.194876880502573,
-0.191399047668888,-0.171813366976952,-0.166173598315468,-0.145401898526034,
-0.126706873608775,-0.123379860192083,-0.103925496661725,-0.0845481894111439,
-0.065567586070534,-0.0621782887363481,-0.05894467115978,-0.0403543924373443,
-0.0220984153978596,-0.00442511140790438,0.),.UNSPECIFIED.);
#2696=B_SPLINE_CURVE_WITH_KNOTS('',3,(#37156,#37157,#37158,#37159,#37160,
#37161,#37162,#37163,#37164,#37165,#37166,#37167,#37168),.UNSPECIFIED.,
 .F.,.F.,(4,3,3,3,4),(-101.213804280572,-100.730920097777,-99.7335842552244,
-98.7362484126722,-98.3403213565322),.UNSPECIFIED.);
#2697=B_SPLINE_CURVE_WITH_KNOTS('',3,(#37171,#37172,#37173,#37174,#37175,
#37176,#37177,#37178,#37179),.UNSPECIFIED.,.F.,.F.,(4,1,1,1,1,1,4),(10.3757270560178,
11.30460783463,12.30261480526,13.3006217758901,14.2986287465202,15.2966357171503,
15.7079632679489),.UNSPECIFIED.);
#2698=B_SPLINE_CURVE_WITH_KNOTS('',3,(#37613,#37614,#37615,#37616,#37617,
#37618,#37619,#37620,#37621,#37622,#37623,#37624,#37625,#37626,#37627,#37628),
 .UNSPECIFIED.,.F.,.F.,(4,3,3,3,3,4),(95.3619706457233,95.8086691804886,
96.8066761511186,97.8046831217487,98.8026900923788,99.1486641472938),
 .UNSPECIFIED.);
#2699=B_SPLINE_CURVE_WITH_KNOTS('',3,(#37629,#37630,#37631,#37632,#37633,
#37634,#37635,#37636,#37637,#37638,#37639,#37640,#37641,#37642,#37643,#37644,
#37645,#37646,#37647,#37648,#37649,#37650,#37651,#37652,#37653,#37654,#37655,
#37656,#37657,#37658,#37659,#37660,#37661,#37662,#37663,#37664,#37665,#37666,
#37667,#37668,#37669,#37670,#37671,#37672,#37673,#37674,#37675,#37676,#37677,
#37678,#37679,#37680,#37681,#37682,#37683,#37684,#37685,#37686,#37687,#37688,
#37689,#37690,#37691,#37692,#37693,#37694,#37695,#37696,#37697,#37698,#37699,
#37700,#37701,#37702,#37703,#37704,#37705,#37706,#37707,#37708,#37709,#37710,
#37711,#37712,#37713),.UNSPECIFIED.,.F.,.F.,(4,3,3,3,3,3,3,3,3,3,3,3,3,
3,3,3,3,3,3,3,3,3,3,3,3,3,3,3,4),(-0.366397579005845,-0.355461226466819,
-0.337490969642209,-0.327214164040339,-0.321649482146298,-0.302840833811487,
-0.288386907394637,-0.281257238921911,-0.277593927902022,-0.258153123971634,
-0.238335729520815,-0.225554152759783,-0.218411056976172,-0.214856426708649,
-0.194426531587897,-0.187209422476688,-0.167504451243421,-0.156894426252658,
-0.149523127563347,-0.145921626399787,-0.125494957624892,-0.104619107174947,
-0.0835512936559854,-0.0752831225832569,-0.0721648689176682,-0.0505208253811386,
-0.028827309118007,-0.00759789023731293,0.),.UNSPECIFIED.);
#3213=LINE('',#35187,#3751);
#3214=LINE('',#35211,#3752);
#3215=LINE('',#35259,#3753);
#3216=LINE('',#35307,#3754);
#3217=LINE('',#35361,#3755);
#3218=LINE('',#35409,#3756);
#3219=LINE('',#35457,#3757);
#3220=LINE('',#35505,#3758);
#3221=LINE('',#35559,#3759);
#3222=LINE('',#35607,#3760);
#3223=LINE('',#35655,#3761);
#3224=LINE('',#35709,#3762);
#3225=LINE('',#35757,#3763);
#3226=LINE('',#35805,#3764);
#3227=LINE('',#35856,#3765);
#3228=LINE('',#35907,#3766);
#3229=LINE('',#35955,#3767);
#3230=LINE('',#35977,#3768);
#3231=LINE('',#36001,#3769);
#3232=LINE('',#36025,#3770);
#3233=LINE('',#36051,#3771);
#3234=LINE('',#36075,#3772);
#3235=LINE('',#36099,#3773);
#3236=LINE('',#36124,#3774);
#3237=LINE('',#36149,#3775);
#3238=LINE('',#36173,#3776);
#3239=LINE('',#36198,#3777);
#3240=LINE('',#36223,#3778);
#3241=LINE('',#36247,#3779);
#3242=LINE('',#36271,#3780);
#3243=LINE('',#36296,#3781);
#3244=LINE('',#36321,#3782);
#3245=LINE('',#36636,#3783);
#3246=LINE('',#37718,#3784);
#3247=LINE('',#37720,#3785);
#3248=LINE('',#37722,#3786);
#3249=LINE('',#37723,#3787);
#3250=LINE('',#37726,#3788);
#3251=LINE('',#37728,#3789);
#3252=LINE('',#37729,#3790);
#3253=LINE('',#37732,#3791);
#3254=LINE('',#37734,#3792);
#3255=LINE('',#37735,#3793);
#3256=LINE('',#37738,#3794);
#3257=LINE('',#37740,#3795);
#3258=LINE('',#37741,#3796);
#3259=LINE('',#37744,#3797);
#3260=LINE('',#37746,#3798);
#3261=LINE('',#37747,#3799);
#3262=LINE('',#37749,#3800);
#3263=LINE('',#37750,#3801);
#3264=LINE('',#37757,#3802);
#3751=VECTOR('',#12838,2.);
#3752=VECTOR('',#12843,2.);
#3753=VECTOR('',#12846,2.);
#3754=VECTOR('',#12849,2.);
#3755=VECTOR('',#12852,2.);
#3756=VECTOR('',#12855,2.);
#3757=VECTOR('',#12858,2.);
#3758=VECTOR('',#12861,2.);
#3759=VECTOR('',#12864,2.);
#3760=VECTOR('',#12867,2.);
#3761=VECTOR('',#12870,2.);
#3762=VECTOR('',#12873,2.);
#3763=VECTOR('',#12876,2.);
#3764=VECTOR('',#12879,2.);
#3765=VECTOR('',#12882,2.);
#3766=VECTOR('',#12885,2.);
#3767=VECTOR('',#12888,1.5555);
#3768=VECTOR('',#12893,1.5555);
#3769=VECTOR('',#12896,1.5555);
#3770=VECTOR('',#12899,1.5555);
#3771=VECTOR('',#12902,1.5555);
#3772=VECTOR('',#12905,1.5555);
#3773=VECTOR('',#12908,1.5555);
#3774=VECTOR('',#12911,1.5555);
#3775=VECTOR('',#12914,1.5555);
#3776=VECTOR('',#12917,1.5555);
#3777=VECTOR('',#12920,1.5555);
#3778=VECTOR('',#12923,1.5555);
#3779=VECTOR('',#12926,1.5555);
#3780=VECTOR('',#12929,1.5555);
#3781=VECTOR('',#12932,1.5555);
#3782=VECTOR('',#12935,1.5555);
#3783=VECTOR('',#12940,1.5);
#3784=VECTOR('',#12951,10.);
#3785=VECTOR('',#12952,10.);
#3786=VECTOR('',#12953,10.);
#3787=VECTOR('',#12954,10.);
#3788=VECTOR('',#12957,10.);
#3789=VECTOR('',#12958,10.);
#3790=VECTOR('',#12959,10.);
#3791=VECTOR('',#12962,10.);
#3792=VECTOR('',#12963,10.);
#3793=VECTOR('',#12964,10.);
#3794=VECTOR('',#12967,10.);
#3795=VECTOR('',#12968,10.);
#3796=VECTOR('',#12969,10.);
#3797=VECTOR('',#12972,10.);
#3798=VECTOR('',#12973,10.);
#3799=VECTOR('',#12974,10.);
#3800=VECTOR('',#12977,10.);
#3801=VECTOR('',#12978,10.);
#3802=VECTOR('',#12987,3.5);
#4653=VERTEX_POINT('',#35185);
#4654=VERTEX_POINT('',#35186);
#4655=VERTEX_POINT('',#35188);
#4656=VERTEX_POINT('',#35199);
#4657=VERTEX_POINT('',#35209);
#4658=VERTEX_POINT('',#35210);
#4659=VERTEX_POINT('',#35257);
#4660=VERTEX_POINT('',#35258);
#4661=VERTEX_POINT('',#35305);
#4662=VERTEX_POINT('',#35306);
#4663=VERTEX_POINT('',#35359);
#4664=VERTEX_POINT('',#35360);
#4665=VERTEX_POINT('',#35407);
#4666=VERTEX_POINT('',#35408);
#4667=VERTEX_POINT('',#35455);
#4668=VERTEX_POINT('',#35456);
#4669=VERTEX_POINT('',#35503);
#4670=VERTEX_POINT('',#35504);
#4671=VERTEX_POINT('',#35557);
#4672=VERTEX_POINT('',#35558);
#4673=VERTEX_POINT('',#35605);
#4674=VERTEX_POINT('',#35606);
#4675=VERTEX_POINT('',#35653);
#4676=VERTEX_POINT('',#35654);
#4677=VERTEX_POINT('',#35707);
#4678=VERTEX_POINT('',#35708);
#4679=VERTEX_POINT('',#35755);
#4680=VERTEX_POINT('',#35756);
#4681=VERTEX_POINT('',#35803);
#4682=VERTEX_POINT('',#35804);
#4683=VERTEX_POINT('',#35854);
#4684=VERTEX_POINT('',#35855);
#4685=VERTEX_POINT('',#35905);
#4686=VERTEX_POINT('',#35906);
#4687=VERTEX_POINT('',#35953);
#4688=VERTEX_POINT('',#35954);
#4689=VERTEX_POINT('',#35956);
#4690=VERTEX_POINT('',#35965);
#4691=VERTEX_POINT('',#35975);
#4692=VERTEX_POINT('',#35976);
#4693=VERTEX_POINT('',#35999);
#4694=VERTEX_POINT('',#36000);
#4695=VERTEX_POINT('',#36023);
#4696=VERTEX_POINT('',#36024);
#4697=VERTEX_POINT('',#36049);
#4698=VERTEX_POINT('',#36050);
#4699=VERTEX_POINT('',#36073);
#4700=VERTEX_POINT('',#36074);
#4701=VERTEX_POINT('',#36097);
#4702=VERTEX_POINT('',#36098);
#4703=VERTEX_POINT('',#36122);
#4704=VERTEX_POINT('',#36123);
#4705=VERTEX_POINT('',#36147);
#4706=VERTEX_POINT('',#36148);
#4707=VERTEX_POINT('',#36171);
#4708=VERTEX_POINT('',#36172);
#4709=VERTEX_POINT('',#36196);
#4710=VERTEX_POINT('',#36197);
#4711=VERTEX_POINT('',#36221);
#4712=VERTEX_POINT('',#36222);
#4713=VERTEX_POINT('',#36245);
#4714=VERTEX_POINT('',#36246);
#4715=VERTEX_POINT('',#36269);
#4716=VERTEX_POINT('',#36270);
#4717=VERTEX_POINT('',#36294);
#4718=VERTEX_POINT('',#36295);
#4719=VERTEX_POINT('',#36319);
#4720=VERTEX_POINT('',#36320);
#4721=VERTEX_POINT('',#36343);
#4722=VERTEX_POINT('',#36471);
#4723=VERTEX_POINT('',#36530);
#4724=VERTEX_POINT('',#36635);
#4725=VERTEX_POINT('',#37062);
#4726=VERTEX_POINT('',#37170);
#4727=VERTEX_POINT('',#37716);
#4728=VERTEX_POINT('',#37717);
#4729=VERTEX_POINT('',#37719);
#4730=VERTEX_POINT('',#37721);
#4731=VERTEX_POINT('',#37725);
#4732=VERTEX_POINT('',#37727);
#4733=VERTEX_POINT('',#37731);
#4734=VERTEX_POINT('',#37733);
#4735=VERTEX_POINT('',#37737);
#4736=VERTEX_POINT('',#37739);
#4737=VERTEX_POINT('',#37743);
#4738=VERTEX_POINT('',#37745);
#4739=VERTEX_POINT('',#37753);
#4740=VERTEX_POINT('',#37756);
#6053=EDGE_CURVE('',#4653,#4654,#3213,.T.);
#6054=EDGE_CURVE('',#4653,#4655,#2627,.T.);
#6055=EDGE_CURVE('',#4655,#4656,#1981,.F.);
#6056=EDGE_CURVE('',#4656,#4654,#2628,.T.);
#6057=EDGE_CURVE('',#4657,#4658,#3214,.T.);
#6058=EDGE_CURVE('',#4657,#4653,#2629,.T.);
#6059=EDGE_CURVE('',#4654,#4658,#2630,.T.);
#6060=EDGE_CURVE('',#4659,#4660,#3215,.T.);
#6061=EDGE_CURVE('',#4659,#4657,#2631,.T.);
#6062=EDGE_CURVE('',#4658,#4660,#2632,.T.);
#6063=EDGE_CURVE('',#4661,#4662,#3216,.T.);
#6064=EDGE_CURVE('',#4661,#4659,#2633,.T.);
#6065=EDGE_CURVE('',#4660,#4662,#2634,.T.);
#6066=EDGE_CURVE('',#4663,#4664,#3217,.T.);
#6067=EDGE_CURVE('',#4663,#4661,#2635,.T.);
#6068=EDGE_CURVE('',#4662,#4664,#2636,.T.);
#6069=EDGE_CURVE('',#4665,#4666,#3218,.T.);
#6070=EDGE_CURVE('',#4665,#4663,#2637,.T.);
#6071=EDGE_CURVE('',#4664,#4666,#2638,.T.);
#6072=EDGE_CURVE('',#4667,#4668,#3219,.T.);
#6073=EDGE_CURVE('',#4667,#4665,#2639,.T.);
#6074=EDGE_CURVE('',#4666,#4668,#2640,.T.);
#6075=EDGE_CURVE('',#4669,#4670,#3220,.T.);
#6076=EDGE_CURVE('',#4669,#4667,#2641,.T.);
#6077=EDGE_CURVE('',#4668,#4670,#2642,.T.);
#6078=EDGE_CURVE('',#4671,#4672,#3221,.T.);
#6079=EDGE_CURVE('',#4671,#4669,#2643,.T.);
#6080=EDGE_CURVE('',#4670,#4672,#2644,.T.);
#6081=EDGE_CURVE('',#4673,#4674,#3222,.T.);
#6082=EDGE_CURVE('',#4673,#4671,#2645,.T.);
#6083=EDGE_CURVE('',#4672,#4674,#2646,.T.);
#6084=EDGE_CURVE('',#4675,#4676,#3223,.T.);
#6085=EDGE_CURVE('',#4675,#4673,#2647,.T.);
#6086=EDGE_CURVE('',#4674,#4676,#2648,.T.);
#6087=EDGE_CURVE('',#4677,#4678,#3224,.T.);
#6088=EDGE_CURVE('',#4677,#4675,#2649,.T.);
#6089=EDGE_CURVE('',#4676,#4678,#2650,.T.);
#6090=EDGE_CURVE('',#4679,#4680,#3225,.T.);
#6091=EDGE_CURVE('',#4679,#4677,#2651,.T.);
#6092=EDGE_CURVE('',#4678,#4680,#2652,.T.);
#6093=EDGE_CURVE('',#4681,#4682,#3226,.T.);
#6094=EDGE_CURVE('',#4681,#4679,#2653,.T.);
#6095=EDGE_CURVE('',#4680,#4682,#2654,.T.);
#6096=EDGE_CURVE('',#4683,#4684,#3227,.T.);
#6097=EDGE_CURVE('',#4683,#4681,#2655,.T.);
#6098=EDGE_CURVE('',#4682,#4684,#2656,.T.);
#6099=EDGE_CURVE('',#4685,#4686,#3228,.T.);
#6100=EDGE_CURVE('',#4685,#4683,#2657,.T.);
#6101=EDGE_CURVE('',#4684,#4686,#2658,.T.);
#6102=EDGE_CURVE('',#4687,#4688,#3229,.T.);
#6103=EDGE_CURVE('',#4687,#4689,#2659,.T.);
#6104=EDGE_CURVE('',#4689,#4690,#1982,.T.);
#6105=EDGE_CURVE('',#4688,#4690,#2660,.T.);
#6106=EDGE_CURVE('',#4691,#4692,#3230,.T.);
#6107=EDGE_CURVE('',#4691,#4687,#2661,.T.);
#6108=EDGE_CURVE('',#4692,#4688,#2662,.T.);
#6109=EDGE_CURVE('',#4693,#4694,#3231,.T.);
#6110=EDGE_CURVE('',#4693,#4691,#2663,.T.);
#6111=EDGE_CURVE('',#4694,#4692,#2664,.T.);
#6112=EDGE_CURVE('',#4695,#4696,#3232,.T.);
#6113=EDGE_CURVE('',#4695,#4693,#2665,.T.);
#6114=EDGE_CURVE('',#4696,#4694,#2666,.T.);
#6115=EDGE_CURVE('',#4697,#4698,#3233,.T.);
#6116=EDGE_CURVE('',#4697,#4695,#2667,.T.);
#6117=EDGE_CURVE('',#4698,#4696,#2668,.T.);
#6118=EDGE_CURVE('',#4699,#4700,#3234,.T.);
#6119=EDGE_CURVE('',#4699,#4697,#2669,.T.);
#6120=EDGE_CURVE('',#4700,#4698,#2670,.T.);
#6121=EDGE_CURVE('',#4701,#4702,#3235,.T.);
#6122=EDGE_CURVE('',#4701,#4699,#2671,.T.);
#6123=EDGE_CURVE('',#4702,#4700,#2672,.T.);
#6124=EDGE_CURVE('',#4703,#4704,#3236,.T.);
#6125=EDGE_CURVE('',#4703,#4701,#2673,.T.);
#6126=EDGE_CURVE('',#4704,#4702,#2674,.T.);
#6127=EDGE_CURVE('',#4705,#4706,#3237,.T.);
#6128=EDGE_CURVE('',#4705,#4703,#2675,.T.);
#6129=EDGE_CURVE('',#4706,#4704,#2676,.T.);
#6130=EDGE_CURVE('',#4707,#4708,#3238,.T.);
#6131=EDGE_CURVE('',#4707,#4705,#2677,.T.);
#6132=EDGE_CURVE('',#4708,#4706,#2678,.T.);
#6133=EDGE_CURVE('',#4709,#4710,#3239,.T.);
#6134=EDGE_CURVE('',#4709,#4707,#2679,.T.);
#6135=EDGE_CURVE('',#4710,#4708,#2680,.T.);
#6136=EDGE_CURVE('',#4711,#4712,#3240,.T.);
#6137=EDGE_CURVE('',#4711,#4709,#2681,.T.);
#6138=EDGE_CURVE('',#4712,#4710,#2682,.T.);
#6139=EDGE_CURVE('',#4713,#4714,#3241,.T.);
#6140=EDGE_CURVE('',#4713,#4711,#2683,.T.);
#6141=EDGE_CURVE('',#4714,#4712,#2684,.T.);
#6142=EDGE_CURVE('',#4715,#4716,#3242,.T.);
#6143=EDGE_CURVE('',#4715,#4713,#2685,.T.);
#6144=EDGE_CURVE('',#4716,#4714,#2686,.T.);
#6145=EDGE_CURVE('',#4717,#4718,#3243,.T.);
#6146=EDGE_CURVE('',#4717,#4715,#2687,.T.);
#6147=EDGE_CURVE('',#4718,#4716,#2688,.T.);
#6148=EDGE_CURVE('',#4719,#4720,#3244,.T.);
#6149=EDGE_CURVE('',#4719,#4717,#2689,.T.);
#6150=EDGE_CURVE('',#4720,#4718,#2690,.T.);
#6151=EDGE_CURVE('',#4690,#4721,#2691,.T.);
#6152=EDGE_CURVE('',#4722,#4689,#2692,.T.);
#6153=EDGE_CURVE('',#4723,#4722,#1983,.T.);
#6154=EDGE_CURVE('',#4721,#4723,#2693,.T.);
#6155=EDGE_CURVE('',#4721,#4724,#3245,.T.);
#6156=EDGE_CURVE('',#4724,#4724,#1984,.T.);
#6157=EDGE_CURVE('',#4725,#4719,#2694,.T.);
#6158=EDGE_CURVE('',#4655,#4725,#2695,.T.);
#6159=EDGE_CURVE('',#4722,#4685,#2696,.T.);
#6160=EDGE_CURVE('',#4726,#4720,#2697,.T.);
#6161=EDGE_CURVE('',#4725,#4726,#1985,.T.);
#6162=EDGE_CURVE('',#4686,#4723,#2698,.T.);
#6163=EDGE_CURVE('',#4726,#4656,#2699,.T.);
#6164=EDGE_CURVE('',#4727,#4728,#3246,.T.);
#6165=EDGE_CURVE('',#4727,#4729,#3247,.T.);
#6166=EDGE_CURVE('',#4729,#4730,#3248,.T.);
#6167=EDGE_CURVE('',#4728,#4730,#3249,.T.);
#6168=EDGE_CURVE('',#4731,#4727,#3250,.T.);
#6169=EDGE_CURVE('',#4731,#4732,#3251,.T.);
#6170=EDGE_CURVE('',#4732,#4729,#3252,.T.);
#6171=EDGE_CURVE('',#4733,#4731,#3253,.T.);
#6172=EDGE_CURVE('',#4733,#4734,#3254,.T.);
#6173=EDGE_CURVE('',#4734,#4732,#3255,.T.);
#6174=EDGE_CURVE('',#4735,#4733,#3256,.T.);
#6175=EDGE_CURVE('',#4735,#4736,#3257,.T.);
#6176=EDGE_CURVE('',#4736,#4734,#3258,.T.);
#6177=EDGE_CURVE('',#4737,#4735,#3259,.T.);
#6178=EDGE_CURVE('',#4737,#4738,#3260,.T.);
#6179=EDGE_CURVE('',#4738,#4736,#3261,.T.);
#6180=EDGE_CURVE('',#4728,#4737,#3262,.T.);
#6181=EDGE_CURVE('',#4730,#4738,#3263,.T.);
#6182=EDGE_CURVE('',#4739,#4739,#1986,.T.);
#6183=EDGE_CURVE('',#4739,#4740,#3264,.T.);
#6184=EDGE_CURVE('',#4740,#4740,#1987,.T.);
#8741=ORIENTED_EDGE('',*,*,#6053,.F.);
#8742=ORIENTED_EDGE('',*,*,#6054,.T.);
#8743=ORIENTED_EDGE('',*,*,#6055,.T.);
#8744=ORIENTED_EDGE('',*,*,#6056,.T.);
#8745=ORIENTED_EDGE('',*,*,#6057,.F.);
#8746=ORIENTED_EDGE('',*,*,#6058,.T.);
#8747=ORIENTED_EDGE('',*,*,#6053,.T.);
#8748=ORIENTED_EDGE('',*,*,#6059,.T.);
#8749=ORIENTED_EDGE('',*,*,#6060,.F.);
#8750=ORIENTED_EDGE('',*,*,#6061,.T.);
#8751=ORIENTED_EDGE('',*,*,#6057,.T.);
#8752=ORIENTED_EDGE('',*,*,#6062,.T.);
#8753=ORIENTED_EDGE('',*,*,#6063,.F.);
#8754=ORIENTED_EDGE('',*,*,#6064,.T.);
#8755=ORIENTED_EDGE('',*,*,#6060,.T.);
#8756=ORIENTED_EDGE('',*,*,#6065,.T.);
#8757=ORIENTED_EDGE('',*,*,#6066,.F.);
#8758=ORIENTED_EDGE('',*,*,#6067,.T.);
#8759=ORIENTED_EDGE('',*,*,#6063,.T.);
#8760=ORIENTED_EDGE('',*,*,#6068,.T.);
#8761=ORIENTED_EDGE('',*,*,#6069,.F.);
#8762=ORIENTED_EDGE('',*,*,#6070,.T.);
#8763=ORIENTED_EDGE('',*,*,#6066,.T.);
#8764=ORIENTED_EDGE('',*,*,#6071,.T.);
#8765=ORIENTED_EDGE('',*,*,#6072,.F.);
#8766=ORIENTED_EDGE('',*,*,#6073,.T.);
#8767=ORIENTED_EDGE('',*,*,#6069,.T.);
#8768=ORIENTED_EDGE('',*,*,#6074,.T.);
#8769=ORIENTED_EDGE('',*,*,#6075,.F.);
#8770=ORIENTED_EDGE('',*,*,#6076,.T.);
#8771=ORIENTED_EDGE('',*,*,#6072,.T.);
#8772=ORIENTED_EDGE('',*,*,#6077,.T.);
#8773=ORIENTED_EDGE('',*,*,#6078,.F.);
#8774=ORIENTED_EDGE('',*,*,#6079,.T.);
#8775=ORIENTED_EDGE('',*,*,#6075,.T.);
#8776=ORIENTED_EDGE('',*,*,#6080,.T.);
#8777=ORIENTED_EDGE('',*,*,#6081,.F.);
#8778=ORIENTED_EDGE('',*,*,#6082,.T.);
#8779=ORIENTED_EDGE('',*,*,#6078,.T.);
#8780=ORIENTED_EDGE('',*,*,#6083,.T.);
#8781=ORIENTED_EDGE('',*,*,#6084,.F.);
#8782=ORIENTED_EDGE('',*,*,#6085,.T.);
#8783=ORIENTED_EDGE('',*,*,#6081,.T.);
#8784=ORIENTED_EDGE('',*,*,#6086,.T.);
#8785=ORIENTED_EDGE('',*,*,#6087,.F.);
#8786=ORIENTED_EDGE('',*,*,#6088,.T.);
#8787=ORIENTED_EDGE('',*,*,#6084,.T.);
#8788=ORIENTED_EDGE('',*,*,#6089,.T.);
#8789=ORIENTED_EDGE('',*,*,#6090,.F.);
#8790=ORIENTED_EDGE('',*,*,#6091,.T.);
#8791=ORIENTED_EDGE('',*,*,#6087,.T.);
#8792=ORIENTED_EDGE('',*,*,#6092,.T.);
#8793=ORIENTED_EDGE('',*,*,#6093,.F.);
#8794=ORIENTED_EDGE('',*,*,#6094,.T.);
#8795=ORIENTED_EDGE('',*,*,#6090,.T.);
#8796=ORIENTED_EDGE('',*,*,#6095,.T.);
#8797=ORIENTED_EDGE('',*,*,#6096,.F.);
#8798=ORIENTED_EDGE('',*,*,#6097,.T.);
#8799=ORIENTED_EDGE('',*,*,#6093,.T.);
#8800=ORIENTED_EDGE('',*,*,#6098,.T.);
#8801=ORIENTED_EDGE('',*,*,#6099,.F.);
#8802=ORIENTED_EDGE('',*,*,#6100,.T.);
#8803=ORIENTED_EDGE('',*,*,#6096,.T.);
#8804=ORIENTED_EDGE('',*,*,#6101,.T.);
#8805=ORIENTED_EDGE('',*,*,#6102,.F.);
#8806=ORIENTED_EDGE('',*,*,#6103,.T.);
#8807=ORIENTED_EDGE('',*,*,#6104,.T.);
#8808=ORIENTED_EDGE('',*,*,#6105,.F.);
#8809=ORIENTED_EDGE('',*,*,#6106,.F.);
#8810=ORIENTED_EDGE('',*,*,#6107,.T.);
#8811=ORIENTED_EDGE('',*,*,#6102,.T.);
#8812=ORIENTED_EDGE('',*,*,#6108,.F.);
#8813=ORIENTED_EDGE('',*,*,#6109,.F.);
#8814=ORIENTED_EDGE('',*,*,#6110,.T.);
#8815=ORIENTED_EDGE('',*,*,#6106,.T.);
#8816=ORIENTED_EDGE('',*,*,#6111,.F.);
#8817=ORIENTED_EDGE('',*,*,#6112,.F.);
#8818=ORIENTED_EDGE('',*,*,#6113,.T.);
#8819=ORIENTED_EDGE('',*,*,#6109,.T.);
#8820=ORIENTED_EDGE('',*,*,#6114,.F.);
#8821=ORIENTED_EDGE('',*,*,#6115,.F.);
#8822=ORIENTED_EDGE('',*,*,#6116,.T.);
#8823=ORIENTED_EDGE('',*,*,#6112,.T.);
#8824=ORIENTED_EDGE('',*,*,#6117,.F.);
#8825=ORIENTED_EDGE('',*,*,#6118,.F.);
#8826=ORIENTED_EDGE('',*,*,#6119,.T.);
#8827=ORIENTED_EDGE('',*,*,#6115,.T.);
#8828=ORIENTED_EDGE('',*,*,#6120,.F.);
#8829=ORIENTED_EDGE('',*,*,#6121,.F.);
#8830=ORIENTED_EDGE('',*,*,#6122,.T.);
#8831=ORIENTED_EDGE('',*,*,#6118,.T.);
#8832=ORIENTED_EDGE('',*,*,#6123,.F.);
#8833=ORIENTED_EDGE('',*,*,#6124,.F.);
#8834=ORIENTED_EDGE('',*,*,#6125,.T.);
#8835=ORIENTED_EDGE('',*,*,#6121,.T.);
#8836=ORIENTED_EDGE('',*,*,#6126,.F.);
#8837=ORIENTED_EDGE('',*,*,#6127,.F.);
#8838=ORIENTED_EDGE('',*,*,#6128,.T.);
#8839=ORIENTED_EDGE('',*,*,#6124,.T.);
#8840=ORIENTED_EDGE('',*,*,#6129,.F.);
#8841=ORIENTED_EDGE('',*,*,#6130,.F.);
#8842=ORIENTED_EDGE('',*,*,#6131,.T.);
#8843=ORIENTED_EDGE('',*,*,#6127,.T.);
#8844=ORIENTED_EDGE('',*,*,#6132,.F.);
#8845=ORIENTED_EDGE('',*,*,#6133,.F.);
#8846=ORIENTED_EDGE('',*,*,#6134,.T.);
#8847=ORIENTED_EDGE('',*,*,#6130,.T.);
#8848=ORIENTED_EDGE('',*,*,#6135,.F.);
#8849=ORIENTED_EDGE('',*,*,#6136,.F.);
#8850=ORIENTED_EDGE('',*,*,#6137,.T.);
#8851=ORIENTED_EDGE('',*,*,#6133,.T.);
#8852=ORIENTED_EDGE('',*,*,#6138,.F.);
#8853=ORIENTED_EDGE('',*,*,#6139,.F.);
#8854=ORIENTED_EDGE('',*,*,#6140,.T.);
#8855=ORIENTED_EDGE('',*,*,#6136,.T.);
#8856=ORIENTED_EDGE('',*,*,#6141,.F.);
#8857=ORIENTED_EDGE('',*,*,#6142,.F.);
#8858=ORIENTED_EDGE('',*,*,#6143,.T.);
#8859=ORIENTED_EDGE('',*,*,#6139,.T.);
#8860=ORIENTED_EDGE('',*,*,#6144,.F.);
#8861=ORIENTED_EDGE('',*,*,#6145,.F.);
#8862=ORIENTED_EDGE('',*,*,#6146,.T.);
#8863=ORIENTED_EDGE('',*,*,#6142,.T.);
#8864=ORIENTED_EDGE('',*,*,#6147,.F.);
#8865=ORIENTED_EDGE('',*,*,#6148,.F.);
#8866=ORIENTED_EDGE('',*,*,#6149,.T.);
#8867=ORIENTED_EDGE('',*,*,#6145,.T.);
#8868=ORIENTED_EDGE('',*,*,#6150,.F.);
#8869=ORIENTED_EDGE('',*,*,#6151,.F.);
#8870=ORIENTED_EDGE('',*,*,#6104,.F.);
#8871=ORIENTED_EDGE('',*,*,#6152,.F.);
#8872=ORIENTED_EDGE('',*,*,#6153,.F.);
#8873=ORIENTED_EDGE('',*,*,#6154,.F.);
#8874=ORIENTED_EDGE('',*,*,#6155,.T.);
#8875=ORIENTED_EDGE('',*,*,#6156,.F.);
#8876=ORIENTED_EDGE('',*,*,#6155,.F.);
#8877=ORIENTED_EDGE('',*,*,#6152,.T.);
#8878=ORIENTED_EDGE('',*,*,#6103,.F.);
#8879=ORIENTED_EDGE('',*,*,#6107,.F.);
#8880=ORIENTED_EDGE('',*,*,#6110,.F.);
#8881=ORIENTED_EDGE('',*,*,#6113,.F.);
#8882=ORIENTED_EDGE('',*,*,#6116,.F.);
#8883=ORIENTED_EDGE('',*,*,#6119,.F.);
#8884=ORIENTED_EDGE('',*,*,#6122,.F.);
#8885=ORIENTED_EDGE('',*,*,#6125,.F.);
#8886=ORIENTED_EDGE('',*,*,#6128,.F.);
#8887=ORIENTED_EDGE('',*,*,#6131,.F.);
#8888=ORIENTED_EDGE('',*,*,#6134,.F.);
#8889=ORIENTED_EDGE('',*,*,#6137,.F.);
#8890=ORIENTED_EDGE('',*,*,#6140,.F.);
#8891=ORIENTED_EDGE('',*,*,#6143,.F.);
#8892=ORIENTED_EDGE('',*,*,#6146,.F.);
#8893=ORIENTED_EDGE('',*,*,#6149,.F.);
#8894=ORIENTED_EDGE('',*,*,#6157,.F.);
#8895=ORIENTED_EDGE('',*,*,#6158,.F.);
#8896=ORIENTED_EDGE('',*,*,#6054,.F.);
#8897=ORIENTED_EDGE('',*,*,#6058,.F.);
#8898=ORIENTED_EDGE('',*,*,#6061,.F.);
#8899=ORIENTED_EDGE('',*,*,#6064,.F.);
#8900=ORIENTED_EDGE('',*,*,#6067,.F.);
#8901=ORIENTED_EDGE('',*,*,#6070,.F.);
#8902=ORIENTED_EDGE('',*,*,#6073,.F.);
#8903=ORIENTED_EDGE('',*,*,#6076,.F.);
#8904=ORIENTED_EDGE('',*,*,#6079,.F.);
#8905=ORIENTED_EDGE('',*,*,#6082,.F.);
#8906=ORIENTED_EDGE('',*,*,#6085,.F.);
#8907=ORIENTED_EDGE('',*,*,#6088,.F.);
#8908=ORIENTED_EDGE('',*,*,#6091,.F.);
#8909=ORIENTED_EDGE('',*,*,#6094,.F.);
#8910=ORIENTED_EDGE('',*,*,#6097,.F.);
#8911=ORIENTED_EDGE('',*,*,#6100,.F.);
#8912=ORIENTED_EDGE('',*,*,#6159,.F.);
#8913=ORIENTED_EDGE('',*,*,#6148,.T.);
#8914=ORIENTED_EDGE('',*,*,#6160,.F.);
#8915=ORIENTED_EDGE('',*,*,#6161,.F.);
#8916=ORIENTED_EDGE('',*,*,#6157,.T.);
#8917=ORIENTED_EDGE('',*,*,#6151,.T.);
#8918=ORIENTED_EDGE('',*,*,#6154,.T.);
#8919=ORIENTED_EDGE('',*,*,#6162,.F.);
#8920=ORIENTED_EDGE('',*,*,#6101,.F.);
#8921=ORIENTED_EDGE('',*,*,#6098,.F.);
#8922=ORIENTED_EDGE('',*,*,#6095,.F.);
#8923=ORIENTED_EDGE('',*,*,#6092,.F.);
#8924=ORIENTED_EDGE('',*,*,#6089,.F.);
#8925=ORIENTED_EDGE('',*,*,#6086,.F.);
#8926=ORIENTED_EDGE('',*,*,#6083,.F.);
#8927=ORIENTED_EDGE('',*,*,#6080,.F.);
#8928=ORIENTED_EDGE('',*,*,#6077,.F.);
#8929=ORIENTED_EDGE('',*,*,#6074,.F.);
#8930=ORIENTED_EDGE('',*,*,#6071,.F.);
#8931=ORIENTED_EDGE('',*,*,#6068,.F.);
#8932=ORIENTED_EDGE('',*,*,#6065,.F.);
#8933=ORIENTED_EDGE('',*,*,#6062,.F.);
#8934=ORIENTED_EDGE('',*,*,#6059,.F.);
#8935=ORIENTED_EDGE('',*,*,#6056,.F.);
#8936=ORIENTED_EDGE('',*,*,#6163,.F.);
#8937=ORIENTED_EDGE('',*,*,#6160,.T.);
#8938=ORIENTED_EDGE('',*,*,#6150,.T.);
#8939=ORIENTED_EDGE('',*,*,#6147,.T.);
#8940=ORIENTED_EDGE('',*,*,#6144,.T.);
#8941=ORIENTED_EDGE('',*,*,#6141,.T.);
#8942=ORIENTED_EDGE('',*,*,#6138,.T.);
#8943=ORIENTED_EDGE('',*,*,#6135,.T.);
#8944=ORIENTED_EDGE('',*,*,#6132,.T.);
#8945=ORIENTED_EDGE('',*,*,#6129,.T.);
#8946=ORIENTED_EDGE('',*,*,#6126,.T.);
#8947=ORIENTED_EDGE('',*,*,#6123,.T.);
#8948=ORIENTED_EDGE('',*,*,#6120,.T.);
#8949=ORIENTED_EDGE('',*,*,#6117,.T.);
#8950=ORIENTED_EDGE('',*,*,#6114,.T.);
#8951=ORIENTED_EDGE('',*,*,#6111,.T.);
#8952=ORIENTED_EDGE('',*,*,#6108,.T.);
#8953=ORIENTED_EDGE('',*,*,#6105,.T.);
#8954=ORIENTED_EDGE('',*,*,#6099,.T.);
#8955=ORIENTED_EDGE('',*,*,#6162,.T.);
#8956=ORIENTED_EDGE('',*,*,#6153,.T.);
#8957=ORIENTED_EDGE('',*,*,#6159,.T.);
#8958=ORIENTED_EDGE('',*,*,#6164,.F.);
#8959=ORIENTED_EDGE('',*,*,#6165,.T.);
#8960=ORIENTED_EDGE('',*,*,#6166,.T.);
#8961=ORIENTED_EDGE('',*,*,#6167,.F.);
#8962=ORIENTED_EDGE('',*,*,#6168,.F.);
#8963=ORIENTED_EDGE('',*,*,#6169,.T.);
#8964=ORIENTED_EDGE('',*,*,#6170,.T.);
#8965=ORIENTED_EDGE('',*,*,#6165,.F.);
#8966=ORIENTED_EDGE('',*,*,#6171,.F.);
#8967=ORIENTED_EDGE('',*,*,#6172,.T.);
#8968=ORIENTED_EDGE('',*,*,#6173,.T.);
#8969=ORIENTED_EDGE('',*,*,#6169,.F.);
#8970=ORIENTED_EDGE('',*,*,#6174,.F.);
#8971=ORIENTED_EDGE('',*,*,#6175,.T.);
#8972=ORIENTED_EDGE('',*,*,#6176,.T.);
#8973=ORIENTED_EDGE('',*,*,#6172,.F.);
#8974=ORIENTED_EDGE('',*,*,#6177,.F.);
#8975=ORIENTED_EDGE('',*,*,#6178,.T.);
#8976=ORIENTED_EDGE('',*,*,#6179,.T.);
#8977=ORIENTED_EDGE('',*,*,#6175,.F.);
#8978=ORIENTED_EDGE('',*,*,#6180,.F.);
#8979=ORIENTED_EDGE('',*,*,#6167,.T.);
#8980=ORIENTED_EDGE('',*,*,#6181,.T.);
#8981=ORIENTED_EDGE('',*,*,#6178,.F.);
#8982=ORIENTED_EDGE('',*,*,#6181,.F.);
#8983=ORIENTED_EDGE('',*,*,#6166,.F.);
#8984=ORIENTED_EDGE('',*,*,#6170,.F.);
#8985=ORIENTED_EDGE('',*,*,#6173,.F.);
#8986=ORIENTED_EDGE('',*,*,#6176,.F.);
#8987=ORIENTED_EDGE('',*,*,#6179,.F.);
#8988=ORIENTED_EDGE('',*,*,#6182,.T.);
#8989=ORIENTED_EDGE('',*,*,#6158,.T.);
#8990=ORIENTED_EDGE('',*,*,#6161,.T.);
#8991=ORIENTED_EDGE('',*,*,#6163,.T.);
#8992=ORIENTED_EDGE('',*,*,#6055,.F.);
#8993=ORIENTED_EDGE('',*,*,#6182,.F.);
#8994=ORIENTED_EDGE('',*,*,#6183,.T.);
#8995=ORIENTED_EDGE('',*,*,#6184,.T.);
#8996=ORIENTED_EDGE('',*,*,#6183,.F.);
#8997=ORIENTED_EDGE('',*,*,#6184,.F.);
#8998=ORIENTED_EDGE('',*,*,#6164,.T.);
#8999=ORIENTED_EDGE('',*,*,#6180,.T.);
#9000=ORIENTED_EDGE('',*,*,#6177,.T.);
#9001=ORIENTED_EDGE('',*,*,#6174,.T.);
#9002=ORIENTED_EDGE('',*,*,#6171,.T.);
#9003=ORIENTED_EDGE('',*,*,#6168,.T.);
#9004=ORIENTED_EDGE('',*,*,#6156,.T.);
#9747=CYLINDRICAL_SURFACE('',#11062,1.954);
#9748=CYLINDRICAL_SURFACE('',#11064,1.954);
#9749=CYLINDRICAL_SURFACE('',#11065,1.954);
#9750=CYLINDRICAL_SURFACE('',#11066,1.954);
#9751=CYLINDRICAL_SURFACE('',#11067,1.954);
#9752=CYLINDRICAL_SURFACE('',#11068,1.954);
#9753=CYLINDRICAL_SURFACE('',#11069,1.954);
#9754=CYLINDRICAL_SURFACE('',#11070,1.954);
#9755=CYLINDRICAL_SURFACE('',#11071,1.954);
#9756=CYLINDRICAL_SURFACE('',#11072,1.954);
#9757=CYLINDRICAL_SURFACE('',#11073,1.954);
#9758=CYLINDRICAL_SURFACE('',#11074,1.954);
#9759=CYLINDRICAL_SURFACE('',#11075,1.954);
#9760=CYLINDRICAL_SURFACE('',#11076,1.954);
#9761=CYLINDRICAL_SURFACE('',#11077,1.954);
#9762=CYLINDRICAL_SURFACE('',#11078,1.954);
#9763=CYLINDRICAL_SURFACE('',#11079,1.5555);
#9764=CYLINDRICAL_SURFACE('',#11081,1.5555);
#9765=CYLINDRICAL_SURFACE('',#11082,1.5555);
#9766=CYLINDRICAL_SURFACE('',#11083,1.5555);
#9767=CYLINDRICAL_SURFACE('',#11084,1.5555);
#9768=CYLINDRICAL_SURFACE('',#11085,1.5555);
#9769=CYLINDRICAL_SURFACE('',#11086,1.5555);
#9770=CYLINDRICAL_SURFACE('',#11087,1.5555);
#9771=CYLINDRICAL_SURFACE('',#11088,1.5555);
#9772=CYLINDRICAL_SURFACE('',#11089,1.5555);
#9773=CYLINDRICAL_SURFACE('',#11090,1.5555);
#9774=CYLINDRICAL_SURFACE('',#11091,1.5555);
#9775=CYLINDRICAL_SURFACE('',#11092,1.5555);
#9776=CYLINDRICAL_SURFACE('',#11093,1.5555);
#9777=CYLINDRICAL_SURFACE('',#11094,1.5555);
#9778=CYLINDRICAL_SURFACE('',#11095,1.5555);
#9779=CYLINDRICAL_SURFACE('',#11099,1.5555);
#9780=CYLINDRICAL_SURFACE('',#11101,1.954);
#9781=CYLINDRICAL_SURFACE('',#11111,3.5);
#10251=ADVANCED_FACE('',(#1015),#9747,.T.);
#10252=ADVANCED_FACE('',(#1016),#9748,.T.);
#10253=ADVANCED_FACE('',(#1017),#9749,.T.);
#10254=ADVANCED_FACE('',(#1018),#9750,.T.);
#10255=ADVANCED_FACE('',(#1019),#9751,.T.);
#10256=ADVANCED_FACE('',(#1020),#9752,.T.);
#10257=ADVANCED_FACE('',(#1021),#9753,.T.);
#10258=ADVANCED_FACE('',(#1022),#9754,.T.);
#10259=ADVANCED_FACE('',(#1023),#9755,.T.);
#10260=ADVANCED_FACE('',(#1024),#9756,.T.);
#10261=ADVANCED_FACE('',(#1025),#9757,.T.);
#10262=ADVANCED_FACE('',(#1026),#9758,.T.);
#10263=ADVANCED_FACE('',(#1027),#9759,.T.);
#10264=ADVANCED_FACE('',(#1028),#9760,.T.);
#10265=ADVANCED_FACE('',(#1029),#9761,.T.);
#10266=ADVANCED_FACE('',(#1030),#9762,.T.);
#10267=ADVANCED_FACE('',(#1031),#9763,.T.);
#10268=ADVANCED_FACE('',(#1032),#9764,.T.);
#10269=ADVANCED_FACE('',(#1033),#9765,.T.);
#10270=ADVANCED_FACE('',(#1034),#9766,.T.);
#10271=ADVANCED_FACE('',(#1035),#9767,.T.);
#10272=ADVANCED_FACE('',(#1036),#9768,.T.);
#10273=ADVANCED_FACE('',(#1037),#9769,.T.);
#10274=ADVANCED_FACE('',(#1038),#9770,.T.);
#10275=ADVANCED_FACE('',(#1039),#9771,.T.);
#10276=ADVANCED_FACE('',(#1040),#9772,.T.);
#10277=ADVANCED_FACE('',(#1041),#9773,.T.);
#10278=ADVANCED_FACE('',(#1042),#9774,.T.);
#10279=ADVANCED_FACE('',(#1043),#9775,.T.);
#10280=ADVANCED_FACE('',(#1044),#9776,.T.);
#10281=ADVANCED_FACE('',(#1045),#9777,.T.);
#10282=ADVANCED_FACE('',(#1046),#9778,.T.);
#10283=ADVANCED_FACE('',(#1047),#311,.T.);
#10284=ADVANCED_FACE('',(#1048),#597,.F.);
#10285=ADVANCED_FACE('',(#1049),#9779,.T.);
#10286=ADVANCED_FACE('',(#1050),#598,.F.);
#10287=ADVANCED_FACE('',(#1051),#9780,.T.);
#10288=ADVANCED_FACE('',(#1052),#547,.F.);
#10289=ADVANCED_FACE('',(#1053),#548,.F.);
#10290=ADVANCED_FACE('',(#1054),#549,.F.);
#10291=ADVANCED_FACE('',(#1055),#550,.F.);
#10292=ADVANCED_FACE('',(#1056),#551,.F.);
#10293=ADVANCED_FACE('',(#1057),#552,.F.);
#10294=ADVANCED_FACE('',(#1058),#553,.F.);
#10295=ADVANCED_FACE('',(#1059,#471),#554,.T.);
#10296=ADVANCED_FACE('',(#1060),#9781,.T.);
#10297=ADVANCED_FACE('',(#1061,#472),#555,.F.);
#10298=ADVANCED_FACE('',(#1062),#556,.T.);
#10389=CLOSED_SHELL('',(#10251,#10252,#10253,#10254,#10255,#10256,#10257,
#10258,#10259,#10260,#10261,#10262,#10263,#10264,#10265,#10266,#10267,#10268,
#10269,#10270,#10271,#10272,#10273,#10274,#10275,#10276,#10277,#10278,#10279,
#10280,#10281,#10282,#10283,#10284,#10285,#10286,#10287,#10288,#10289,#10290,
#10291,#10292,#10293,#10294,#10295,#10296,#10297,#10298));
#11061=AXIS2_PLACEMENT_3D('',#35183,#12834,#12835);
#11062=AXIS2_PLACEMENT_3D('',#35184,#12836,#12837);
#11063=AXIS2_PLACEMENT_3D('',#35200,#12839,#12840);
#11064=AXIS2_PLACEMENT_3D('',#35208,#12841,#12842);
#11065=AXIS2_PLACEMENT_3D('',#35256,#12844,#12845);
#11066=AXIS2_PLACEMENT_3D('',#35304,#12847,#12848);
#11067=AXIS2_PLACEMENT_3D('',#35358,#12850,#12851);
#11068=AXIS2_PLACEMENT_3D('',#35406,#12853,#12854);
#11069=AXIS2_PLACEMENT_3D('',#35454,#12856,#12857);
#11070=AXIS2_PLACEMENT_3D('',#35502,#12859,#12860);
#11071=AXIS2_PLACEMENT_3D('',#35556,#12862,#12863);
#11072=AXIS2_PLACEMENT_3D('',#35604,#12865,#12866);
#11073=AXIS2_PLACEMENT_3D('',#35652,#12868,#12869);
#11074=AXIS2_PLACEMENT_3D('',#35706,#12871,#12872);
#11075=AXIS2_PLACEMENT_3D('',#35754,#12874,#12875);
#11076=AXIS2_PLACEMENT_3D('',#35802,#12877,#12878);
#11077=AXIS2_PLACEMENT_3D('',#35853,#12880,#12881);
#11078=AXIS2_PLACEMENT_3D('',#35904,#12883,#12884);
#11079=AXIS2_PLACEMENT_3D('',#35952,#12886,#12887);
#11080=AXIS2_PLACEMENT_3D('',#35966,#12889,#12890);
#11081=AXIS2_PLACEMENT_3D('',#35974,#12891,#12892);
#11082=AXIS2_PLACEMENT_3D('',#35998,#12894,#12895);
#11083=AXIS2_PLACEMENT_3D('',#36022,#12897,#12898);
#11084=AXIS2_PLACEMENT_3D('',#36048,#12900,#12901);
#11085=AXIS2_PLACEMENT_3D('',#36072,#12903,#12904);
#11086=AXIS2_PLACEMENT_3D('',#36096,#12906,#12907);
#11087=AXIS2_PLACEMENT_3D('',#36121,#12909,#12910);
#11088=AXIS2_PLACEMENT_3D('',#36146,#12912,#12913);
#11089=AXIS2_PLACEMENT_3D('',#36170,#12915,#12916);
#11090=AXIS2_PLACEMENT_3D('',#36195,#12918,#12919);
#11091=AXIS2_PLACEMENT_3D('',#36220,#12921,#12922);
#11092=AXIS2_PLACEMENT_3D('',#36244,#12924,#12925);
#11093=AXIS2_PLACEMENT_3D('',#36268,#12927,#12928);
#11094=AXIS2_PLACEMENT_3D('',#36293,#12930,#12931);
#11095=AXIS2_PLACEMENT_3D('',#36318,#12933,#12934);
#11096=AXIS2_PLACEMENT_3D('',#36342,#12936,#12937);
#11097=AXIS2_PLACEMENT_3D('',#36531,#12938,#12939);
#11098=AXIS2_PLACEMENT_3D('',#36637,#12941,#12942);
#11099=AXIS2_PLACEMENT_3D('',#37169,#12943,#12944);
#11100=AXIS2_PLACEMENT_3D('',#37180,#12945,#12946);
#11101=AXIS2_PLACEMENT_3D('',#37714,#12947,#12948);
#11102=AXIS2_PLACEMENT_3D('',#37715,#12949,#12950);
#11103=AXIS2_PLACEMENT_3D('',#37724,#12955,#12956);
#11104=AXIS2_PLACEMENT_3D('',#37730,#12960,#12961);
#11105=AXIS2_PLACEMENT_3D('',#37736,#12965,#12966);
#11106=AXIS2_PLACEMENT_3D('',#37742,#12970,#12971);
#11107=AXIS2_PLACEMENT_3D('',#37748,#12975,#12976);
#11108=AXIS2_PLACEMENT_3D('',#37751,#12979,#12980);
#11109=AXIS2_PLACEMENT_3D('',#37752,#12981,#12982);
#11110=AXIS2_PLACEMENT_3D('',#37754,#12983,#12984);
#11111=AXIS2_PLACEMENT_3D('',#37755,#12985,#12986);
#11112=AXIS2_PLACEMENT_3D('',#37758,#12988,#12989);
#11113=AXIS2_PLACEMENT_3D('',#37759,#12990,#12991);
#11114=AXIS2_PLACEMENT_3D('',#37760,#12992,#12993);
#12834=DIRECTION('axis',(0.,0.,1.));
#12835=DIRECTION('refdir',(1.,0.,0.));
#12836=DIRECTION('center_axis',(0.,0.,1.));
#12837=DIRECTION('ref_axis',(1.,0.,0.));
#12838=DIRECTION('',(0.,0.,-1.));
#12839=DIRECTION('center_axis',(0.,0.,-1.));
#12840=DIRECTION('ref_axis',(1.,0.,0.));
#12841=DIRECTION('center_axis',(0.,0.,1.));
#12842=DIRECTION('ref_axis',(1.,0.,0.));
#12843=DIRECTION('',(0.,0.,-1.));
#12844=DIRECTION('center_axis',(0.,0.,1.));
#12845=DIRECTION('ref_axis',(1.,0.,0.));
#12846=DIRECTION('',(0.,0.,-1.));
#12847=DIRECTION('center_axis',(0.,0.,1.));
#12848=DIRECTION('ref_axis',(1.,0.,0.));
#12849=DIRECTION('',(0.,0.,-1.));
#12850=DIRECTION('center_axis',(0.,0.,1.));
#12851=DIRECTION('ref_axis',(1.,0.,0.));
#12852=DIRECTION('',(0.,0.,-1.));
#12853=DIRECTION('center_axis',(0.,0.,1.));
#12854=DIRECTION('ref_axis',(1.,0.,0.));
#12855=DIRECTION('',(0.,0.,-1.));
#12856=DIRECTION('center_axis',(0.,0.,1.));
#12857=DIRECTION('ref_axis',(1.,0.,0.));
#12858=DIRECTION('',(0.,0.,-1.));
#12859=DIRECTION('center_axis',(0.,0.,1.));
#12860=DIRECTION('ref_axis',(1.,0.,0.));
#12861=DIRECTION('',(0.,0.,-1.));
#12862=DIRECTION('center_axis',(0.,0.,1.));
#12863=DIRECTION('ref_axis',(1.,0.,0.));
#12864=DIRECTION('',(0.,0.,-1.));
#12865=DIRECTION('center_axis',(0.,0.,1.));
#12866=DIRECTION('ref_axis',(1.,0.,0.));
#12867=DIRECTION('',(0.,0.,-1.));
#12868=DIRECTION('center_axis',(0.,0.,1.));
#12869=DIRECTION('ref_axis',(1.,0.,0.));
#12870=DIRECTION('',(0.,0.,-1.));
#12871=DIRECTION('center_axis',(0.,0.,1.));
#12872=DIRECTION('ref_axis',(1.,0.,0.));
#12873=DIRECTION('',(0.,0.,-1.));
#12874=DIRECTION('center_axis',(0.,0.,1.));
#12875=DIRECTION('ref_axis',(1.,0.,0.));
#12876=DIRECTION('',(0.,0.,-1.));
#12877=DIRECTION('center_axis',(0.,0.,1.));
#12878=DIRECTION('ref_axis',(1.,0.,0.));
#12879=DIRECTION('',(0.,0.,-1.));
#12880=DIRECTION('center_axis',(0.,0.,1.));
#12881=DIRECTION('ref_axis',(1.,0.,0.));
#12882=DIRECTION('',(0.,0.,-1.));
#12883=DIRECTION('center_axis',(0.,0.,1.));
#12884=DIRECTION('ref_axis',(1.,0.,0.));
#12885=DIRECTION('',(0.,0.,-1.));
#12886=DIRECTION('center_axis',(0.,0.,1.));
#12887=DIRECTION('ref_axis',(1.,1.29731060939901E-13,0.));
#12888=DIRECTION('',(0.,0.,1.));
#12889=DIRECTION('center_axis',(0.,0.,-1.));
#12890=DIRECTION('ref_axis',(1.,1.29731060939901E-13,0.));
#12891=DIRECTION('center_axis',(0.,0.,1.));
#12892=DIRECTION('ref_axis',(1.,1.29731060939901E-13,0.));
#12893=DIRECTION('',(0.,0.,1.));
#12894=DIRECTION('center_axis',(0.,0.,1.));
#12895=DIRECTION('ref_axis',(1.,1.29731060939901E-13,0.));
#12896=DIRECTION('',(0.,0.,1.));
#12897=DIRECTION('center_axis',(0.,0.,1.));
#12898=DIRECTION('ref_axis',(1.,1.29731060939901E-13,0.));
#12899=DIRECTION('',(0.,0.,1.));
#12900=DIRECTION('center_axis',(0.,0.,1.));
#12901=DIRECTION('ref_axis',(1.,1.29731060939901E-13,0.));
#12902=DIRECTION('',(0.,0.,1.));
#12903=DIRECTION('center_axis',(0.,0.,1.));
#12904=DIRECTION('ref_axis',(1.,1.29731060939901E-13,0.));
#12905=DIRECTION('',(0.,0.,1.));
#12906=DIRECTION('center_axis',(0.,0.,1.));
#12907=DIRECTION('ref_axis',(1.,1.29731060939901E-13,0.));
#12908=DIRECTION('',(0.,0.,1.));
#12909=DIRECTION('center_axis',(0.,0.,1.));
#12910=DIRECTION('ref_axis',(1.,1.29731060939901E-13,0.));
#12911=DIRECTION('',(0.,0.,1.));
#12912=DIRECTION('center_axis',(0.,0.,1.));
#12913=DIRECTION('ref_axis',(1.,1.29731060939901E-13,0.));
#12914=DIRECTION('',(0.,0.,1.));
#12915=DIRECTION('center_axis',(0.,0.,1.));
#12916=DIRECTION('ref_axis',(1.,1.29731060939901E-13,0.));
#12917=DIRECTION('',(0.,0.,1.));
#12918=DIRECTION('center_axis',(0.,0.,1.));
#12919=DIRECTION('ref_axis',(1.,1.29731060939901E-13,0.));
#12920=DIRECTION('',(0.,0.,1.));
#12921=DIRECTION('center_axis',(0.,0.,1.));
#12922=DIRECTION('ref_axis',(1.,1.29731060939901E-13,0.));
#12923=DIRECTION('',(0.,0.,1.));
#12924=DIRECTION('center_axis',(0.,0.,1.));
#12925=DIRECTION('ref_axis',(1.,1.29731060939901E-13,0.));
#12926=DIRECTION('',(0.,0.,1.));
#12927=DIRECTION('center_axis',(0.,0.,1.));
#12928=DIRECTION('ref_axis',(1.,1.29731060939901E-13,0.));
#12929=DIRECTION('',(0.,0.,1.));
#12930=DIRECTION('center_axis',(0.,0.,1.));
#12931=DIRECTION('ref_axis',(1.,1.29731060939901E-13,0.));
#12932=DIRECTION('',(0.,0.,1.));
#12933=DIRECTION('center_axis',(0.,0.,1.));
#12934=DIRECTION('ref_axis',(1.,1.29731060939901E-13,0.));
#12935=DIRECTION('',(0.,0.,1.));
#12936=DIRECTION('center_axis',(0.,0.,-1.));
#12937=DIRECTION('ref_axis',(1.,0.,0.));
#12938=DIRECTION('center_axis',(0.,0.,-1.));
#12939=DIRECTION('ref_axis',(1.,0.,0.));
#12940=DIRECTION('',(0.707106781186548,8.65956056235494E-17,0.707106781186547));
#12941=DIRECTION('center_axis',(0.,0.,1.));
#12942=DIRECTION('ref_axis',(1.,0.,0.));
#12943=DIRECTION('center_axis',(0.,0.,1.));
#12944=DIRECTION('ref_axis',(1.,1.29731060939901E-13,0.));
#12945=DIRECTION('center_axis',(0.,0.,-1.));
#12946=DIRECTION('ref_axis',(1.,1.29731060939901E-13,0.));
#12947=DIRECTION('center_axis',(0.,0.,1.));
#12948=DIRECTION('ref_axis',(1.,0.,0.));
#12949=DIRECTION('center_axis',(-1.60246890531964E-16,-1.,0.));
#12950=DIRECTION('ref_axis',(1.,-1.60246890531964E-16,0.));
#12951=DIRECTION('',(1.,-1.60246890531964E-16,0.));
#12952=DIRECTION('',(0.,0.,1.));
#12953=DIRECTION('',(1.,-1.60246890531964E-16,0.));
#12954=DIRECTION('',(0.,0.,1.));
#12955=DIRECTION('center_axis',(-0.866025403784439,-0.5,0.));
#12956=DIRECTION('ref_axis',(0.5,-0.866025403784439,0.));
#12957=DIRECTION('',(0.5,-0.866025403784439,0.));
#12958=DIRECTION('',(0.,0.,1.));
#12959=DIRECTION('',(0.5,-0.866025403784439,0.));
#12960=DIRECTION('center_axis',(-0.866025403784439,0.5,0.));
#12961=DIRECTION('ref_axis',(-0.5,-0.866025403784439,0.));
#12962=DIRECTION('',(-0.5,-0.866025403784439,0.));
#12963=DIRECTION('',(0.,0.,1.));
#12964=DIRECTION('',(-0.5,-0.866025403784439,0.));
#12965=DIRECTION('center_axis',(1.60246890531964E-16,1.,0.));
#12966=DIRECTION('ref_axis',(-1.,1.60246890531964E-16,0.));
#12967=DIRECTION('',(-1.,1.60246890531964E-16,0.));
#12968=DIRECTION('',(0.,0.,1.));
#12969=DIRECTION('',(-1.,1.60246890531964E-16,0.));
#12970=DIRECTION('center_axis',(0.866025403784439,0.5,0.));
#12971=DIRECTION('ref_axis',(-0.5,0.866025403784439,0.));
#12972=DIRECTION('',(-0.5,0.866025403784439,0.));
#12973=DIRECTION('',(0.,0.,1.));
#12974=DIRECTION('',(-0.5,0.866025403784439,0.));
#12975=DIRECTION('center_axis',(0.866025403784439,-0.5,0.));
#12976=DIRECTION('ref_axis',(0.5,0.866025403784439,0.));
#12977=DIRECTION('',(0.5,0.866025403784439,0.));
#12978=DIRECTION('',(0.5,0.866025403784439,0.));
#12979=DIRECTION('center_axis',(0.,0.,1.));
#12980=DIRECTION('ref_axis',(1.,0.,0.));
#12981=DIRECTION('center_axis',(0.,0.,1.));
#12982=DIRECTION('ref_axis',(1.,0.,0.));
#12983=DIRECTION('center_axis',(0.,0.,1.));
#12984=DIRECTION('ref_axis',(1.,0.,0.));
#12985=DIRECTION('center_axis',(0.,0.,1.));
#12986=DIRECTION('ref_axis',(1.,0.,0.));
#12987=DIRECTION('',(0.,0.,-1.));
#12988=DIRECTION('center_axis',(0.,0.,1.));
#12989=DIRECTION('ref_axis',(1.,0.,0.));
#12990=DIRECTION('center_axis',(0.,0.,1.));
#12991=DIRECTION('ref_axis',(1.,0.,0.));
#12992=DIRECTION('center_axis',(0.,0.,1.));
#12993=DIRECTION('ref_axis',(1.,0.,0.));
#35183=CARTESIAN_POINT('',(0.,0.,0.));
#35184=CARTESIAN_POINT('Origin',(0.,0.,0.));
#35185=CARTESIAN_POINT('',(-1.95633559071744,0.0012731057411345,0.225869692124231));
#35186=CARTESIAN_POINT('',(-1.95587799559821,0.00207186393275607,0.124130307875758));
#35187=CARTESIAN_POINT('',(-1.954,-2.39295984553393E-16,0.));
#35188=CARTESIAN_POINT('',(0.861525859670522,1.75382131162755,0.));
#35189=CARTESIAN_POINT('Ctrl Pts',(-1.95633559071744,0.0012731057411345,
0.225869692124231));
#35190=CARTESIAN_POINT('Ctrl Pts',(-1.95680032440099,0.0682557629313676,
0.222037301306047));
#35191=CARTESIAN_POINT('Ctrl Pts',(-1.95365903766855,0.135191473590706,
0.218204910487863));
#35192=CARTESIAN_POINT('Ctrl Pts',(-1.94676806606145,0.201735328972743,
0.214372519669679));
#35193=CARTESIAN_POINT('Ctrl Pts',(-1.88017193281744,0.844832371344698,
0.1773353028412));
#35194=CARTESIAN_POINT('Ctrl Pts',(-1.46336311091822,1.45133095416213,0.140298086012721));
#35195=CARTESIAN_POINT('Ctrl Pts',(-0.886884671668765,1.7445317403525,0.103260869184242));
#35196=CARTESIAN_POINT('Ctrl Pts',(-0.351138290053491,2.01701592986141,
0.0688405794561611));
#35197=CARTESIAN_POINT('Ctrl Pts',(0.322511385444639,2.01891139473935,0.0344202897280807));
#35198=CARTESIAN_POINT('Ctrl Pts',(0.863567639152679,1.75641488315944,2.92734586571086E-17));
#35199=CARTESIAN_POINT('',(-0.861525859670574,1.75382131162752,1.38777878078145E-16));
#35200=CARTESIAN_POINT('Origin',(0.,0.,0.));
#35201=CARTESIAN_POINT('Ctrl Pts',(-0.861525859670571,1.75382131162752,
2.28983498828939E-15));
#35202=CARTESIAN_POINT('Ctrl Pts',(-1.44496782441851,1.46721837385109,0.0370621399437224));
#35203=CARTESIAN_POINT('Ctrl Pts',(-1.8691020329229,0.869083656944534,0.0741242798874424));
#35204=CARTESIAN_POINT('Ctrl Pts',(-1.94380023116171,0.227435527544788,
0.111186419831163));
#35205=CARTESIAN_POINT('Ctrl Pts',(-1.95249630318745,0.152737362394887,
0.115501049179361));
#35206=CARTESIAN_POINT('Ctrl Pts',(-1.95645657185248,0.0774494727773659,
0.119815678527559));
#35207=CARTESIAN_POINT('Ctrl Pts',(-1.95587799559821,0.00207186393275607,
0.124130307875758));
#35208=CARTESIAN_POINT('Origin',(0.,0.,0.));
#35209=CARTESIAN_POINT('',(-1.95128203910989,0.000979727872364722,0.92586969212423));
#35210=CARTESIAN_POINT('',(-1.95118672945361,0.000916100096969453,0.824130307875757));
#35211=CARTESIAN_POINT('',(-1.954,-2.39295984553393E-16,0.));
#35212=CARTESIAN_POINT('Ctrl Pts',(-1.95128203910989,0.000979727872364722,
0.92586969212423));
#35213=CARTESIAN_POINT('Ctrl Pts',(-1.9524730612105,0.263901717292074,0.910927268943587));
#35214=CARTESIAN_POINT('Ctrl Pts',(-1.90305141123492,0.526394079969068,
0.895984845762944));
#35215=CARTESIAN_POINT('Ctrl Pts',(-1.80089049647467,0.766440059940591,
0.881042422582301));
#35216=CARTESIAN_POINT('Ctrl Pts',(-1.54766811710363,1.36143291361156,0.844005205753822));
#35217=CARTESIAN_POINT('Ctrl Pts',(-0.970428066964404,1.81852045762203,
0.806967988925342));
#35218=CARTESIAN_POINT('Ctrl Pts',(-0.333230591869142,1.92861999489257,
0.769930772096863));
#35219=CARTESIAN_POINT('Ctrl Pts',(0.30396688322612,2.0387195321631,0.732893555268385));
#35220=CARTESIAN_POINT('Ctrl Pts',(1.00112178327742,1.8018310626937,0.695856338439906));
#35221=CARTESIAN_POINT('Ctrl Pts',(1.43930998255098,1.32629143144902,0.658819121611426));
#35222=CARTESIAN_POINT('Ctrl Pts',(1.87749818182454,0.850751800204341,0.621781904782947));
#35223=CARTESIAN_POINT('Ctrl Pts',(2.05671968032037,0.136561007184397,0.584744687954468));
#35224=CARTESIAN_POINT('Ctrl Pts',(1.89499805994521,-0.489512382298273,
0.547707471125989));
#35225=CARTESIAN_POINT('Ctrl Pts',(1.73327643957006,-1.11558577178094,0.51067025429751));
#35226=CARTESIAN_POINT('Ctrl Pts',(1.23061170032392,-1.65354175772633,0.473633037469032));
#35227=CARTESIAN_POINT('Ctrl Pts',(0.616932989107385,-1.8573955796291,0.436595820640553));
#35228=CARTESIAN_POINT('Ctrl Pts',(0.00325427789084558,-2.06124940153187,
0.399558603812074));
#35229=CARTESIAN_POINT('Ctrl Pts',(-0.721438405296094,-1.93100105939202,
0.362521386983595));
#35230=CARTESIAN_POINT('Ctrl Pts',(-1.22559302459517,-1.52602913735885,
0.325484170155115));
#35231=CARTESIAN_POINT('Ctrl Pts',(-1.67758072371516,-1.1629613001496,0.29227934414482));
#35232=CARTESIAN_POINT('Ctrl Pts',(-1.95230901779331,-0.579081973692791,
0.259074518134526));
#35233=CARTESIAN_POINT('Ctrl Pts',(-1.95633559071744,0.0012731057411345,
0.225869692124231));
#35234=CARTESIAN_POINT('Ctrl Pts',(-1.95587799559821,0.00207186393275607,
0.124130307875758));
#35235=CARTESIAN_POINT('Ctrl Pts',(-1.95148667238412,-0.570034995103637,
0.15687781847128));
#35236=CARTESIAN_POINT('Ctrl Pts',(-1.68562951923343,-1.14731024226281,
0.189625329066803));
#35237=CARTESIAN_POINT('Ctrl Pts',(-1.2444215732779,-1.51113938431406,0.222372839662326));
#35238=CARTESIAN_POINT('Ctrl Pts',(-0.745082529182101,-1.92290462488019,
0.259434979606046));
#35239=CARTESIAN_POINT('Ctrl Pts',(-0.0211422530173012,-2.0612735641195,
0.296497119549767));
#35240=CARTESIAN_POINT('Ctrl Pts',(0.595334795120667,-1.86428772433344,
0.333559259493488));
#35241=CARTESIAN_POINT('Ctrl Pts',(1.21181184325864,-1.66730188454737,0.370621399437209));
#35242=CARTESIAN_POINT('Ctrl Pts',(1.72082566336977,-1.13496126573593,0.40768353938093));
#35243=CARTESIAN_POINT('Ctrl Pts',(1.8894870924304,-0.510370283185346,0.444745679324651));
#35244=CARTESIAN_POINT('Ctrl Pts',(2.05814852149104,0.114220699365238,0.481807819268372));
#35245=CARTESIAN_POINT('Ctrl Pts',(1.88645755950116,0.831062045654966,0.518869959212093));
#35246=CARTESIAN_POINT('Ctrl Pts',(1.45292142815886,1.31145007703775,0.555932099155814));
#35247=CARTESIAN_POINT('Ctrl Pts',(1.01938529681656,1.79183810842053,0.592994239099535));
#35248=CARTESIAN_POINT('Ctrl Pts',(0.324003996121834,2.03577282489637,0.630056379043256));
#35249=CARTESIAN_POINT('Ctrl Pts',(-0.314654015224673,1.93172336479658,
0.667118518986976));
#35250=CARTESIAN_POINT('Ctrl Pts',(-0.953312026571179,1.8276739046968,0.704180658930697));
#35251=CARTESIAN_POINT('Ctrl Pts',(-1.53524674856946,1.37564026802139,0.741242798874417));
#35252=CARTESIAN_POINT('Ctrl Pts',(-1.79395555636014,0.782560471576942,
0.778304938818138));
#35253=CARTESIAN_POINT('Ctrl Pts',(-1.90058212652462,0.538123240897563,
0.793580061837345));
#35254=CARTESIAN_POINT('Ctrl Pts',(-1.95230335199157,0.269726953471863,
0.808855184856551));
#35255=CARTESIAN_POINT('Ctrl Pts',(-1.95118672945361,0.000916100096969453,
0.824130307875757));
#35256=CARTESIAN_POINT('Origin',(0.,0.,0.));
#35257=CARTESIAN_POINT('',(-1.95279554503994,-0.00168121501241181,1.62586969212423));
#35258=CARTESIAN_POINT('',(-1.95287184048439,-0.001702989282844,1.52413030787576));
#35259=CARTESIAN_POINT('',(-1.954,-2.39295984553393E-16,0.));
#35260=CARTESIAN_POINT('Ctrl Pts',(-1.95279554503994,-0.00168121501241181,
1.62586969212423));
#35261=CARTESIAN_POINT('Ctrl Pts',(-1.94903656010943,0.455834752155161,
1.59981723658113));
#35262=CARTESIAN_POINT('Ctrl Pts',(-1.78856730317397,0.91572573117829,1.57376478103802));
#35263=CARTESIAN_POINT('Ctrl Pts',(-1.49500760249196,1.26316552728133,1.54771232549492));
#35264=CARTESIAN_POINT('Ctrl Pts',(-1.07767134532899,1.75709989142681,1.51067510866644));
#35265=CARTESIAN_POINT('Ctrl Pts',(-0.39135122029848,2.02376358702057,1.47363789183796));
#35266=CARTESIAN_POINT('Ctrl Pts',(0.249990333148566,1.94116955279127,1.43660067500948));
#35267=CARTESIAN_POINT('Ctrl Pts',(0.891331886595613,1.85857551856197,1.39956345818101));
#35268=CARTESIAN_POINT('Ctrl Pts',(1.4876948684592,1.42672375450961,1.36252624135253));
#35269=CARTESIAN_POINT('Ctrl Pts',(1.76626827046517,0.843167597229759,1.32548902452405));
#35270=CARTESIAN_POINT('Ctrl Pts',(2.04484167247113,0.259611439949913,1.28845180769557));
#35271=CARTESIAN_POINT('Ctrl Pts',(2.00562549461947,-0.475649110557425,
1.25141459086709));
#35272=CARTESIAN_POINT('Ctrl Pts',(1.66655969053473,-1.02626219289756,1.21437737403861));
#35273=CARTESIAN_POINT('Ctrl Pts',(1.32749388644999,-1.57687527523771,1.17734015721013));
#35274=CARTESIAN_POINT('Ctrl Pts',(0.688578456132156,-1.94284088941065,
1.14030294038165));
#35275=CARTESIAN_POINT('Ctrl Pts',(0.0420898544956178,-1.9567474659654,
1.10326572355317));
#35276=CARTESIAN_POINT('Ctrl Pts',(-0.604398747140919,-1.97065404252014,
1.06622850672469));
#35277=CARTESIAN_POINT('Ctrl Pts',(-1.25846052009616,-1.6325015814567,1.02919128989622));
#35278=CARTESIAN_POINT('Ctrl Pts',(-1.62088905227235,-1.09697626925925,
0.992154073067737));
#35279=CARTESIAN_POINT('Ctrl Pts',(-1.83709816073764,-0.777505145902677,
0.970059279419901));
#35280=CARTESIAN_POINT('Ctrl Pts',(-1.94952091996443,-0.387793032173158,
0.947964485772066));
#35281=CARTESIAN_POINT('Ctrl Pts',(-1.95128203910989,0.000979727872364722,
0.92586969212423));
#35282=CARTESIAN_POINT('Ctrl Pts',(-1.95118672945361,0.000916100096969453,
0.824130307875757));
#35283=CARTESIAN_POINT('Ctrl Pts',(-1.94959408276249,-0.382490737583375,
0.845917324800272));
#35284=CARTESIAN_POINT('Ctrl Pts',(-1.84051065227066,-0.766740948347571,
0.867704341724787));
#35285=CARTESIAN_POINT('Ctrl Pts',(-1.62993550876047,-1.0835175828476,0.889491358649302));
#35286=CARTESIAN_POINT('Ctrl Pts',(-1.27172375978704,-1.62238988461419,
0.926553498593023));
#35287=CARTESIAN_POINT('Ctrl Pts',(-0.619817368257128,-1.96600853193387,
0.963615638536743));
#35288=CARTESIAN_POINT('Ctrl Pts',(0.0271864367452719,-1.95701720127518,
1.00067777848046));
#35289=CARTESIAN_POINT('Ctrl Pts',(0.674190241747668,-1.94802587061648,
1.03773991842418));
#35290=CARTESIAN_POINT('Ctrl Pts',(1.31629146022255,-1.5864245619794,1.07480205836791));
#35291=CARTESIAN_POINT('Ctrl Pts',(1.65939903784035,-1.03781956343241,1.11186419831163));
#35292=CARTESIAN_POINT('Ctrl Pts',(2.00250661545815,-0.489214564885407,
1.14892633825535));
#35293=CARTESIAN_POINT('Ctrl Pts',(2.04662055221888,0.246394123571516,1.18598847819907));
#35294=CARTESIAN_POINT('Ctrl Pts',(1.77153295980734,0.832073910176122,1.22305061814279));
#35295=CARTESIAN_POINT('Ctrl Pts',(1.49644536739581,1.41775369678073,1.26011275808651));
#35296=CARTESIAN_POINT('Ctrl Pts',(0.902156245812001,1.85350458153303,1.29717489803023));
#35297=CARTESIAN_POINT('Ctrl Pts',(0.260864347694114,1.93974733338565,1.33423703797395));
#35298=CARTESIAN_POINT('Ctrl Pts',(-0.380427550423769,2.02599008523827,
1.37129917791767));
#35299=CARTESIAN_POINT('Ctrl Pts',(-1.06872222507573,1.76272470419122,1.40836131786139));
#35300=CARTESIAN_POINT('Ctrl Pts',(-1.48876654315921,1.27053027794487,1.44542345780511));
#35301=CARTESIAN_POINT('Ctrl Pts',(-1.78610829781436,0.922114770268632,
1.47165907449533));
#35302=CARTESIAN_POINT('Ctrl Pts',(-1.94903067523895,0.458983666015645,
1.49789469118554));
#35303=CARTESIAN_POINT('Ctrl Pts',(-1.95287184048439,-0.001702989282844,
1.52413030787576));
#35304=CARTESIAN_POINT('Origin',(0.,0.,0.));
#35305=CARTESIAN_POINT('',(-1.9571996697324,4.08272333451705E-5,2.32586969212423));
#35306=CARTESIAN_POINT('',(-1.95720915199432,4.37834080700025E-5,2.22413030787575));
#35307=CARTESIAN_POINT('',(-1.954,-2.39295984553393E-16,0.));
#35308=CARTESIAN_POINT('Ctrl Pts',(-1.9571996697324,4.08272333451412E-5,
2.32586969212423));
#35309=CARTESIAN_POINT('Ctrl Pts',(-1.9572003426898,0.00222795607483405,
2.32574442104715));
#35310=CARTESIAN_POINT('Ctrl Pts',(-1.95719699336635,0.00441508279392128,
2.32561914997006));
#35311=CARTESIAN_POINT('Ctrl Pts',(-1.95718961556757,0.00660219592375261,
2.32549387889298));
#35312=CARTESIAN_POINT('Ctrl Pts',(-1.9550083208942,0.653236559609951,2.2884566620645));
#35313=CARTESIAN_POINT('Ctrl Pts',(-1.60068669068514,1.29868304829585,2.25141944523602));
#35314=CARTESIAN_POINT('Ctrl Pts',(-1.05631192010051,1.64767712566922,2.21438222840754));
#35315=CARTESIAN_POINT('Ctrl Pts',(-0.511937149515876,1.9966712030426,2.17734501157906));
#35316=CARTESIAN_POINT('Ctrl Pts',(0.222490761444335,2.04921286910345,2.14030779475058));
#35317=CARTESIAN_POINT('Ctrl Pts',(0.811002035332165,1.78126653559889,2.10327057792211));
#35318=CARTESIAN_POINT('Ctrl Pts',(1.39951330921999,1.51332020209433,2.06623336109363));
#35319=CARTESIAN_POINT('Ctrl Pts',(1.84210794603544,0.92488586902436,2.02919614426515));
#35320=CARTESIAN_POINT('Ctrl Pts',(1.93631757329266,0.28514740055385,1.99215892743667));
#35321=CARTESIAN_POINT('Ctrl Pts',(2.03052720054988,-0.354591067916664,
1.95512171060819));
#35322=CARTESIAN_POINT('Ctrl Pts',(1.77635181824887,-1.04563367178771,1.91808449377971));
#35323=CARTESIAN_POINT('Ctrl Pts',(1.29006594271768,-1.47185755477259,1.88104727695123));
#35324=CARTESIAN_POINT('Ctrl Pts',(0.803780067186484,-1.89808143775746,
1.84401006012275));
#35325=CARTESIAN_POINT('Ctrl Pts',(0.0853836984250916,-2.05948659985616,
1.80697284329427));
#35326=CARTESIAN_POINT('Ctrl Pts',(-0.536487147273854,-1.88223703762279,
1.76993562646579));
#35327=CARTESIAN_POINT('Ctrl Pts',(-1.1583579929728,-1.70498747538942,1.73289840963732));
#35328=CARTESIAN_POINT('Ctrl Pts',(-1.68370331560931,-1.18908318882399,
1.69586119280884));
#35329=CARTESIAN_POINT('Ctrl Pts',(-1.87219978227984,-0.570528529192665,
1.65882397598036));
#35330=CARTESIAN_POINT('Ctrl Pts',(-1.92810540551016,-0.387073187246384,
1.64783921469498));
#35331=CARTESIAN_POINT('Ctrl Pts',(-1.95438048401311,-0.194588316428208,
1.63685445340961));
#35332=CARTESIAN_POINT('Ctrl Pts',(-1.95279554503994,-0.00168121501241192,
1.62586969212423));
#35333=CARTESIAN_POINT('Ctrl Pts',(-1.95287184048439,-0.00170298928284375,
1.52413030787576));
#35334=CARTESIAN_POINT('Ctrl Pts',(-1.95445695530526,-0.191812291650776,
1.53495683112926));
#35335=CARTESIAN_POINT('Ctrl Pts',(-1.92895173588402,-0.381505322742495,
1.54578335438277));
#35336=CARTESIAN_POINT('Ctrl Pts',(-1.87462310228398,-0.562548805321496,
1.55660987763628));
#35337=CARTESIAN_POINT('Ctrl Pts',(-1.68864138181028,-1.18230999089587,
1.59367201758));
#35338=CARTESIAN_POINT('Ctrl Pts',(-1.16488397934787,-1.70070889059895,
1.63073415752372));
#35339=CARTESIAN_POINT('Ctrl Pts',(-0.543243355780667,-1.88030816136644,
1.66779629746744));
#35340=CARTESIAN_POINT('Ctrl Pts',(0.0783972677865321,-2.05990743213392,
1.70485843741116));
#35341=CARTESIAN_POINT('Ctrl Pts',(0.797921112458524,-1.90070707396579,
1.74192057735488));
#35342=CARTESIAN_POINT('Ctrl Pts',(1.28577075941843,-1.47562399010748,1.7789827172986));
#35343=CARTESIAN_POINT('Ctrl Pts',(1.77362040637834,-1.05054090624917,1.81604485724232));
#35344=CARTESIAN_POINT('Ctrl Pts',(2.02979585562615,-0.359575096700667,
1.85310699718604));
#35345=CARTESIAN_POINT('Ctrl Pts',(1.93696313672928,0.28079594435252,1.89016913712977));
#35346=CARTESIAN_POINT('Ctrl Pts',(1.84413041783241,0.921166985405712,1.92723127707349));
#35347=CARTESIAN_POINT('Ctrl Pts',(1.40228953079084,1.51094325796358,1.96429341701721));
#35348=CARTESIAN_POINT('Ctrl Pts',(0.813813216582781,1.77999452248681,2.00135555696093));
#35349=CARTESIAN_POINT('Ctrl Pts',(0.225336902374724,2.04904578701004,2.03841769690465));
#35350=CARTESIAN_POINT('Ctrl Pts',(-0.509774838999831,1.99737204349863,
2.07547983684837));
#35351=CARTESIAN_POINT('Ctrl Pts',(-1.05482489992153,1.64864094185095,2.11254197679209));
#35352=CARTESIAN_POINT('Ctrl Pts',(-1.59987496084323,1.29990984020327,2.14960411673581));
#35353=CARTESIAN_POINT('Ctrl Pts',(-1.95486334131209,0.654121380419318,
2.18666625667953));
#35354=CARTESIAN_POINT('Ctrl Pts',(-1.95719765431867,0.0070607094029605,
2.22372839662325));
#35355=CARTESIAN_POINT('Ctrl Pts',(-1.95720609227958,0.00472174601940803,
2.22386236704075));
#35356=CARTESIAN_POINT('Ctrl Pts',(-1.95720992231195,0.00238276601260064,
2.22399633745825));
#35357=CARTESIAN_POINT('Ctrl Pts',(-1.95720915199432,4.37834080701142E-5,
2.22413030787575));
#35358=CARTESIAN_POINT('Origin',(0.,0.,0.));
#35359=CARTESIAN_POINT('',(-1.95267691385146,0.00165493661177622,3.02586969212423));
#35360=CARTESIAN_POINT('',(-1.95274315056508,0.00167675988910205,2.92413030787576));
#35361=CARTESIAN_POINT('',(-1.954,-2.39295984553393E-16,0.));
#35362=CARTESIAN_POINT('Ctrl Pts',(-1.95267691385146,0.00165493661177622,
3.02586969212423));
#35363=CARTESIAN_POINT('Ctrl Pts',(-1.95426560914452,0.198992208020636,
3.01463438868469));
#35364=CARTESIAN_POINT('Ctrl Pts',(-1.92675342506316,0.395896803504792,
3.00339908524515));
#35365=CARTESIAN_POINT('Ctrl Pts',(-1.86830808103941,0.583146374609883,
2.9921637818056));
#35366=CARTESIAN_POINT('Ctrl Pts',(-1.67564280138135,1.20041523640586,2.95512656497712));
#35367=CARTESIAN_POINT('Ctrl Pts',(-1.14682887836242,1.71276357431471,2.91808934814864));
#35368=CARTESIAN_POINT('Ctrl Pts',(-0.523776367443795,1.8858136432031,2.88105213132016));
#35369=CARTESIAN_POINT('Ctrl Pts',(0.0992761434748341,2.0588637120915,2.84401491449168));
#35370=CARTESIAN_POINT('Ctrl Pts',(0.816567242293159,1.89261551195942,2.80697769766321));
#35371=CARTESIAN_POINT('Ctrl Pts',(1.29996651882171,1.46312057934516,2.76994048083473));
#35372=CARTESIAN_POINT('Ctrl Pts',(1.78336579535026,1.03362564673089,2.73290326400625));
#35373=CARTESIAN_POINT('Ctrl Pts',(2.03287324958903,0.340883981634439,2.69586604717777));
#35374=CARTESIAN_POINT('Ctrl Pts',(1.93434974962867,-0.298204336020968,
2.65882883034929));
#35375=CARTESIAN_POINT('Ctrl Pts',(1.83582624966831,-0.937292653676373,
2.62179161352081));
#35376=CARTESIAN_POINT('Ctrl Pts',(1.38927179550881,-1.52272762389073,2.58475439669233));
#35377=CARTESIAN_POINT('Ctrl Pts',(0.798966206784796,-1.78669745083631,
2.54771717986385));
#35378=CARTESIAN_POINT('Ctrl Pts',(0.208660618060775,-2.05066727778188,
2.51067996303538));
#35379=CARTESIAN_POINT('Ctrl Pts',(-0.525396105227766,-1.99317196145866,
2.4736427462069));
#35380=CARTESIAN_POINT('Ctrl Pts',(-1.0674039873032,-1.6405131839538,2.43660552937842));
#35381=CARTESIAN_POINT('Ctrl Pts',(-1.60757863467609,-1.28904720517098,
2.39969358362702));
#35382=CARTESIAN_POINT('Ctrl Pts',(-1.95700137841649,-0.644411052866131,
2.36278163787563));
#35383=CARTESIAN_POINT('Ctrl Pts',(-1.9571996697324,4.08272333451705E-5,
2.32586969212423));
#35384=CARTESIAN_POINT('Ctrl Pts',(-1.95720915199432,4.37834080700025E-5,
2.22413030787575));
#35385=CARTESIAN_POINT('Ctrl Pts',(-1.95699681840184,-0.644683222376,2.26105847740198));
#35386=CARTESIAN_POINT('Ctrl Pts',(-1.60725113883781,-1.28960760246236,
2.2979866469282));
#35387=CARTESIAN_POINT('Ctrl Pts',(-1.06669244200308,-1.64098742623895,
2.33491481645442));
#35388=CARTESIAN_POINT('Ctrl Pts',(-0.524172671136578,-1.99364200861572,
2.37197695639814));
#35389=CARTESIAN_POINT('Ctrl Pts',(0.210547116140745,-2.05061829112049,
2.40903909634186));
#35390=CARTESIAN_POINT('Ctrl Pts',(0.800949322066953,-1.78581989384044,
2.44610123628558));
#35391=CARTESIAN_POINT('Ctrl Pts',(1.39135152799316,-1.52102149656038,2.4831633762293));
#35392=CARTESIAN_POINT('Ctrl Pts',(1.83743615256826,-0.934448419495488,
2.52022551617302));
#35393=CARTESIAN_POINT('Ctrl Pts',(1.93488676008295,-0.294763859316313,
2.55728765611674));
#35394=CARTESIAN_POINT('Ctrl Pts',(2.03233736759764,0.344920700862864,2.59434979606046));
#35395=CARTESIAN_POINT('Ctrl Pts',(1.78115395805193,1.03771674415633,2.63141193600418));
#35396=CARTESIAN_POINT('Ctrl Pts',(1.29638398231036,1.46630865646616,2.6684740759479));
#35397=CARTESIAN_POINT('Ctrl Pts',(0.811614006568792,1.894900568776,2.70553621589162));
#35398=CARTESIAN_POINT('Ctrl Pts',(0.0932574646313782,2.05928835010221,
2.74259835583535));
#35399=CARTESIAN_POINT('Ctrl Pts',(-0.529662765081927,1.88417882975093,
2.77966049577907));
#35400=CARTESIAN_POINT('Ctrl Pts',(-1.15258299479523,1.70906930939964,2.81672263572279));
#35401=CARTESIAN_POINT('Ctrl Pts',(-1.68006691228442,1.19446248737086,2.85378477566651));
#35402=CARTESIAN_POINT('Ctrl Pts',(-1.87051544101399,0.576059451476712,
2.89084691561023));
#35403=CARTESIAN_POINT('Ctrl Pts',(-1.92752575844056,0.390941962730205,
2.90194137969874));
#35404=CARTESIAN_POINT('Ctrl Pts',(-1.95433466869055,0.196523398123763,
2.91303584378725));
#35405=CARTESIAN_POINT('Ctrl Pts',(-1.95274315056508,0.00167675988910205,
2.92413030787576));
#35406=CARTESIAN_POINT('Origin',(0.,0.,0.));
#35407=CARTESIAN_POINT('',(-1.95135107115213,-0.00103745302926256,3.72586969212423));
#35408=CARTESIAN_POINT('',(-1.95125983814034,-0.000967513988672578,3.62413030787576));
#35409=CARTESIAN_POINT('',(-1.954,-2.39295984553393E-16,0.));
#35410=CARTESIAN_POINT('Ctrl Pts',(-1.95135107115213,-0.00103745302926256,
3.72586969212423));
#35411=CARTESIAN_POINT('Ctrl Pts',(-1.9494564270682,0.392108141373472,3.70352435632223));
#35412=CARTESIAN_POINT('Ctrl Pts',(-1.83428685915158,0.78627490539017,3.68117902052023));
#35413=CARTESIAN_POINT('Ctrl Pts',(-1.61345116677478,1.10788542383069,3.65883368471823));
#35414=CARTESIAN_POINT('Ctrl Pts',(-1.24741775852795,1.64095230684139,3.62179646788975));
#35415=CARTESIAN_POINT('Ctrl Pts',(-0.591089924893776,1.97468687095231,
3.58475925106126));
#35416=CARTESIAN_POINT('Ctrl Pts',(0.0552900452708404,1.95641963566092,
3.54772203423278));
#35417=CARTESIAN_POINT('Ctrl Pts',(0.701670015435453,1.93815240036952,3.51068481740431));
#35418=CARTESIAN_POINT('Ctrl Pts',(1.3381021221305,1.56788336567581,3.47364760057583));
#35419=CARTESIAN_POINT('Ctrl Pts',(1.6734455320356,1.01499499073225,3.43661038374735));
#35420=CARTESIAN_POINT('Ctrl Pts',(2.0087889419407,0.462106615788698,3.39957316691887));
#35421=CARTESIAN_POINT('Ctrl Pts',(2.04304365505584,-0.273401099404705,
3.36253595009039));
#35422=CARTESIAN_POINT('Ctrl Pts',(1.76053958557416,-0.855064411333041,
3.32549873326191));
#35423=CARTESIAN_POINT('Ctrl Pts',(1.47803551609248,-1.43672772326139,3.28846151643343));
#35424=CARTESIAN_POINT('Ctrl Pts',(0.878772664013962,-1.86454663192466,
3.25142429960495));
#35425=CARTESIAN_POINT('Ctrl Pts',(0.236888497103484,-1.94281203925035,
3.21438708277648));
#35426=CARTESIAN_POINT('Ctrl Pts',(-0.404995669806982,-2.02107744657604,
3.177349865948));
#35427=CARTESIAN_POINT('Ctrl Pts',(-1.08950115154941,-1.74978935256416,
3.14031264911952));
#35428=CARTESIAN_POINT('Ctrl Pts',(-1.50349557427203,-1.25305061271667,
3.10327543229104));
#35429=CARTESIAN_POINT('Ctrl Pts',(-1.79190407667273,-0.906998424134863,
3.0774735189021));
#35430=CARTESIAN_POINT('Ctrl Pts',(-1.94902846959061,-0.451530792879088,
3.05167160551317));
#35431=CARTESIAN_POINT('Ctrl Pts',(-1.95267691385146,0.00165493661177622,
3.02586969212423));
#35432=CARTESIAN_POINT('Ctrl Pts',(-1.95274315056508,0.00167675988910205,
2.92413030787576));
#35433=CARTESIAN_POINT('Ctrl Pts',(-1.94901804708373,-0.45438081105706,
2.95009798373097));
#35434=CARTESIAN_POINT('Ctrl Pts',(-1.78970412039892,-0.912783539307832,
2.97606565958618));
#35435=CARTESIAN_POINT('Ctrl Pts',(-1.49789482266332,-1.25975537577289,
3.00203333544139));
#35436=CARTESIAN_POINT('Ctrl Pts',(-1.08141253561316,-1.75496791736879,
3.03909547538511));
#35437=CARTESIAN_POINT('Ctrl Pts',(-0.3950348215429,-2.02319375080107,3.07615761532883));
#35438=CARTESIAN_POINT('Ctrl Pts',(0.246862437687336,-1.94157962588032,
3.11321975527255));
#35439=CARTESIAN_POINT('Ctrl Pts',(0.888759696917571,-1.85996550095957,
3.15028189521628));
#35440=CARTESIAN_POINT('Ctrl Pts',(1.48617650130778,-1.4285114176858,3.18734403516));
#35441=CARTESIAN_POINT('Ctrl Pts',(1.76548299529208,-0.84483270534745,3.22440617510372));
#35442=CARTESIAN_POINT('Ctrl Pts',(2.04478948927638,-0.261153993009101,
3.26146831504744));
#35443=CARTESIAN_POINT('Ctrl Pts',(2.00598567285476,0.474749348393822,3.29853045499116));
#35444=CARTESIAN_POINT('Ctrl Pts',(1.66684453569178,1.02581762536563,3.33559259493488));
#35445=CARTESIAN_POINT('Ctrl Pts',(1.3277033985288,1.57688590233743,3.3726547348786));
#35446=CARTESIAN_POINT('Ctrl Pts',(0.688224940624468,1.94311911487812,3.40971687482232));
#35447=CARTESIAN_POINT('Ctrl Pts',(0.0413041672205065,1.95677450731496,
3.44677901476604));
#35448=CARTESIAN_POINT('Ctrl Pts',(-0.605616606183457,1.9704298997518,3.48384115470976));
#35449=CARTESIAN_POINT('Ctrl Pts',(-1.25997969508704,1.63150747208479,3.52090329465349));
#35450=CARTESIAN_POINT('Ctrl Pts',(-1.62207261036362,1.09524104808107,3.55796543459721));
#35451=CARTESIAN_POINT('Ctrl Pts',(-1.83754705311226,0.776119342016343,
3.58002039235672));
#35452=CARTESIAN_POINT('Ctrl Pts',(-1.94952253842872,0.387114015523011,
3.60207535011624));
#35453=CARTESIAN_POINT('Ctrl Pts',(-1.95125983814034,-0.000967513988672578,
3.62413030787576));
#35454=CARTESIAN_POINT('Origin',(0.,0.,0.));
#35455=CARTESIAN_POINT('',(-1.95645574651684,-0.00107576288577632,4.42586969212423));
#35456=CARTESIAN_POINT('',(-1.95628130950281,-0.00119277919923279,4.32413030787576));
#35457=CARTESIAN_POINT('',(-1.954,-2.39295984553393E-16,0.));
#35458=CARTESIAN_POINT('Ctrl Pts',(-1.95645574651684,-0.00107576288577632,
4.42586969212423));
#35459=CARTESIAN_POINT('Ctrl Pts',(-1.95258201164419,0.583617837825317,
4.39241432395977));
#35460=CARTESIAN_POINT('Ctrl Pts',(-1.67312331125722,1.17152394520949,4.35895895579531));
#35461=CARTESIAN_POINT('Ctrl Pts',(-1.21525966387556,1.53420296221226,4.32550358763085));
#35462=CARTESIAN_POINT('Ctrl Pts',(-0.70837553387317,1.93571166257503,4.28846637080237));
#35463=CARTESIAN_POINT('Ctrl Pts',(0.0171598407939347,2.06118438706562,
4.25142915397389));
#35464=CARTESIAN_POINT('Ctrl Pts',(0.629444641593513,1.8532226587955,4.21439193714541));
#35465=CARTESIAN_POINT('Ctrl Pts',(1.24172944239309,1.64526093052537,4.17735472031693));
#35466=CARTESIAN_POINT('Ctrl Pts',(1.74076366932515,1.10386474949453,4.14031750348845));
#35467=CARTESIAN_POINT('Ctrl Pts',(1.89826022128925,0.476700023258525,4.10328028665997));
#35468=CARTESIAN_POINT('Ctrl Pts',(2.05575677325334,-0.150464702977478,
4.06624306983149));
#35469=CARTESIAN_POINT('Ctrl Pts',(1.87171565024948,-0.86339797441863,4.02920585300301));
#35470=CARTESIAN_POINT('Ctrl Pts',(1.43032790007833,-1.33596290298842,3.99216863617453));
#35471=CARTESIAN_POINT('Ctrl Pts',(0.988940149907184,-1.80852783155821,
3.95513141934605));
#35472=CARTESIAN_POINT('Ctrl Pts',(0.290205772568748,-2.04072441725662,
3.91809420251758));
#35473=CARTESIAN_POINT('Ctrl Pts',(-0.346233738762281,-1.92633252011348,
3.8810569856891));
#35474=CARTESIAN_POINT('Ctrl Pts',(-0.982673250093302,-1.81194062297035,
3.84401976886062));
#35475=CARTESIAN_POINT('Ctrl Pts',(-1.55681789541692,-1.35096024298568,
3.80698255203214));
#35476=CARTESIAN_POINT('Ctrl Pts',(-1.806020726649,-0.754270452038098,3.76994533520366));
#35477=CARTESIAN_POINT('Ctrl Pts',(-1.90487422217158,-0.517576224744695,
3.75525345417718));
#35478=CARTESIAN_POINT('Ctrl Pts',(-1.9525967846073,-0.259527562563923,
3.74056157315071));
#35479=CARTESIAN_POINT('Ctrl Pts',(-1.95135107115213,-0.00103745302926256,
3.72586969212423));
#35480=CARTESIAN_POINT('Ctrl Pts',(-1.95125983814034,-0.000967513988672578,
3.62413030787576));
#35481=CARTESIAN_POINT('Ctrl Pts',(-1.95244197476311,-0.265035587897937,
3.63913749005996));
#35482=CARTESIAN_POINT('Ctrl Pts',(-1.90258326051973,-0.528675939020291,
3.65414467224416));
#35483=CARTESIAN_POINT('Ctrl Pts',(-1.799560505048,-0.769580726996389,3.66915185442837));
#35484=CARTESIAN_POINT('Ctrl Pts',(-1.54513274280624,-1.36452565772967,
3.70621399437209));
#35485=CARTESIAN_POINT('Ctrl Pts',(-0.966454476673152,-1.8208050988558,
3.74327613431581));
#35486=CARTESIAN_POINT('Ctrl Pts',(-0.328572905191125,-1.92943316874967,
3.78033827425953));
#35487=CARTESIAN_POINT('Ctrl Pts',(0.309308666290907,-2.03806123864353,
3.81740041420325));
#35488=CARTESIAN_POINT('Ctrl Pts',(1.00639354312189,-1.79903793730513,3.85446255414697));
#35489=CARTESIAN_POINT('Ctrl Pts',(1.44340173058911,-1.32184112162819,3.89152469409069));
#35490=CARTESIAN_POINT('Ctrl Pts',(1.88040991805633,-0.844644305951239,
3.92858683403441));
#35491=CARTESIAN_POINT('Ctrl Pts',(2.05734141615979,-0.129273975935752,
3.96564897397814));
#35492=CARTESIAN_POINT('Ctrl Pts',(1.89315776078089,0.496614739501458,4.00271111392186));
#35493=CARTESIAN_POINT('Ctrl Pts',(1.72897410540198,1.12250345493866,4.03977325386558));
#35494=CARTESIAN_POINT('Ctrl Pts',(1.22367529654071,1.65891055579759,4.0768353938093));
#35495=CARTESIAN_POINT('Ctrl Pts',(0.608699149567017,1.86014995417357,4.11389753375302));
#35496=CARTESIAN_POINT('Ctrl Pts',(-0.00627699740667481,2.06138935254956,
4.15095967369674));
#35497=CARTESIAN_POINT('Ctrl Pts',(-0.730930482492791,1.9274610484426,4.18802181364046));
#35498=CARTESIAN_POINT('Ctrl Pts',(-1.23335429038162,1.51970711029871,4.22508395358418));
#35499=CARTESIAN_POINT('Ctrl Pts',(-1.68092015819396,1.15647443240051,4.25809940501471));
#35500=CARTESIAN_POINT('Ctrl Pts',(-1.95213599025838,0.575947822566119,
4.29111485644523));
#35501=CARTESIAN_POINT('Ctrl Pts',(-1.95628130950281,-0.00119277919923279,
4.32413030787576));
#35502=CARTESIAN_POINT('Origin',(0.,0.,0.));
#35503=CARTESIAN_POINT('',(-1.95458266482996,0.00173443779922018,5.12586969212423));
#35504=CARTESIAN_POINT('',(-1.95491180920002,0.00168629508682236,5.02413030787576));
#35505=CARTESIAN_POINT('',(-1.954,-2.39295984553393E-16,0.));
#35506=CARTESIAN_POINT('Ctrl Pts',(-1.95458266482996,0.00173443779922018,
5.12586969212423));
#35507=CARTESIAN_POINT('Ctrl Pts',(-1.95579683437623,0.13363129532035,5.11834150842579));
#35508=CARTESIAN_POINT('Ctrl Pts',(-1.94358523444966,0.265304620125551,
5.11081332472735));
#35509=CARTESIAN_POINT('Ctrl Pts',(-1.91712292268468,0.394048828472761,
5.10328514102891));
#35510=CARTESIAN_POINT('Ctrl Pts',(-1.78693343503641,1.0274455880328,5.06624792420043));
#35511=CARTESIAN_POINT('Ctrl Pts',(-1.31181246839585,1.58994452273665,5.02921070737195));
#35512=CARTESIAN_POINT('Ctrl Pts',(-0.709107816346671,1.8242261056952,4.99217349054347));
#35513=CARTESIAN_POINT('Ctrl Pts',(-0.106403164297495,2.05850768865374,
4.95513627371499));
#35514=CARTESIAN_POINT('Ctrl Pts',(0.623885173160298,1.96457191986698,4.91809905688651));
#35515=CARTESIAN_POINT('Ctrl Pts',(1.14768109757825,1.58539044975217,4.88106184005803));
#35516=CARTESIAN_POINT('Ctrl Pts',(1.67147702199619,1.20620897963737,4.84402462322955));
#35517=CARTESIAN_POINT('Ctrl Pts',(1.9887805333743,0.541781808194522,4.80698740640107));
#35518=CARTESIAN_POINT('Ctrl Pts',(1.95443866449662,-0.103943670439598,
4.76995018957259));
#35519=CARTESIAN_POINT('Ctrl Pts',(1.92009679561895,-0.749669149073727,
4.73291297274411));
#35520=CARTESIAN_POINT('Ctrl Pts',(1.53410954648549,-1.37669293489913,4.69587575591563));
#35521=CARTESIAN_POINT('Ctrl Pts',(0.973049796091196,-1.69817810439032,
4.65883853908716));
#35522=CARTESIAN_POINT('Ctrl Pts',(0.411990045696909,-2.0196632738815,4.62180132225868));
#35523=CARTESIAN_POINT('Ctrl Pts',(-0.324142205958206,-2.03560982703848,
4.5847641054302));
#35524=CARTESIAN_POINT('Ctrl Pts',(-0.898597516275757,-1.7387228886878,
4.54772688860172));
#35525=CARTESIAN_POINT('Ctrl Pts',(-1.47305282659331,-1.44183595033712,
4.51068967177324));
#35526=CARTESIAN_POINT('Ctrl Pts',(-1.8858311955733,-0.832115520478776,
4.47365245494476));
#35527=CARTESIAN_POINT('Ctrl Pts',(-1.94810393739446,-0.188482967432129,
4.43661523811628));
#35528=CARTESIAN_POINT('Ctrl Pts',(-1.9541262996613,-0.126237620787308,
4.43303338945226));
#35529=CARTESIAN_POINT('Ctrl Pts',(-1.95687048211354,-0.0636751036633503,
4.42945154078825));
#35530=CARTESIAN_POINT('Ctrl Pts',(-1.95645574651684,-0.00107576288577632,
4.42586969212423));
#35531=CARTESIAN_POINT('Ctrl Pts',(-1.95628130950281,-0.00119277919923279,
4.32413030787576));
#35532=CARTESIAN_POINT('Ctrl Pts',(-1.95678939935296,-0.0719326340995119,
4.32817699638895));
#35533=CARTESIAN_POINT('Ctrl Pts',(-1.95328521122814,-0.14262162001596,
4.33222368490215));
#35534=CARTESIAN_POINT('Ctrl Pts',(-1.94560169264522,-0.212853377401693,
4.33627037341534));
#35535=CARTESIAN_POINT('Ctrl Pts',(-1.87523115632842,-0.856080354777335,
4.37333251335906));
#35536=CARTESIAN_POINT('Ctrl Pts',(-1.45429595300328,-1.46095473734778,
4.41039465330279));
#35537=CARTESIAN_POINT('Ctrl Pts',(-0.875593536694013,-1.75043093699665,
4.44745679324651));
#35538=CARTESIAN_POINT('Ctrl Pts',(-0.296891120384743,-2.03990713664554,
4.48451893319023));
#35539=CARTESIAN_POINT('Ctrl Pts',(0.439578508908652,-2.01398515337285,
4.52158107313395));
#35540=CARTESIAN_POINT('Ctrl Pts',(0.9964962855145,-1.68453781781564,4.55864321307767));
#35541=CARTESIAN_POINT('Ctrl Pts',(1.55341406212034,-1.35509048225843,4.59570535302139));
#35542=CARTESIAN_POINT('Ctrl Pts',(1.93077998603865,-0.72211779441669,4.63276749296511));
#35543=CARTESIAN_POINT('Ctrl Pts',(1.95575227831571,-0.0755349757277263,
4.66982963290883));
#35544=CARTESIAN_POINT('Ctrl Pts',(1.98072457059277,0.571047842961237,4.70689177285256));
#35545=CARTESIAN_POINT('Ctrl Pts',(1.6533032312286,1.23124079249743,4.74395391279628));
#35546=CARTESIAN_POINT('Ctrl Pts',(1.12345433605614,1.60266118112717,4.78101605273999));
#35547=CARTESIAN_POINT('Ctrl Pts',(0.59360544088369,1.97408156975691,4.81807819268371));
#35548=CARTESIAN_POINT('Ctrl Pts',(-0.138671010097046,2.05672939748021,
4.85514033262744));
#35549=CARTESIAN_POINT('Ctrl Pts',(-0.737976517839776,1.81275016640803,
4.89220247257116));
#35550=CARTESIAN_POINT('Ctrl Pts',(-1.33728202558251,1.56877093533586,4.92926461251488));
#35551=CARTESIAN_POINT('Ctrl Pts',(-1.80361659008724,0.998164645468222,
4.9663267524586));
#35552=CARTESIAN_POINT('Ctrl Pts',(-1.92338886510923,0.362281355122108,
5.00338889240232));
#35553=CARTESIAN_POINT('Ctrl Pts',(-1.94573194011967,0.243659678682544,
5.01030269756014));
#35554=CARTESIAN_POINT('Ctrl Pts',(-1.95601481281436,0.122766393772507,
5.01721650271795));
#35555=CARTESIAN_POINT('Ctrl Pts',(-1.95491180920002,0.00168629508682236,
5.02413030787576));
#35556=CARTESIAN_POINT('Origin',(0.,0.,0.));
#35557=CARTESIAN_POINT('',(-1.9507978584999,-3.45334863967226E-5,5.82586969212423));
#35558=CARTESIAN_POINT('',(-1.95080468396925,0.00018981806121043,5.72413030787576));
#35559=CARTESIAN_POINT('',(-1.954,-2.39295984553393E-16,0.));
#35560=CARTESIAN_POINT('Ctrl Pts',(-1.95079815420139,-3.45302974047446E-5,
5.82586969212423));
#35561=CARTESIAN_POINT('Ctrl Pts',(-1.95074640707532,0.328120037045956,
5.80723147606333));
#35562=CARTESIAN_POINT('Ctrl Pts',(-1.87237758907749,0.656297824114404,
5.78859326000243));
#35563=CARTESIAN_POINT('Ctrl Pts',(-1.715829951129,0.941574404236039,5.76995504394152));
#35564=CARTESIAN_POINT('Ctrl Pts',(-1.4047439120071,1.50846613462089,5.73291782711304));
#35565=CARTESIAN_POINT('Ctrl Pts',(-0.784943311216198,1.90594846094957,
5.69588061028457));
#35566=CARTESIAN_POINT('Ctrl Pts',(-0.139960769924853,1.95218999146749,
5.65884339345609));
#35567=CARTESIAN_POINT('Ctrl Pts',(0.505021771366483,1.99843152198542,5.62180617662761));
#35568=CARTESIAN_POINT('Ctrl Pts',(1.17518625315826,1.69343225669258,5.58476895979913));
#35569=CARTESIAN_POINT('Ctrl Pts',(1.56396070392606,1.17671648942254,5.54773174297065));
#35570=CARTESIAN_POINT('Ctrl Pts',(1.95273515469386,0.660000722152496,5.51069452614217));
#35571=CARTESIAN_POINT('Ctrl Pts',(2.06011957443768,-0.0684315470947738,
5.47365730931369));
#35572=CARTESIAN_POINT('Ctrl Pts',(1.83699012241942,-0.675353292756691,
5.43662009248521));
#35573=CARTESIAN_POINT('Ctrl Pts',(1.61386067040115,-1.28227503841861,5.39958287565673));
#35574=CARTESIAN_POINT('Ctrl Pts',(1.06021734662079,-1.76768626049519,5.36254565882826));
#35575=CARTESIAN_POINT('Ctrl Pts',(0.429328609649713,-1.90953180775813,
5.32550844199978));
#35576=CARTESIAN_POINT('Ctrl Pts',(-0.201560127321352,-2.05137735502108,
5.2884712251713));
#35577=CARTESIAN_POINT('Ctrl Pts',(-0.909694277483132,-1.84965722747041,
5.25143400834282));
#35578=CARTESIAN_POINT('Ctrl Pts',(-1.37113234823603,-1.39664987148696,
5.21439679151434));
#35579=CARTESIAN_POINT('Ctrl Pts',(-1.73877852911313,-1.03572077852157,
5.1848877583843));
#35580=CARTESIAN_POINT('Ctrl Pts',(-1.94982335358017,-0.515275892214865,
5.15537872525427));
#35581=CARTESIAN_POINT('Ctrl Pts',(-1.95458266482996,0.00173443779922018,
5.12586969212423));
#35582=CARTESIAN_POINT('Ctrl Pts',(-1.95491180920002,0.00168629508682236,
5.02413030787576));
#35583=CARTESIAN_POINT('Ctrl Pts',(-1.95010205227512,-0.526295513449078,
5.05427864266167));
#35584=CARTESIAN_POINT('Ctrl Pts',(-1.72879182329996,-1.05782955367232,
5.08442697744757));
#35585=CARTESIAN_POINT('Ctrl Pts',(-1.34689356786549,-1.42005289462677,
5.11457531223348));
#35586=CARTESIAN_POINT('Ctrl Pts',(-0.877416010060499,-1.86534356320495,
5.1516374521772));
#35587=CARTESIAN_POINT('Ctrl Pts',(-0.165250908911267,-2.05476460953673,
5.18869959212092));
#35588=CARTESIAN_POINT('Ctrl Pts',(0.463414671012952,-1.90155708549211,
5.22576173206464));
#35589=CARTESIAN_POINT('Ctrl Pts',(1.09208025093718,-1.74834956144749,5.26282387200837));
#35590=CARTESIAN_POINT('Ctrl Pts',(1.63724630963639,-1.25251346702646,5.29988601195209));
#35591=CARTESIAN_POINT('Ctrl Pts',(1.84921496651671,-0.641152489120857,
5.33694815189581));
#35592=CARTESIAN_POINT('Ctrl Pts',(2.06118362339704,-0.0297915112152539,
5.37401029183953));
#35593=CARTESIAN_POINT('Ctrl Pts',(1.93995487845847,0.697094350174917,5.41107243178325));
#35594=CARTESIAN_POINT('Ctrl Pts',(1.54105412656959,1.20657560296821,5.44813457172697));
#35595=CARTESIAN_POINT('Ctrl Pts',(1.14215337468071,1.71605685576151,5.48519671167069));
#35596=CARTESIAN_POINT('Ctrl Pts',(0.465580615841514,2.00813349995792,5.52225885161441));
#35597=CARTESIAN_POINT('Ctrl Pts',(-0.178779150223708,1.94902809680635,
5.55932099155813));
#35598=CARTESIAN_POINT('Ctrl Pts',(-0.823138916288934,1.88992269365477,
5.59638313150186));
#35599=CARTESIAN_POINT('Ctrl Pts',(-1.43528568958019,1.4796352431552,5.63344527144558));
#35600=CARTESIAN_POINT('Ctrl Pts',(-1.73484296927877,0.906086297567352,
5.6705074113893));
#35601=CARTESIAN_POINT('Ctrl Pts',(-1.87931321146693,0.629475576708828,
5.68838171021812));
#35602=CARTESIAN_POINT('Ctrl Pts',(-1.95107725773013,0.31489133949035,5.70625600904694));
#35603=CARTESIAN_POINT('Ctrl Pts',(-1.95080468396925,0.00018981806121043,
5.72413030787576));
#35604=CARTESIAN_POINT('Origin',(0.,0.,0.));
#35605=CARTESIAN_POINT('',(-1.95470932084261,-0.00171584046685047,6.52586969212424));
#35606=CARTESIAN_POINT('',(-1.95421427783755,-0.00177812761388513,6.42413030787576));
#35607=CARTESIAN_POINT('',(-1.954,-2.39295984553393E-16,0.));
#35608=CARTESIAN_POINT('Ctrl Pts',(-1.95470932084261,-0.00171584046685047,
6.52586969212424));
#35609=CARTESIAN_POINT('Ctrl Pts',(-1.94992946923152,0.519398730151351,
6.49612144370087));
#35610=CARTESIAN_POINT('Ctrl Pts',(-1.73506994162404,1.04399306729571,6.46637319527751));
#35611=CARTESIAN_POINT('Ctrl Pts',(-1.36210733975536,1.40545308526766,6.43662494685414));
#35612=CARTESIAN_POINT('Ctrl Pts',(-0.897760782010601,1.85547867567989,
6.39958773002566));
#35613=CARTESIAN_POINT('Ctrl Pts',(-0.188341937200331,2.05263315093338,
6.36255051319719));
#35614=CARTESIAN_POINT('Ctrl Pts',(0.441620008484366,1.90672665791667,6.32551329636871));
#35615=CARTESIAN_POINT('Ctrl Pts',(1.07158195416906,1.76082016489995,6.28847607954023));
#35616=CARTESIAN_POINT('Ctrl Pts',(1.62208700072817,1.27185270361303,6.25143886271175));
#35617=CARTESIAN_POINT('Ctrl Pts',(1.84130231899333,0.663506254660481,6.21440164588327));
#35618=CARTESIAN_POINT('Ctrl Pts',(2.0605176372585,0.0551598057079281,6.17736442905479));
#35619=CARTESIAN_POINT('Ctrl Pts',(1.94844322722972,-0.672565630910262,
6.14032721222632));
#35620=CARTESIAN_POINT('Ctrl Pts',(1.55634840229719,-1.18676637573315,6.10328999539784));
#35621=CARTESIAN_POINT('Ctrl Pts',(1.16425357736466,-1.70096712055603,6.06625277856936));
#35622=CARTESIAN_POINT('Ctrl Pts',(0.492138337528384,-2.00164317358361,
6.02921556174087));
#35623=CARTESIAN_POINT('Ctrl Pts',(-0.152532956197894,-1.95124792816734,
5.9921783449124));
#35624=CARTESIAN_POINT('Ctrl Pts',(-0.797204249924167,-1.90085268275106,
5.95514112808392));
#35625=CARTESIAN_POINT('Ctrl Pts',(-1.41443159754043,-1.49938613889095,
5.91810391125544));
#35626=CARTESIAN_POINT('Ctrl Pts',(-1.72185953262212,-0.930502299740384,
5.88106669442696));
#35627=CARTESIAN_POINT('Ctrl Pts',(-1.87458069522289,-0.647897528391999,
5.86266769365939));
#35628=CARTESIAN_POINT('Ctrl Pts',(-1.95084923717034,-0.323977343102287,
5.84426869289181));
#35629=CARTESIAN_POINT('Ctrl Pts',(-1.95079815420139,-3.45302974047446E-5,
5.82586969212423));
#35630=CARTESIAN_POINT('Ctrl Pts',(-1.95080468396925,0.00018981806121043,
5.72413030787576));
#35631=CARTESIAN_POINT('Ctrl Pts',(-1.95051207937167,-0.337638415069996,
5.74331814899066));
#35632=CARTESIAN_POINT('Ctrl Pts',(-1.86720620393942,-0.675601803708791,
5.76250599010555));
#35633=CARTESIAN_POINT('Ctrl Pts',(-1.70171536425399,-0.966869859783203,
5.78169383122045));
#35634=CARTESIAN_POINT('Ctrl Pts',(-1.38206269342473,-1.5294666308698,5.81875597116418));
#35635=CARTESIAN_POINT('Ctrl Pts',(-0.755789565660301,-1.91784973236686,
5.85581811110791));
#35636=CARTESIAN_POINT('Ctrl Pts',(-0.109742658556152,-1.95413127900566,
5.89288025105163));
#35637=CARTESIAN_POINT('Ctrl Pts',(0.536304248547996,-1.99041282564447,
5.92994239099535));
#35638=CARTESIAN_POINT('Ctrl Pts',(1.20212493499187,-1.674592817425,5.96700453093906));
#35639=CARTESIAN_POINT('Ctrl Pts',(1.58275908344154,-1.15132366886058,6.00406667088278));
#35640=CARTESIAN_POINT('Ctrl Pts',(1.9633932318912,-0.628054520296152,6.0411288108265));
#35641=CARTESIAN_POINT('Ctrl Pts',(2.05884084234667,0.102663768613233,6.07819095077022));
#35642=CARTESIAN_POINT('Ctrl Pts',(1.82538483877546,0.706146370849535,6.11525309071394));
#35643=CARTESIAN_POINT('Ctrl Pts',(1.59192883520425,1.30962897308584,6.15231523065767));
#35644=CARTESIAN_POINT('Ctrl Pts',(1.02956921760636,1.78587588864905,6.18937737060139));
#35645=CARTESIAN_POINT('Ctrl Pts',(0.395878889512919,1.91675569949154,6.22643951054511));
#35646=CARTESIAN_POINT('Ctrl Pts',(-0.237811438580523,2.04763551033402,
6.26350165048883));
#35647=CARTESIAN_POINT('Ctrl Pts',(-0.942832477169518,1.83314821645578,
6.30056379043255));
#35648=CARTESIAN_POINT('Ctrl Pts',(-1.39626929730598,1.37153365109863,6.33762593037627));
#35649=CARTESIAN_POINT('Ctrl Pts',(-1.7490486198241,1.01239194403086,6.3664607228761));
#35650=CARTESIAN_POINT('Ctrl Pts',(-1.94954331224527,0.503663409317413,
6.39529551537593));
#35651=CARTESIAN_POINT('Ctrl Pts',(-1.95421427783755,-0.00177812761388513,
6.42413030787576));
#35652=CARTESIAN_POINT('Origin',(0.,0.,0.));
#35653=CARTESIAN_POINT('',(-1.95636369417486,0.00113518110994186,7.22586969212423));
#35654=CARTESIAN_POINT('',(-1.95675615924934,0.000851174274233985,7.12413030787576));
#35655=CARTESIAN_POINT('',(-1.954,-2.39295984553393E-16,0.));
#35656=CARTESIAN_POINT('Ctrl Pts',(-1.95636369417486,0.00113518110994186,
7.22586969212423));
#35657=CARTESIAN_POINT('Ctrl Pts',(-1.95682546989371,0.0679235189129894,
7.22204862816689));
#35658=CARTESIAN_POINT('Ctrl Pts',(-1.95370156992351,0.134668159558925,
7.21822756420955));
#35659=CARTESIAN_POINT('Ctrl Pts',(-1.94684940168549,0.201027826582277,
7.2144065002522));
#35660=CARTESIAN_POINT('Ctrl Pts',(-1.88043197355288,0.844245894546327,
7.17736928342373));
#35661=CARTESIAN_POINT('Ctrl Pts',(-1.46373463610807,1.45129475044757,7.14033206659525));
#35662=CARTESIAN_POINT('Ctrl Pts',(-0.887378837876281,1.74447515831938,
7.10329484976677));
#35663=CARTESIAN_POINT('Ctrl Pts',(-0.31102303964449,2.03765556619118,7.06625763293829));
#35664=CARTESIAN_POINT('Ctrl Pts',(0.424991219374283,2.01696752603353,7.02922041610981));
#35665=CARTESIAN_POINT('Ctrl Pts',(0.983968473233738,1.69187494324663,6.99218319928133));
#35666=CARTESIAN_POINT('Ctrl Pts',(1.54294572709319,1.36678236045973,6.95514598245285));
#35667=CARTESIAN_POINT('Ctrl Pts',(1.92488597579333,0.737285235043576,6.91810876562437));
#35668=CARTESIAN_POINT('Ctrl Pts',(1.95506767226643,0.0913519390189264,
6.8810715487959));
#35669=CARTESIAN_POINT('Ctrl Pts',(1.98524936873952,-0.554581357005719,
6.84403433196742));
#35670=CARTESIAN_POINT('Ctrl Pts',(1.66367251298559,-1.21695082363886,6.80699711513894));
#35671=CARTESIAN_POINT('Ctrl Pts',(1.13744494695038,-1.59275037986524,6.76995989831046));
#35672=CARTESIAN_POINT('Ctrl Pts',(0.611217380915185,-1.96854993609162,
6.73292268148198));
#35673=CARTESIAN_POINT('Ctrl Pts',(-0.119660895401274,-2.05777958191125,
6.69588546465349));
#35674=CARTESIAN_POINT('Ctrl Pts',(-0.72084391141631,-1.81962051958034,
6.65884824782502));
#35675=CARTESIAN_POINT('Ctrl Pts',(-1.32202692743135,-1.58146145724943,
6.62181103099654));
#35676=CARTESIAN_POINT('Ctrl Pts',(-1.79351468314497,-1.01591368676797,
6.58477381416807));
#35677=CARTESIAN_POINT('Ctrl Pts',(-1.91962142566216,-0.381691448741754,
6.54773659733959));
#35678=CARTESIAN_POINT('Ctrl Pts',(-1.9444393828574,-0.256875756563692,
6.54044762893447));
#35679=CARTESIAN_POINT('Ctrl Pts',(-1.95588048853217,-0.129400253566584,
6.53315866052935));
#35680=CARTESIAN_POINT('Ctrl Pts',(-1.95470932084261,-0.00171584046685047,
6.52586969212424));
#35681=CARTESIAN_POINT('Ctrl Pts',(-1.95421427783755,-0.00177812761388513,
6.42413030787576));
#35682=CARTESIAN_POINT('Ctrl Pts',(-1.95554703085897,-0.145994290672205,
6.43235765531965));
#35683=CARTESIAN_POINT('Ctrl Pts',(-1.94093747105224,-0.289942854151266,
6.44058500276354));
#35684=CARTESIAN_POINT('Ctrl Pts',(-1.90937423221194,-0.430072724152966,
6.44881235020743));
#35685=CARTESIAN_POINT('Ctrl Pts',(-1.7671897452975,-1.06132269721135,6.48587449015115));
#35686=CARTESIAN_POINT('Ctrl Pts',(-1.28096816978468,-1.61508080649208,
6.52293663009487));
#35687=CARTESIAN_POINT('Ctrl Pts',(-0.67340953434779,-1.83771382585667,
6.55999877003859));
#35688=CARTESIAN_POINT('Ctrl Pts',(-0.0658508989108841,-2.06034684522128,
6.59706090998232));
#35689=CARTESIAN_POINT('Ctrl Pts',(0.663044796450101,-1.95185477466974,
6.63412304992604));
#35690=CARTESIAN_POINT('Ctrl Pts',(1.17942751209788,-1.56192933591821,6.67118518986976));
#35691=CARTESIAN_POINT('Ctrl Pts',(1.69581022774564,-1.17200389716668,6.70824732981348));
#35692=CARTESIAN_POINT('Ctrl Pts',(1.9996799636802,-0.500645090215166,6.7453094697572));
#35693=CARTESIAN_POINT('Ctrl Pts',(1.95185778931935,0.144650188277344,6.78237160970092));
#35694=CARTESIAN_POINT('Ctrl Pts',(1.90403561495849,0.789945466769872,6.81943374964464));
#35695=CARTESIAN_POINT('Ctrl Pts',(1.5045215303022,1.4091772168034,6.85649588958836));
#35696=CARTESIAN_POINT('Ctrl Pts',(0.936301652358751,1.71872386452436,6.89355802953208));
#35697=CARTESIAN_POINT('Ctrl Pts',(0.368081774415317,2.02827051224532,6.9306201694758));
#35698=CARTESIAN_POINT('Ctrl Pts',(-0.368843896815252,2.02813205765373,
6.96768230941953));
#35699=CARTESIAN_POINT('Ctrl Pts',(-0.936947418561655,1.71837191595589,
7.00474444936325));
#35700=CARTESIAN_POINT('Ctrl Pts',(-1.50505094030807,1.40861177425805,7.04180658930697));
#35701=CARTESIAN_POINT('Ctrl Pts',(-1.90433231257031,0.78922994545395,7.07886872925069));
#35702=CARTESIAN_POINT('Ctrl Pts',(-1.95191200566454,0.143916742729559,
7.11593086919441));
#35703=CARTESIAN_POINT('Ctrl Pts',(-1.95542076848464,0.0963281429343837,
7.11866401542153));
#35704=CARTESIAN_POINT('Ctrl Pts',(-1.95701686505733,0.0485985200318871,
7.12139716164864));
#35705=CARTESIAN_POINT('Ctrl Pts',(-1.95675615924934,0.000851174274233985,
7.12413030787576));
#35706=CARTESIAN_POINT('Origin',(0.,0.,0.));
#35707=CARTESIAN_POINT('',(-1.95128545551857,0.000980157954364874,7.92586969212424));
#35708=CARTESIAN_POINT('',(-1.95166123101285,0.00126544742759004,7.82413030787576));
#35709=CARTESIAN_POINT('',(-1.954,-2.39295984553393E-16,0.));
#35710=CARTESIAN_POINT('Ctrl Pts',(-1.95128545551857,0.000980157954364874,
7.92586969212424));
#35711=CARTESIAN_POINT('Ctrl Pts',(-1.95247914943593,0.263701155015296,
7.91093859580443));
#35712=CARTESIAN_POINT('Ctrl Pts',(-1.90313505751618,0.525992349613935,
7.89600749948463));
#35713=CARTESIAN_POINT('Ctrl Pts',(-1.80112460177197,0.765888339627252,
7.88107640316483));
#35714=CARTESIAN_POINT('Ctrl Pts',(-1.54808334564134,1.36096050365993,7.84403918633635));
#35715=CARTESIAN_POINT('Ctrl Pts',(-0.970981193167941,1.81823294990903,
7.80700196950786));
#35716=CARTESIAN_POINT('Ctrl Pts',(-0.333818027149729,1.92852282969788,
7.76996475267938));
#35717=CARTESIAN_POINT('Ctrl Pts',(0.303345138868501,2.03881270948674,7.73292753585091));
#35718=CARTESIAN_POINT('Ctrl Pts',(1.00056931843154,1.80212002281537,7.69589031902244));
#35719=CARTESIAN_POINT('Ctrl Pts',(1.43890387011628,1.32672168613705,7.65885310219396));
#35720=CARTESIAN_POINT('Ctrl Pts',(1.87723842180101,0.851323349458752,7.62181588536548));
#35721=CARTESIAN_POINT('Ctrl Pts',(2.05668334560742,0.13721936277351,7.58477866853699));
#35722=CARTESIAN_POINT('Ctrl Pts',(1.8951501609247,-0.488917833023672,7.54774145170851));
#35723=CARTESIAN_POINT('Ctrl Pts',(1.73361697624198,-1.11505502882086,7.51070423488003));
#35724=CARTESIAN_POINT('Ctrl Pts',(1.23110568307013,-1.65322543373001,7.47366701805156));
#35725=CARTESIAN_POINT('Ctrl Pts',(0.61749399359133,-1.85723879665063,7.43662980122308));
#35726=CARTESIAN_POINT('Ctrl Pts',(0.00388230411252383,-2.06125215957126,
7.3995925843946));
#35727=CARTESIAN_POINT('Ctrl Pts',(-0.72082978167322,-1.93110848050335,
7.36255536756612));
#35728=CARTESIAN_POINT('Ctrl Pts',(-1.22511706515588,-1.52634300095596,
7.32551815073764));
#35729=CARTESIAN_POINT('Ctrl Pts',(-1.6773779241913,-1.16333645789233,7.2923019978665));
#35730=CARTESIAN_POINT('Ctrl Pts',(-1.95234952088687,-0.579449614967985,
7.25908584499537));
#35731=CARTESIAN_POINT('Ctrl Pts',(-1.95636369417486,0.00113518110994186,
7.22586969212423));
#35732=CARTESIAN_POINT('Ctrl Pts',(-1.95675615924934,0.000851174274233985,
7.12413030787576));
#35733=CARTESIAN_POINT('Ctrl Pts',(-1.95348162971424,-0.598867317271105,
7.15845930159236));
#35734=CARTESIAN_POINT('Ctrl Pts',(-1.65727828481393,-1.20138176331325,
7.19278829530897));
#35735=CARTESIAN_POINT('Ctrl Pts',(-1.17884051406102,-1.56237241050387,
7.22711728902557));
#35736=CARTESIAN_POINT('Ctrl Pts',(-0.662311315437018,-1.95210378436822,
7.2641794289693));
#35737=CARTESIAN_POINT('Ctrl Pts',(0.0666250957372189,-2.06032195545224,
7.30124156891302));
#35738=CARTESIAN_POINT('Ctrl Pts',(0.674100031098693,-1.83746065393738,
7.33830370885674));
#35739=CARTESIAN_POINT('Ctrl Pts',(1.28157496646017,-1.61459935242253,7.37536584880046));
#35740=CARTESIAN_POINT('Ctrl Pts',(1.76758842600887,-1.0606585783088,7.41242798874417));
#35741=CARTESIAN_POINT('Ctrl Pts',(1.9095357026966,-0.429355222190436,7.44949012868789));
#35742=CARTESIAN_POINT('Ctrl Pts',(2.05148297938434,0.201948133927931,7.48655226863161));
#35743=CARTESIAN_POINT('Ctrl Pts',(1.84936407321109,0.910614072050953,7.52361440857534));
#35744=CARTESIAN_POINT('Ctrl Pts',(1.39575382755531,1.37205822017881,7.56067654851907));
#35745=CARTESIAN_POINT('Ctrl Pts',(0.942143581899539,1.83350236830666,7.59773868846279));
#35746=CARTESIAN_POINT('Ctrl Pts',(0.237041996761252,2.04772472643938,7.6348008284065));
#35747=CARTESIAN_POINT('Ctrl Pts',(-0.396599106844383,1.91660680765389,
7.67186296835022));
#35748=CARTESIAN_POINT('Ctrl Pts',(-1.03024021045003,1.78548888886839,7.70892510829394));
#35749=CARTESIAN_POINT('Ctrl Pts',(-1.59242083252301,1.30903069316467,7.74598724823766));
#35750=CARTESIAN_POINT('Ctrl Pts',(-1.82565005336597,0.705460409477194,
7.78304938818139));
#35751=CARTESIAN_POINT('Ctrl Pts',(-1.9118230851659,0.482454556858425,7.79674302807951));
#35752=CARTESIAN_POINT('Ctrl Pts',(-1.95308968355645,0.242096139413284,
7.81043666797764));
#35753=CARTESIAN_POINT('Ctrl Pts',(-1.95166123101285,0.00126544742759004,
7.82413030787576));
#35754=CARTESIAN_POINT('Origin',(0.,0.,0.));
#35755=CARTESIAN_POINT('',(-1.95279013340439,-0.00168009551267251,8.62586969212423));
#35756=CARTESIAN_POINT('',(-1.95215444869335,-0.00150235120299324,8.52413030787576));
#35757=CARTESIAN_POINT('',(-1.954,-2.39295984553393E-16,0.));
#35758=CARTESIAN_POINT('Ctrl Pts',(-1.95279013340439,-0.00168009551267251,
8.62586969212423));
#35759=CARTESIAN_POINT('Ctrl Pts',(-1.94903607268958,0.455640131522026,
8.59982856344197));
#35760=CARTESIAN_POINT('Ctrl Pts',(-1.78871895344458,0.915331173731693,
8.57378743475971));
#35761=CARTESIAN_POINT('Ctrl Pts',(-1.49539281844263,1.26270942713959,8.54774630607745));
#35762=CARTESIAN_POINT('Ctrl Pts',(-1.07820722729247,1.75677110357261,8.51070908924897));
#35763=CARTESIAN_POINT('Ctrl Pts',(-0.391968436807465,2.02364430724413,
8.47367187242049));
#35764=CARTESIAN_POINT('Ctrl Pts',(0.24939826400162,1.94124580780539,8.43663465559201));
#35765=CARTESIAN_POINT('Ctrl Pts',(0.890764964810705,1.85884730836666,8.39959743876353));
#35766=CARTESIAN_POINT('Ctrl Pts',(1.48725957594388,1.42717710581768,8.36256022193505));
#35767=CARTESIAN_POINT('Ctrl Pts',(1.76601098282085,0.843706103134459,8.32552300510657));
#35768=CARTESIAN_POINT('Ctrl Pts',(2.04476238969783,0.260235100451228,8.28848578827809));
#35769=CARTESIAN_POINT('Ctrl Pts',(2.00577059231861,-0.475036702366233,
8.25144857144961));
#35770=CARTESIAN_POINT('Ctrl Pts',(1.66687269277466,-1.02575348200379,8.21441135462113));
#35771=CARTESIAN_POINT('Ctrl Pts',(1.32797479323072,-1.57647026164133,8.17737413779266));
#35772=CARTESIAN_POINT('Ctrl Pts',(0.689170791522051,-1.94263201809897,
8.14033692096418));
#35773=CARTESIAN_POINT('Ctrl Pts',(0.0426865627857745,-1.95673519857469,
8.1032997041357));
#35774=CARTESIAN_POINT('Ctrl Pts',(-0.60379766595052,-1.97083837905041,
8.06626248730722));
#35775=CARTESIAN_POINT('Ctrl Pts',(-1.25796212171444,-1.6328829835442,8.02922527047874));
#35776=CARTESIAN_POINT('Ctrl Pts',(-1.62055416970245,-1.09746934488294,
7.99218805365026));
#35777=CARTESIAN_POINT('Ctrl Pts',(-1.83697171385623,-0.777901098892797,
7.97008193314158));
#35778=CARTESIAN_POINT('Ctrl Pts',(-1.94951814111497,-0.387989405753114,
7.94797581263291));
#35779=CARTESIAN_POINT('Ctrl Pts',(-1.95128545551857,0.000980157954364874,
7.92586969212424));
#35780=CARTESIAN_POINT('Ctrl Pts',(-1.95166123101285,0.00126544742759004,
7.82413030787576));
#35781=CARTESIAN_POINT('Ctrl Pts',(-1.94922354508138,-0.409717467160323,
7.84749880792136));
#35782=CARTESIAN_POINT('Ctrl Pts',(-1.82244856716882,-0.822075748123473,
7.87086730796695));
#35783=CARTESIAN_POINT('Ctrl Pts',(-1.58232634722073,-1.15191832939155,
7.89423580801255));
#35784=CARTESIAN_POINT('Ctrl Pts',(-1.20149560061961,-1.67504441290151,
7.93129794795627));
#35785=CARTESIAN_POINT('Ctrl Pts',(-0.535556287804454,-1.99061420825021,
7.96836008789999));
#35786=CARTESIAN_POINT('Ctrl Pts',(0.110476940437387,-1.95408990384897,
8.00542222784371));
#35787=CARTESIAN_POINT('Ctrl Pts',(0.756510168679237,-1.91756559944773,
8.04248436778743));
#35788=CARTESIAN_POINT('Ctrl Pts',(1.38263731234777,-1.52894719529654,8.07954650773116));
#35789=CARTESIAN_POINT('Ctrl Pts',(1.70207855773424,-0.966230350379699,
8.11660864767487));
#35790=CARTESIAN_POINT('Ctrl Pts',(2.02151980312072,-0.403513505462853,
8.1536707876186));
#35791=CARTESIAN_POINT('Ctrl Pts',(2.03427515022513,0.333301780219651,8.19073292756232));
#35792=CARTESIAN_POINT('Ctrl Pts',(1.73450237337761,0.906738122863988,8.22779506750604));
#35793=CARTESIAN_POINT('Ctrl Pts',(1.43472959653009,1.48017446550833,8.26485720744976));
#35794=CARTESIAN_POINT('Ctrl Pts',(0.822428695730641,1.89023186511451,8.30191934739348));
#35795=CARTESIAN_POINT('Ctrl Pts',(0.178046765554912,1.94909513773745,8.3389814873372));
#35796=CARTESIAN_POINT('Ctrl Pts',(-0.466335164620799,2.00795841036038,
8.37604362728092));
#35797=CARTESIAN_POINT('Ctrl Pts',(-1.14279812417278,1.71562755600011,8.41310576722464));
#35798=CARTESIAN_POINT('Ctrl Pts',(-1.54150740386038,1.20599644714809,8.45016790716836));
#35799=CARTESIAN_POINT('Ctrl Pts',(-1.80673309918174,0.866984359672774,
8.47482204073749));
#35800=CARTESIAN_POINT('Ctrl Pts',(-1.94905131081074,0.431815751432988,
8.49947617430663));
#35801=CARTESIAN_POINT('Ctrl Pts',(-1.95215444869335,-0.00150235120299324,
8.52413030787576));
#35802=CARTESIAN_POINT('Origin',(0.,0.,0.));
#35803=CARTESIAN_POINT('',(-1.95719986784682,3.71606954582295E-5,9.32586969212424));
#35804=CARTESIAN_POINT('',(-1.95707453392556,-0.000466568259871601,9.22413030787576));
#35805=CARTESIAN_POINT('',(-1.954,-2.39295984553393E-16,0.));
#35806=CARTESIAN_POINT('Ctrl Pts',(-1.95719986784682,3.71606954581456E-5,
9.32586969212423));
#35807=CARTESIAN_POINT('Ctrl Pts',(-1.95720042510874,0.00202653151786848,
9.32575574790799));
#35808=CARTESIAN_POINT('Ctrl Pts',(-1.95719765412071,0.00401590074103218,
9.32564180369175));
#35809=CARTESIAN_POINT('Ctrl Pts',(-1.95719155021855,0.00600525973720184,
9.32552785947551));
#35810=CARTESIAN_POINT('Ctrl Pts',(-1.95520749560565,0.65264027922361,9.28849064264703));
#35811=CARTESIAN_POINT('Ctrl Pts',(-1.60108272580438,1.29819476052309,9.25145342581855));
#35812=CARTESIAN_POINT('Ctrl Pts',(-1.0568144211536,1.64735485073218,9.21441620899007));
#35813=CARTESIAN_POINT('Ctrl Pts',(-0.512546116502833,1.99651494094127,
9.17737899216159));
#35814=CARTESIAN_POINT('Ctrl Pts',(0.221865722997436,2.04928064005996,9.14034177533311));
#35815=CARTESIAN_POINT('Ctrl Pts',(0.810458692323854,1.78151382429043,9.10330455850463));
#35816=CARTESIAN_POINT('Ctrl Pts',(1.39905166165026,1.51374700852089,9.06626734167615));
#35817=CARTESIAN_POINT('Ctrl Pts',(1.84182576080283,0.925447677863139,9.02923012484767));
#35818=CARTESIAN_POINT('Ctrl Pts',(1.93623051178265,0.285737974246437,8.99219290801919));
#35819=CARTESIAN_POINT('Ctrl Pts',(2.03063526276248,-0.353971729370283,
8.95515569119071));
#35820=CARTESIAN_POINT('Ctrl Pts',(1.77667066556955,-1.04509180594595,8.91811847436223));
#35821=CARTESIAN_POINT('Ctrl Pts',(1.29051481285208,-1.47146399547075,8.88108125753376));
#35822=CARTESIAN_POINT('Ctrl Pts',(0.804358960134614,-1.89783618499555,
8.84404404070528));
#35823=CARTESIAN_POINT('Ctrl Pts',(0.0860118518926114,-2.05946048746948,
8.8070068238768));
#35824=CARTESIAN_POINT('Ctrl Pts',(-0.535913025040727,-1.88240059832962,
8.76996960704832));
#35825=CARTESIAN_POINT('Ctrl Pts',(-1.15783790197406,-1.70534070918976,
8.73293239021984));
#35826=CARTESIAN_POINT('Ctrl Pts',(-1.68334054759872,-1.18959662843613,
8.69589517339136));
#35827=CARTESIAN_POINT('Ctrl Pts',(-1.87202567450341,-0.571099513462055,
8.65885795656288));
#35828=CARTESIAN_POINT('Ctrl Pts',(-1.92804495632289,-0.387472087407564,
8.64786186841667));
#35829=CARTESIAN_POINT('Ctrl Pts',(-1.95437531748109,-0.194787452297348,
8.63686578027045));
#35830=CARTESIAN_POINT('Ctrl Pts',(-1.95279013340439,-0.00168009551267234,
8.62586969212424));
#35831=CARTESIAN_POINT('Ctrl Pts',(-1.95215444869335,-0.00150235120299324,
8.52413030787576));
#35832=CARTESIAN_POINT('Ctrl Pts',(-1.95371620524508,-0.21958398707372,
8.53653831425035));
#35833=CARTESIAN_POINT('Ctrl Pts',(-1.92001564940553,-0.437196901383431,
8.54894632062494));
#35834=CARTESIAN_POINT('Ctrl Pts',(-1.84897391479539,-0.641847309864828,
8.56135432699953));
#35835=CARTESIAN_POINT('Ctrl Pts',(-1.63677554621959,-1.25312859468192,
8.59841646694325));
#35836=CARTESIAN_POINT('Ctrl Pts',(-1.0914232092448,-1.74875980097234,8.63547860688697));
#35837=CARTESIAN_POINT('Ctrl Pts',(-0.462700104058479,-1.90173108515756,
8.67254074683069));
#35838=CARTESIAN_POINT('Ctrl Pts',(0.166023001127845,-2.05470236934278,
8.70960288677441));
#35839=CARTESIAN_POINT('Ctrl Pts',(0.878116874525705,-1.86501373142281,
8.74666502671813));
#35840=CARTESIAN_POINT('Ctrl Pts',(1.34742707561642,-1.41954668207959,8.78372716666185));
#35841=CARTESIAN_POINT('Ctrl Pts',(1.81673727670714,-0.974079632736377,
8.82078930660557));
#35842=CARTESIAN_POINT('Ctrl Pts',(2.04326380549072,-0.272834171969915,
8.85785144654929));
#35843=CARTESIAN_POINT('Ctrl Pts',(1.92325259761237,0.363004067433246,8.89491358649301));
#35844=CARTESIAN_POINT('Ctrl Pts',(1.80324138973402,0.998842306836407,8.93197572643673));
#35845=CARTESIAN_POINT('Ctrl Pts',(1.33669244519374,1.56927332487627,8.96903786638045));
#35846=CARTESIAN_POINT('Ctrl Pts',(0.737295301650971,1.81302734225987,9.00610000632417));
#35847=CARTESIAN_POINT('Ctrl Pts',(0.137898158108199,2.05678135964346,9.0431621462679));
#35848=CARTESIAN_POINT('Ctrl Pts',(-0.59434718443707,1.9738583763708,9.08022428621162));
#35849=CARTESIAN_POINT('Ctrl Pts',(-1.12405647662483,1.60223891616111,9.11728642615534));
#35850=CARTESIAN_POINT('Ctrl Pts',(-1.63307724594775,1.24513356361944,9.15290105339548));
#35851=CARTESIAN_POINT('Ctrl Pts',(-1.95507366281261,0.621442230158499,
9.18851568063562));
#35852=CARTESIAN_POINT('Ctrl Pts',(-1.95707453392556,-0.000466568259871601,
9.22413030787576));
#35853=CARTESIAN_POINT('Origin',(0.,0.,0.));
#35854=CARTESIAN_POINT('',(-1.95268202714777,0.00165579016441021,10.0258696921242));
#35855=CARTESIAN_POINT('',(-1.9535343393295,0.00178280253715055,9.92413030787576));
#35856=CARTESIAN_POINT('',(-1.954,-2.39295984553393E-16,0.));
#35857=CARTESIAN_POINT('Ctrl Pts',(-1.95268202714777,0.00165579016441021,
10.0258696921242));
#35858=CARTESIAN_POINT('Ctrl Pts',(-1.9542709496717,0.198793394721131,10.0146457155455));
#35859=CARTESIAN_POINT('Ctrl Pts',(-1.92681564478375,0.395498739780043,
10.0034217389668));
#35860=CARTESIAN_POINT('Ctrl Pts',(-1.86848643290836,0.582577638715851,
9.99219776238813));
#35861=CARTESIAN_POINT('Ctrl Pts',(-1.67600993827966,1.1999062383733,9.95516054555966));
#35862=CARTESIAN_POINT('Ctrl Pts',(-1.14735119634562,1.71241362792136,9.91812332873117));
#35863=CARTESIAN_POINT('Ctrl Pts',(-0.524351231736321,1.8856531990772,9.88108611190269));
#35864=CARTESIAN_POINT('Ctrl Pts',(0.0986487328729629,2.05889277023303,
9.84404889507421));
#35865=CARTESIAN_POINT('Ctrl Pts',(0.815989920157508,1.89286452299667,9.80701167824573));
#35866=CARTESIAN_POINT('Ctrl Pts',(1.29952003507049,1.46351732792493,9.76997446141725));
#35867=CARTESIAN_POINT('Ctrl Pts',(1.78305014998348,1.03417013285319,9.73293724458878));
#35868=CARTESIAN_POINT('Ctrl Pts',(2.0327691925249,0.341503989946047,9.69590002776029));
#35869=CARTESIAN_POINT('Ctrl Pts',(1.9344406978275,-0.297614493697593,9.65886281093182));
#35870=CARTESIAN_POINT('Ctrl Pts',(1.8361122031301,-0.936732977341234,9.62182559410334));
#35871=CARTESIAN_POINT('Ctrl Pts',(1.38973617119388,-1.52230380172138,9.58478837727486));
#35872=CARTESIAN_POINT('Ctrl Pts',(0.799511084736072,-1.78645358874384,
9.54775116044638));
#35873=CARTESIAN_POINT('Ctrl Pts',(0.209285998278261,-2.0506033757663,9.5107139436179));
#35874=CARTESIAN_POINT('Ctrl Pts',(-0.524788142701144,-1.99333212543108,
9.47367672678942));
#35875=CARTESIAN_POINT('Ctrl Pts',(-1.06690354347858,-1.6408387214268,9.43663950996094));
#35876=CARTESIAN_POINT('Ctrl Pts',(-1.60735113766186,-1.28942975594381,
9.3997162373487));
#35877=CARTESIAN_POINT('Ctrl Pts',(-1.95701928883641,-0.644612332051665,
9.36279296473647));
#35878=CARTESIAN_POINT('Ctrl Pts',(-1.95719986784682,3.71606954582295E-5,
9.32586969212424));
#35879=CARTESIAN_POINT('Ctrl Pts',(-1.95707453392556,-0.000466568259871601,
9.22413030787576));
#35880=CARTESIAN_POINT('Ctrl Pts',(-1.95715585687005,-0.0257432861687418,
9.22557782057934));
#35881=CARTESIAN_POINT('Ctrl Pts',(-1.95670857405052,-0.0510170594794435,
9.22702533328292));
#35882=CARTESIAN_POINT('Ctrl Pts',(-1.95572375776859,-0.0762698699047084,
9.2284728459865));
#35883=CARTESIAN_POINT('Ctrl Pts',(-1.93050850489432,-0.722843258614067,
9.26553498593022));
#35884=CARTESIAN_POINT('Ctrl Pts',(-1.55290475731554,-1.35567409888606,
9.30259712587394));
#35885=CARTESIAN_POINT('Ctrl Pts',(-0.995863227266852,-1.68491214354887,
9.33965926581766));
#35886=CARTESIAN_POINT('Ctrl Pts',(-0.438821697218168,-2.01415018821168,
9.37672140576139));
#35887=CARTESIAN_POINT('Ctrl Pts',(0.297657615300397,-2.03979543726533,
9.4137835457051));
#35888=CARTESIAN_POINT('Ctrl Pts',(0.876251218790847,-1.75010180082627,
9.45084568564882));
#35889=CARTESIAN_POINT('Ctrl Pts',(1.45484482228131,-1.46040816438721,9.48790782559255));
#35890=CARTESIAN_POINT('Ctrl Pts',(1.87555271674363,-0.855375642455424,
9.52496996553627));
#35891=CARTESIAN_POINT('Ctrl Pts',(1.94568154283725,-0.21212227253196,9.56203210547999));
#35892=CARTESIAN_POINT('Ctrl Pts',(2.01581036893087,0.431131097391505,9.59909424542371));
#35893=CARTESIAN_POINT('Ctrl Pts',(1.73536012665579,1.11260531530666,9.63615638536743));
#35894=CARTESIAN_POINT('Ctrl Pts',(1.23278314419194,1.52017044141902,9.67321852531115));
#35895=CARTESIAN_POINT('Ctrl Pts',(0.730206161728088,1.92773556753138,9.71028066525487));
#35896=CARTESIAN_POINT('Ctrl Pts',(0.00550243907548716,2.06139160184095,
9.74734280519859));
#35897=CARTESIAN_POINT('Ctrl Pts',(-0.609398062732146,1.85992111567971,
9.78440494514231));
#35898=CARTESIAN_POINT('Ctrl Pts',(-1.22429856453979,1.65845062951848,9.82146708508603));
#35899=CARTESIAN_POINT('Ctrl Pts',(-1.72939584550245,1.12185362288641,9.85852922502976));
#35900=CARTESIAN_POINT('Ctrl Pts',(-1.89334427223443,0.495903289718102,
9.89559136497348));
#35901=CARTESIAN_POINT('Ctrl Pts',(-1.93542598326109,0.335236538822793,
9.90510434594091));
#35902=CARTESIAN_POINT('Ctrl Pts',(-1.95503184094814,0.168682937546108,
9.91461732690834));
#35903=CARTESIAN_POINT('Ctrl Pts',(-1.9535343393295,0.00178280253715055,
9.92413030787576));
#35904=CARTESIAN_POINT('Origin',(0.,0.,0.));
#35905=CARTESIAN_POINT('',(-1.95129684289216,-0.00113636086278679,10.7258696921242));
#35906=CARTESIAN_POINT('',(-1.95093054978418,-0.000550606481354719,10.6241303078758));
#35907=CARTESIAN_POINT('',(-1.954,-2.39295984553393E-16,0.));
#35908=CARTESIAN_POINT('Ctrl Pts',(-1.95129684289216,-0.00113636086278679,
10.7258696921242));
#35909=CARTESIAN_POINT('Ctrl Pts',(-1.94942963316978,0.391854106201406,
10.7035356831831));
#35910=CARTESIAN_POINT('Ctrl Pts',(-1.83442754086643,0.785903964976412,
10.6812016742419));
#35911=CARTESIAN_POINT('Ctrl Pts',(-1.61381630858742,1.10744756631717,10.6588676653008));
#35912=CARTESIAN_POINT('Ctrl Pts',(-1.24796949325566,1.64067382739912,10.6218304484723));
#35913=CARTESIAN_POINT('Ctrl Pts',(-0.591690439027595,1.97450300329055,
10.5847932316438));
#35914=CARTESIAN_POINT('Ctrl Pts',(0.0547076636758263,1.95640786233593,
10.5477560148153));
#35915=CARTESIAN_POINT('Ctrl Pts',(0.701105766379276,1.9383127213813,10.5107187979868));
#35916=CARTESIAN_POINT('Ctrl Pts',(1.33762291755807,1.56829326358058,10.4736815811584));
#35917=CARTESIAN_POINT('Ctrl Pts',(1.67312833478204,1.01552035674769,10.4366443643299));
#35918=CARTESIAN_POINT('Ctrl Pts',(2.00863375200599,0.462747449914819,10.3996071475014));
#35919=CARTESIAN_POINT('Ctrl Pts',(2.04312743527515,-0.272778905950186,
10.3625699306729));
#35920=CARTESIAN_POINT('Ctrl Pts',(1.7608042651717,-0.854535269464722,10.3255327138444));
#35921=CARTESIAN_POINT('Ctrl Pts',(1.47848109506825,-1.43629163297926,10.288495497016));
#35922=CARTESIAN_POINT('Ctrl Pts',(0.879341071592168,-1.86427800414334,
10.2514582801875));
#35923=CARTESIAN_POINT('Ctrl Pts',(0.237478981470821,-1.94273555725334,
10.214421063359));
#35924=CARTESIAN_POINT('Ctrl Pts',(-0.404383108650536,-2.02119311036335,
10.1773838465305));
#35925=CARTESIAN_POINT('Ctrl Pts',(-1.08896726541717,-1.75012184541928,
10.140346629702));
#35926=CARTESIAN_POINT('Ctrl Pts',(-1.5031122201388,-1.25351130806383,10.1033094128736));
#35927=CARTESIAN_POINT('Ctrl Pts',(-1.7917522457641,-0.907396556226723,
10.0774961726238));
#35928=CARTESIAN_POINT('Ctrl Pts',(-1.94902777514884,-0.451727225472274,
10.051682932374));
#35929=CARTESIAN_POINT('Ctrl Pts',(-1.95268202714777,0.00165579016441021,
10.0258696921242));
#35930=CARTESIAN_POINT('Ctrl Pts',(-1.9535343393295,0.00178280253715055,
9.92413030787576));
#35931=CARTESIAN_POINT('Ctrl Pts',(-1.94919764294582,-0.481552375812319,
9.95167946685205));
#35932=CARTESIAN_POINT('Ctrl Pts',(-1.76787653021499,-0.967793777264111,
9.97922862582834));
#35933=CARTESIAN_POINT('Ctrl Pts',(-1.44290486192301,-1.32238333502052,
10.0067777848046));
#35934=CARTESIAN_POINT('Ctrl Pts',(-1.00571745237828,-1.79941596688631,
10.0438399247484));
#35935=CARTESIAN_POINT('Ctrl Pts',(-0.308543060787511,-2.03817757091334,
10.0809020646921));
#35936=CARTESIAN_POINT('Ctrl Pts',(0.329297761185238,-1.92930969998698,
10.1179642046358));
#35937=CARTESIAN_POINT('Ctrl Pts',(0.967138583157977,-1.82044182906063,
10.1550263445795));
#35938=CARTESIAN_POINT('Ctrl Pts',(1.5456458355127,-1.36394448318089,10.1920884845232));
#35939=CARTESIAN_POINT('Ctrl Pts',(1.79984980484802,-0.76890421197536,10.229150624467));
#35940=CARTESIAN_POINT('Ctrl Pts',(2.05405377418334,-0.173863940769825,
10.2662127644107));
#35941=CARTESIAN_POINT('Ctrl Pts',(1.98395446049928,0.5597192557615,10.3032749043544));
#35942=CARTESIAN_POINT('Ctrl Pts',(1.62166047466929,1.09585000349956,10.3403370442981));
#35943=CARTESIAN_POINT('Ctrl Pts',(1.2593664888393,1.63198075123761,10.3773991842419));
#35944=CARTESIAN_POINT('Ctrl Pts',(0.604877830863377,1.9706590501824,10.4144613241856));
#35945=CARTESIAN_POINT('Ctrl Pts',(-0.042038551539475,1.95675976549601,
10.4515234641293));
#35946=CARTESIAN_POINT('Ctrl Pts',(-0.688954933942345,1.94286048080962,
10.488585604073));
#35947=CARTESIAN_POINT('Ctrl Pts',(-1.32829904077215,1.57638361249205,10.5256477440167));
#35948=CARTESIAN_POINT('Ctrl Pts',(-1.66723158702796,1.02518946943711,10.5627098839605));
#35949=CARTESIAN_POINT('Ctrl Pts',(-1.85446111291195,0.720704641366568,
10.5831833585989));
#35950=CARTESIAN_POINT('Ctrl Pts',(-1.95001820365716,0.359852200961074,
10.6036568332373));
#35951=CARTESIAN_POINT('Ctrl Pts',(-1.95093054978418,-0.000550606481354719,
10.6241303078758));
#35952=CARTESIAN_POINT('Origin',(0.,0.,-1.29405622560369));
#35953=CARTESIAN_POINT('',(-1.55334812646815,-0.000904610707407963,10.9559437743963));
#35954=CARTESIAN_POINT('',(-1.55659711405804,-0.00105088068675666,11.0940562256037));
#35955=CARTESIAN_POINT('',(-1.5555,-2.01987159101623E-13,-1.29405622560369));
#35956=CARTESIAN_POINT('',(0.499806597877791,1.47301514408978,11.4445));
#35957=CARTESIAN_POINT('Ctrl Pts',(-1.55334812646815,-0.000904610707408108,
10.9559437743963));
#35958=CARTESIAN_POINT('Ctrl Pts',(-1.55432667860164,-0.206859868644216,
10.9706469822836));
#35959=CARTESIAN_POINT('Ctrl Pts',(-1.42041322258558,-0.930327919713715,
11.0223874069994));
#35960=CARTESIAN_POINT('Ctrl Pts',(-0.324962964057439,-1.80887727526569,
11.1111650485437));
#35961=CARTESIAN_POINT('Ctrl Pts',(1.34445241673909,-1.25560970886474,11.2222766990291));
#35962=CARTESIAN_POINT('Ctrl Pts',(1.78171768593789,0.450698535437549,11.3333883495146));
#35963=CARTESIAN_POINT('Ctrl Pts',(0.989503531151977,1.30685679928735,11.4074627831715));
#35964=CARTESIAN_POINT('Ctrl Pts',(0.499806597877626,1.47301514408983,11.4445));
#35965=CARTESIAN_POINT('',(1.55548765964692,0.00619602180124784,11.4445));
#35966=CARTESIAN_POINT('Origin',(0.,0.,11.4445));
#35967=CARTESIAN_POINT('Ctrl Pts',(-1.55659711405804,-0.0010508806867568,
11.0940562256037));
#35968=CARTESIAN_POINT('Ctrl Pts',(-1.55726922058417,-0.079449137192624,
11.099684397238));
#35969=CARTESIAN_POINT('Ctrl Pts',(-1.51630179095532,-0.673453815214831,
11.142374708816));
#35970=CARTESIAN_POINT('Ctrl Pts',(-0.75277483453787,-1.67898453189698,
11.2221271603377));
#35971=CARTESIAN_POINT('Ctrl Pts',(1.00462758039806,-1.53944373403644,11.3333135801688));
#35972=CARTESIAN_POINT('Ctrl Pts',(1.55754888396286,-0.511266487217653,
11.4074378600563));
#35973=CARTESIAN_POINT('Ctrl Pts',(1.55548765964692,0.00619602180124784,
11.4445));
#35974=CARTESIAN_POINT('Origin',(0.,0.,-1.29405622560369));
#35975=CARTESIAN_POINT('',(-1.55445081536763,0.00131810726739325,10.2559437743963));
#35976=CARTESIAN_POINT('',(-1.55305653540906,-0.000438315446397164,10.3940562256037));
#35977=CARTESIAN_POINT('',(-1.5555,-2.01987159101623E-13,-1.29405622560369));
#35978=CARTESIAN_POINT('Ctrl Pts',(-1.55445081536763,0.00131810726739319,
10.2559437743963));
#35979=CARTESIAN_POINT('Ctrl Pts',(-1.55154181384031,-0.359601688445403,
10.2817570146461));
#35980=CARTESIAN_POINT('Ctrl Pts',(-1.24670140973274,-1.24280598265434,
10.3446074717243));
#35981=CARTESIAN_POINT('Ctrl Pts',(0.223056668548975,-1.82477852394609,
10.4444951456311));
#35982=CARTESIAN_POINT('Ctrl Pts',(1.65390974917898,-0.802670846854376,
10.5556067961165));
#35983=CARTESIAN_POINT('Ctrl Pts',(1.57153269033781,0.953897085409752,10.6667184466019));
#35984=CARTESIAN_POINT('Ctrl Pts',(0.0514163720288116,1.83756944970195,
10.7778300970874));
#35985=CARTESIAN_POINT('Ctrl Pts',(-1.30849536725084,1.14582374749785,10.8742385396855));
#35986=CARTESIAN_POINT('Ctrl Pts',(-1.55186171668149,0.311939131113674,
10.9336097654551));
#35987=CARTESIAN_POINT('Ctrl Pts',(-1.55334812646815,-0.000904610707408108,
10.9559437743963));
#35988=CARTESIAN_POINT('Ctrl Pts',(-1.55305653540906,-0.000438315446397077,
10.3940562256037));
#35989=CARTESIAN_POINT('Ctrl Pts',(-1.55364500629154,-0.232901140548306,
10.410644890909));
#35990=CARTESIAN_POINT('Ctrl Pts',(-1.39557528484751,-0.983968830408974,
10.464295696158));
#35991=CARTESIAN_POINT('Ctrl Pts',(-0.231259578302998,-1.82421227428175,
10.5550086413507));
#35992=CARTESIAN_POINT('Ctrl Pts',(1.40774638007895,-1.1829694620695,10.6661950611819));
#35993=CARTESIAN_POINT('Ctrl Pts',(1.75706993010233,0.541796064983141,10.7773814810131));
#35994=CARTESIAN_POINT('Ctrl Pts',(0.497080432048737,1.77049779856472,10.8885679008442));
#35995=CARTESIAN_POINT('Ctrl Pts',(-1.13185991314487,1.39680492671116,10.9941261490411));
#35996=CARTESIAN_POINT('Ctrl Pts',(-1.55284332390808,0.436812153822664,
11.0626222572943));
#35997=CARTESIAN_POINT('Ctrl Pts',(-1.55659711405804,-0.0010508806867568,
11.0940562256037));
#35998=CARTESIAN_POINT('Origin',(0.,0.,-1.29405622560369));
#35999=CARTESIAN_POINT('',(-1.55804728476752,2.95821195149996E-5,9.5559437743963));
#36000=CARTESIAN_POINT('',(-1.55512930646214,0.00141921665610299,9.69405622560371));
#36001=CARTESIAN_POINT('',(-1.5555,-2.01987159101623E-13,-1.29405622560369));
#36002=CARTESIAN_POINT('Ctrl Pts',(-1.55804728476752,2.95821195150548E-5,
9.5559437743963));
#36003=CARTESIAN_POINT('Ctrl Pts',(-1.55790353315504,-0.513149683984934,
9.59286704700854));
#36004=CARTESIAN_POINT('Ctrl Pts',(-1.00033131917675,-1.54135965233235,
9.66682753644926));
#36005=CARTESIAN_POINT('Ctrl Pts',(0.750970673805211,-1.67799333720618,
9.77782524271844));
#36006=CARTESIAN_POINT('Ctrl Pts',(1.81699613594968,-0.279545920640164,
9.88893689320389));
#36007=CARTESIAN_POINT('Ctrl Pts',(1.22062258834496,1.37466418983892,10.0000485436893));
#36008=CARTESIAN_POINT('Ctrl Pts',(-0.492515922639386,1.77116921324136,
10.1111601941748));
#36009=CARTESIAN_POINT('Ctrl Pts',(-1.46173837715872,0.831558022400444,
10.1964586044104));
#36010=CARTESIAN_POINT('Ctrl Pts',(-1.55571569202373,0.15825134364817,10.2447197978176));
#36011=CARTESIAN_POINT('Ctrl Pts',(-1.55445081536763,0.00131810726739319,
10.2559437743963));
#36012=CARTESIAN_POINT('Ctrl Pts',(-1.55512930646214,0.00141921665610296,
9.69405622560371));
#36013=CARTESIAN_POINT('Ctrl Pts',(-1.55167703869094,-0.383344278698275,
9.72160538457999));
#36014=CARTESIAN_POINT('Ctrl Pts',(-1.21314953523015,-1.29115961930375,
9.7862166835));
#36015=CARTESIAN_POINT('Ctrl Pts',(0.309373610575528,-1.81257875466721,
9.88789012236375));
#36016=CARTESIAN_POINT('Ctrl Pts',(1.69095195914933,-0.722381792257861,
9.99907654219489));
#36017=CARTESIAN_POINT('Ctrl Pts',(1.52354231364944,1.0295455294481,10.1102629620261));
#36018=CARTESIAN_POINT('Ctrl Pts',(-0.0394931635484403,1.83836962465064,
10.2214493818572));
#36019=CARTESIAN_POINT('Ctrl Pts',(-1.33855689695156,1.09373648628768,10.3160471363831));
#36020=CARTESIAN_POINT('Ctrl Pts',(-1.5523302537302,0.286463714736223,10.3735827509653));
#36021=CARTESIAN_POINT('Ctrl Pts',(-1.55305653540906,-0.000438315446397077,
10.3940562256037));
#36022=CARTESIAN_POINT('Origin',(0.,0.,-1.29405622560369));
#36023=CARTESIAN_POINT('',(-1.55453687436568,-0.00133745576774406,8.85594377439631));
#36024=CARTESIAN_POINT('',(-1.55794751152569,-0.000371416033132788,8.99405622560372));
#36025=CARTESIAN_POINT('',(-1.5555,-2.01987159101623E-13,-1.29405622560369));
#36026=CARTESIAN_POINT('Ctrl Pts',(-1.55453687436568,-0.00133745576774402,
8.85594377439631));
#36027=CARTESIAN_POINT('Ctrl Pts',(-1.55579877499581,-0.155062375664632,
8.86693986254252));
#36028=CARTESIAN_POINT('Ctrl Pts',(-1.46423861786649,-0.825096309536398,
8.91497316751722));
#36029=CARTESIAN_POINT('Ctrl Pts',(-0.503376402892206,-1.7681153483915,
9.00004368932038));
#36030=CARTESIAN_POINT('Ctrl Pts',(1.2121644264892,-1.38212772940753,9.11115533980582));
#36031=CARTESIAN_POINT('Ctrl Pts',(1.81867711471885,0.26839009932345,9.22226699029127));
#36032=CARTESIAN_POINT('Ctrl Pts',(0.761253709552246,1.67335367481701,9.33337864077668));
#36033=CARTESIAN_POINT('Ctrl Pts',(-0.99265255914171,1.54733978795034,9.44449029126215));
#36034=CARTESIAN_POINT('Ctrl Pts',(-1.55732851093913,0.517959404958592,
9.51867866913534));
#36035=CARTESIAN_POINT('Ctrl Pts',(-1.55804772838109,0.00161323939398619,
9.55582983018006));
#36036=CARTESIAN_POINT('Ctrl Pts',(-1.55804728476752,2.95821195150548E-5,
9.5559437743963));
#36037=CARTESIAN_POINT('Ctrl Pts',(-1.55794751152569,-0.000371416033132616,
8.99405622560372));
#36038=CARTESIAN_POINT('Ctrl Pts',(-1.55801224941728,-0.020493184051098,
8.99550373830729));
#36039=CARTESIAN_POINT('Ctrl Pts',(-1.54853952527048,-0.55575068168544,
9.03401339095459));
#36040=CARTESIAN_POINT('Ctrl Pts',(-0.935609375970031,-1.5829679799695,
9.1095851835456));
#36041=CARTESIAN_POINT('Ctrl Pts',(0.823234386500799,-1.64421340203127,
9.22077160337675));
#36042=CARTESIAN_POINT('Ctrl Pts',(1.82795976495949,-0.199287985657338,
9.33195802320793));
#36043=CARTESIAN_POINT('Ctrl Pts',(1.15819463928053,1.42819381470141,9.44314444303908));
#36044=CARTESIAN_POINT('Ctrl Pts',(-0.572526917402423,1.74738822826618,
9.55433086287024));
#36045=CARTESIAN_POINT('Ctrl Pts',(-1.47990815776177,0.783419353749631,
9.63796812372513));
#36046=CARTESIAN_POINT('Ctrl Pts',(-1.5563214066504,0.1342816322173,9.68454324463628));
#36047=CARTESIAN_POINT('Ctrl Pts',(-1.55512930646214,0.00141921665610296,
9.69405622560371));
#36048=CARTESIAN_POINT('Origin',(0.,0.,-1.29405622560369));
#36049=CARTESIAN_POINT('',(-1.55333906144275,0.000780263919018194,8.15594377439631));
#36050=CARTESIAN_POINT('',(-1.55403083159801,-0.00119596074553197,8.29405622560371));
#36051=CARTESIAN_POINT('',(-1.5555,-2.01987159101623E-13,-1.29405622560369));
#36052=CARTESIAN_POINT('Ctrl Pts',(-1.55333906144275,0.000780263919018167,
8.15594377439631));
#36053=CARTESIAN_POINT('Ctrl Pts',(-1.55193217426013,-0.308862600127516,
8.17804989490498));
#36054=CARTESIAN_POINT('Ctrl Pts',(-1.3122308335565,-1.13929638534857,8.23719323224213));
#36055=CARTESIAN_POINT('Ctrl Pts',(0.0400949547363229,-1.83793690702293,
8.33337378640777));
#36056=CARTESIAN_POINT('Ctrl Pts',(1.56567267939011,-0.963477420579929,
8.44448543689319));
#36057=CARTESIAN_POINT('Ctrl Pts',(1.65879203582308,0.792482593671729,8.55559708737864));
#36058=CARTESIAN_POINT('Ctrl Pts',(0.234256671005791,1.82338791618694,8.66670873786407));
#36059=CARTESIAN_POINT('Ctrl Pts',(-1.24241507899534,1.24912116508194,8.7668243002033));
#36060=CARTESIAN_POINT('Ctrl Pts',(-1.55154841917538,0.362716593952071,
8.82990264571404));
#36061=CARTESIAN_POINT('Ctrl Pts',(-1.55453687436568,-0.00133745576774402,
8.85594377439631));
#36062=CARTESIAN_POINT('Ctrl Pts',(-1.55403083159801,-0.00119596074553188,
8.29405622560371));
#36063=CARTESIAN_POINT('Ctrl Pts',(-1.55527408252746,-0.17480188940304,
8.30646423197829));
#36064=CARTESIAN_POINT('Ctrl Pts',(-1.4483135129372,-0.865473027753662,
8.3559343782966));
#36065=CARTESIAN_POINT('Ctrl Pts',(-0.434704832044991,-1.78666848096071,
8.44246666455862));
#36066=CARTESIAN_POINT('Ctrl Pts',(1.26590215885116,-1.33365823077974,8.55365308438979));
#36067=CARTESIAN_POINT('Ctrl Pts',(1.8068878531032,0.341040818691465,8.66483950422094));
#36068=CARTESIAN_POINT('Ctrl Pts',(0.69268588294083,1.70333168137465,8.77602592405212));
#36069=CARTESIAN_POINT('Ctrl Pts',(-1.03328002592178,1.50787500329959,8.88576483117969));
#36070=CARTESIAN_POINT('Ctrl Pts',(-1.55635469933735,0.494704907375218,
8.95844159836357));
#36071=CARTESIAN_POINT('Ctrl Pts',(-1.55794751152569,-0.000371416033132616,
8.99405622560372));
#36072=CARTESIAN_POINT('Origin',(0.,0.,-1.29405622560369));
#36073=CARTESIAN_POINT('',(-1.55738164088485,0.00090367155389158,7.45594377439631));
#36074=CARTESIAN_POINT('',(-1.55363820104426,0.00100737127591941,7.59405622560371));
#36075=CARTESIAN_POINT('',(-1.5555,-2.01987159101623E-13,-1.29405622560369));
#36076=CARTESIAN_POINT('Ctrl Pts',(-1.55738164088485,0.000903671553891608,
7.45594377439631));
#36077=CARTESIAN_POINT('Ctrl Pts',(-1.55418612064456,-0.461276292775272,
7.48915992726744));
#36078=CARTESIAN_POINT('Ctrl Pts',(-1.09121796390773,-1.44436334125619,
7.55941329696705));
#36079=CARTESIAN_POINT('Ctrl Pts',(0.580004387659595,-1.74448118065669,
7.66670388349515));
#36080=CARTESIAN_POINT('Ctrl Pts',(1.7800908511122,-0.459234407622611,7.77781553398057));
#36081=CARTESIAN_POINT('Ctrl Pts',(1.35154441460109,1.24617309179735,7.88892718446602));
#36082=CARTESIAN_POINT('Ctrl Pts',(-0.313551099181417,1.81143738163968,
8.00003883495145));
#36083=CARTESIAN_POINT('Ctrl Pts',(-1.41757073229054,0.936656796997624,
8.08904436492822));
#36084=CARTESIAN_POINT('Ctrl Pts',(-1.55428931266511,0.209921774117757,
8.1410126780765));
#36085=CARTESIAN_POINT('Ctrl Pts',(-1.55333906144275,0.000780263919018167,
8.15594377439631));
#36086=CARTESIAN_POINT('Ctrl Pts',(-1.55363820104426,0.00100737127591942,
7.59405622560371));
#36087=CARTESIAN_POINT('Ctrl Pts',(-1.55169765832855,-0.326159426902871,
7.6174247256493));
#36088=CARTESIAN_POINT('Ctrl Pts',(-1.29071878250434,-1.17503987929593,
7.67785536563862));
#36089=CARTESIAN_POINT('Ctrl Pts',(0.103792628149562,-1.8358593744105,7.77534814557165));
#36090=CARTESIAN_POINT('Ctrl Pts',(1.59909575810308,-0.907769413831382,
7.8865345654028));
#36091=CARTESIAN_POINT('Ctrl Pts',(1.62955779866738,0.851876712390422,7.99772098523398));
#36092=CARTESIAN_POINT('Ctrl Pts',(0.167274199086701,1.83116681231986,8.10890740506512));
#36093=CARTESIAN_POINT('Ctrl Pts',(-1.26795424285233,1.21093838634352,8.20768581852172));
#36094=CARTESIAN_POINT('Ctrl Pts',(-1.55156054962447,0.343750973057136,
8.26940209203457));
#36095=CARTESIAN_POINT('Ctrl Pts',(-1.55403083159801,-0.00119596074553188,
8.29405622560371));
#36096=CARTESIAN_POINT('Origin',(0.,0.,-1.29405622560369));
#36097=CARTESIAN_POINT('',(-1.55606466149984,-0.00136591087330588,6.7559437743963));
#36098=CARTESIAN_POINT('',(-1.55769406638298,0.000677585252333857,6.89405622560371));
#36099=CARTESIAN_POINT('',(-1.5555,-2.01987159101623E-13,-1.29405622560369));
#36100=CARTESIAN_POINT('Ctrl Pts',(-1.55606466149984,-0.00136591087330577,
6.7559437743963));
#36101=CARTESIAN_POINT('Ctrl Pts',(-1.55699698050756,-0.10301028373747,
6.76323274280142));
#36102=CARTESIAN_POINT('Ctrl Pts',(-1.50160999329305,-0.720125819190329,
6.80755892803501));
#36103=CARTESIAN_POINT('Ctrl Pts',(-0.677079673289082,-1.70914680334463,
6.8889223300971));
#36104=CARTESIAN_POINT('Ctrl Pts',(1.06838781720774,-1.49605051766532,7.00003398058251));
#36105=CARTESIAN_POINT('Ctrl Pts',(1.83637062036826,0.0858057341481814,
7.11114563106797));
#36106=CARTESIAN_POINT('Ctrl Pts',(0.924229284360448,1.589156980696,7.22225728155339));
#36107=CARTESIAN_POINT('Ctrl Pts',(-0.833503847528551,1.63856370505402,
7.33336893203883));
#36108=CARTESIAN_POINT('Ctrl Pts',(-1.53115801604342,0.622214122864029,
7.41126442965314));
#36109=CARTESIAN_POINT('Ctrl Pts',(-1.55774924177056,0.0540711533618156,
7.45212271043896));
#36110=CARTESIAN_POINT('Ctrl Pts',(-1.55738164088485,0.000903671553891608,
7.45594377439631));
#36111=CARTESIAN_POINT('Ctrl Pts',(-1.55769406638298,0.000677585252333878,
6.89405622560371));
#36112=CARTESIAN_POINT('Ctrl Pts',(-1.55508734647919,-0.476733936548398,
6.92838521932031));
#36113=CARTESIAN_POINT('Ctrl Pts',(-1.06472330039144,-1.47419539900055,
6.99977635298063));
#36114=CARTESIAN_POINT('Ctrl Pts',(0.633314188332071,-1.72628667698419,
7.10822962658467));
#36115=CARTESIAN_POINT('Ctrl Pts',(1.7940008868909,-0.403377453646542,7.21941604641583));
#36116=CARTESIAN_POINT('Ctrl Pts',(1.31130494233742,1.28904301731096,7.33060246624699));
#36117=CARTESIAN_POINT('Ctrl Pts',(-0.372603218894873,1.80064416072257,
7.44178888607816));
#36118=CARTESIAN_POINT('Ctrl Pts',(-1.43301362666466,0.901927254173143,
7.52960680586373));
#36119=CARTESIAN_POINT('Ctrl Pts',(-1.55477533406966,0.192722899107996,
7.58036258570558));
#36120=CARTESIAN_POINT('Ctrl Pts',(-1.55363820104426,0.00100737127591942,
7.59405622560371));
#36121=CARTESIAN_POINT('Origin',(0.,0.,-1.29405622560369));
#36122=CARTESIAN_POINT('',(-1.55295085115974,-2.74912889200857E-5,6.0559437743963));
#36123=CARTESIAN_POINT('',(-1.55567057787938,-0.00141549514015751,6.19405622560371));
#36124=CARTESIAN_POINT('',(-1.5555,-2.01987159101623E-13,-1.29405622560369));
#36125=CARTESIAN_POINT('Ctrl Pts',(-1.55295114066544,-2.74881667468134E-5,
6.0559437743963));
#36126=CARTESIAN_POINT('Ctrl Pts',(-1.55299180574127,-0.257905198155464,
6.07434277516388));
#36127=CARTESIAN_POINT('Ctrl Pts',(-1.37005956536857,-1.03483686203599,
6.12977899275993));
#36128=CARTESIAN_POINT('Ctrl Pts',(-0.143272298638598,-1.83278278249422,
6.22225242718446));
#36129=CARTESIAN_POINT('Ctrl Pts',(1.46185859526926,-1.11471481859797,6.33336407766989));
#36130=CARTESIAN_POINT('Ctrl Pts',(1.72951224644592,0.623223129190563,6.44447572815534));
#36131=CARTESIAN_POINT('Ctrl Pts',(0.414808152398764,1.79096450999678,6.55558737864077));
#36132=CARTESIAN_POINT('Ctrl Pts',(-1.1682689842466,1.35101180160119,6.6594100607211));
#36133=CARTESIAN_POINT('Ctrl Pts',(-1.55225961585962,0.413472223515983,
6.72619552597294));
#36134=CARTESIAN_POINT('Ctrl Pts',(-1.55606466149984,-0.00136591087330577,
6.7559437743963));
#36135=CARTESIAN_POINT('Ctrl Pts',(-1.55567057787938,-0.00141549514015748,
6.19405622560371));
#36136=CARTESIAN_POINT('Ctrl Pts',(-1.55673152840384,-0.11622012238534,
6.2022835730476));
#36137=CARTESIAN_POINT('Ctrl Pts',(-1.49271086742403,-0.747018195902368,
6.2475730604352));
#36138=CARTESIAN_POINT('Ctrl Pts',(-0.632665469493242,-1.72652453095426,
6.32992468776653));
#36139=CARTESIAN_POINT('Ctrl Pts',(1.10806726459172,-1.46742614445027,6.44111110759769));
#36140=CARTESIAN_POINT('Ctrl Pts',(1.83376231205259,0.135898253011021,6.55229752742886));
#36141=CARTESIAN_POINT('Ctrl Pts',(0.879651525947856,1.61473395492061,6.66348394726001));
#36142=CARTESIAN_POINT('Ctrl Pts',(-0.880258220622017,1.61440330069759,
6.77467036709119));
#36143=CARTESIAN_POINT('Ctrl Pts',(-1.53940153309356,0.591912849892102,
6.85152779320574));
#36144=CARTESIAN_POINT('Ctrl Pts',(-1.55790160368306,0.0386873070159844,
6.89132307937659));
#36145=CARTESIAN_POINT('Ctrl Pts',(-1.55769406638298,0.000677585252333878,
6.89405622560371));
#36146=CARTESIAN_POINT('Origin',(0.,0.,-1.29405622560369));
#36147=CARTESIAN_POINT('',(-1.55596383579478,0.00138071545366175,5.3559437743963));
#36148=CARTESIAN_POINT('',(-1.5529563387483,0.000151106445085702,5.49405622560371));
#36149=CARTESIAN_POINT('',(-1.5555,-2.01987159101623E-13,-1.29405622560369));
#36150=CARTESIAN_POINT('Ctrl Pts',(-1.55596383579478,0.00138071545366179,
5.3559437743963));
#36151=CARTESIAN_POINT('Ctrl Pts',(-1.55217514150148,-0.410190199764792,
5.38545280752634));
#36152=CARTESIAN_POINT('Ctrl Pts',(-1.17330640529453,-1.34449549172498,
5.45199905748485));
#36153=CARTESIAN_POINT('Ctrl Pts',(0.403262995152723,-1.79359935217008,
5.55558252427184));
#36154=CARTESIAN_POINT('Ctrl Pts',(1.72546185411942,-0.634350903950841,
5.66669417475728));
#36155=CARTESIAN_POINT('Ctrl Pts',(1.46900873501267,1.1052750860401,5.77780582524271));
#36156=CARTESIAN_POINT('Ctrl Pts',(-0.13146340126236,1.83366765077345,5.88891747572816));
#36157=CARTESIAN_POINT('Ctrl Pts',(-1.36655195880861,1.04159698732297,5.98163012544601));
#36158=CARTESIAN_POINT('Ctrl Pts',(-1.55290994688111,0.261203028467153,
6.0373055583354));
#36159=CARTESIAN_POINT('Ctrl Pts',(-1.55295114066544,-2.74881667468134E-5,
6.0559437743963));
#36160=CARTESIAN_POINT('Ctrl Pts',(-1.5529563387483,0.000151106445085633,
5.49405622560371));
#36161=CARTESIAN_POINT('Ctrl Pts',(-1.55272340811799,-0.268780222436924,
5.5132440667186));
#36162=CARTESIAN_POINT('Ctrl Pts',(-1.35831396530156,-1.05747938365068,
5.56949404777722));
#36163=CARTESIAN_POINT('Ctrl Pts',(-0.103102773360761,-1.83589824620028,
5.66280616877956));
#36164=CARTESIAN_POINT('Ctrl Pts',(1.4869956060099,-1.08166382022474,5.77399258861071));
#36165=CARTESIAN_POINT('Ctrl Pts',(1.71494149863546,0.663421591850831,5.88517900844189));
#36166=CARTESIAN_POINT('Ctrl Pts',(0.371926577693494,1.80078404398782,5.99636542827304));
#36167=CARTESIAN_POINT('Ctrl Pts',(-1.18720103315053,1.32645343006727,6.09932450066032));
#36168=CARTESIAN_POINT('Ctrl Pts',(-1.55195221197423,0.40094597399841,6.16522143310387));
#36169=CARTESIAN_POINT('Ctrl Pts',(-1.55567057787938,-0.00141549514015748,
6.19405622560371));
#36170=CARTESIAN_POINT('Origin',(0.,0.,-1.29405622560369));
#36171=CARTESIAN_POINT('',(-1.55745492001379,-0.000856371120316566,4.6559437743963));
#36172=CARTESIAN_POINT('',(-1.55622585425313,0.00134239099646036,4.79405622560371));
#36173=CARTESIAN_POINT('',(-1.5555,-2.01987159101623E-13,-1.29405622560369));
#36174=CARTESIAN_POINT('Ctrl Pts',(-1.55745492001379,-0.000856371120316864,
4.65594377439631));
#36175=CARTESIAN_POINT('Ctrl Pts',(-1.5577850741697,-0.0506891626144068,
4.65952562306032));
#36176=CARTESIAN_POINT('Ctrl Pts',(-1.53301192978291,-0.615473136307116,
4.70014468855281));
#36177=CARTESIAN_POINT('Ctrl Pts',(-0.844041411881997,-1.63316067010957,
4.77780097087378));
#36178=CARTESIAN_POINT('Ctrl Pts',(0.913973507436636,-1.59507746114991,
4.88891262135923));
#36179=CARTESIAN_POINT('Ctrl Pts',(1.83577980123458,-0.0976329900371924,
5.00002427184466));
#36180=CARTESIAN_POINT('Ctrl Pts',(1.0780025055099,1.48913742733129,5.1111359223301));
#36181=CARTESIAN_POINT('Ctrl Pts',(-0.666056105926533,1.7134727727987,5.22224757281553));
#36182=CARTESIAN_POINT('Ctrl Pts',(-1.49938299705611,0.726891414718789,
5.30385019017093));
#36183=CARTESIAN_POINT('Ctrl Pts',(-1.55693038683329,0.106378444150779,
5.34841559069786));
#36184=CARTESIAN_POINT('Ctrl Pts',(-1.55596383579478,0.00138071545366179,
5.3559437743963));
#36185=CARTESIAN_POINT('Ctrl Pts',(-1.55622585425313,0.00134239099646029,
4.79405622560371));
#36186=CARTESIAN_POINT('Ctrl Pts',(-1.55239700220769,-0.418962472451577,
4.82420456038961));
#36187=CARTESIAN_POINT('Ctrl Pts',(-1.15964303797854,-1.36226320639006,
4.89141503511923));
#36188=CARTESIAN_POINT('Ctrl Pts',(0.435376164803608,-1.7865050090601,4.99568764979258));
#36189=CARTESIAN_POINT('Ctrl Pts',(1.73732980498774,-0.602360109052031,
5.10687406962374));
#36190=CARTESIAN_POINT('Ctrl Pts',(1.44781397169404,1.13357278356683,5.21806048945491));
#36191=CARTESIAN_POINT('Ctrl Pts',(-0.167962271460079,1.83110382765203,
5.32924690928607));
#36192=CARTESIAN_POINT('Ctrl Pts',(-1.37758975876034,1.02035875886683,5.42124548800234));
#36193=CARTESIAN_POINT('Ctrl Pts',(-1.55317332364345,0.250672199885809,
5.47618192677488));
#36194=CARTESIAN_POINT('Ctrl Pts',(-1.5529563387483,0.000151106445085633,
5.49405622560371));
#36195=CARTESIAN_POINT('Origin',(0.,0.,-1.29405622560369));
#36196=CARTESIAN_POINT('',(-1.55339129538237,-0.00082587420025254,3.9559437743963));
#36197=CARTESIAN_POINT('',(-1.5573160577951,-0.00094952305265919,4.09405622560371));
#36198=CARTESIAN_POINT('',(-1.5555,-2.01987159101623E-13,-1.29405622560369));
#36199=CARTESIAN_POINT('Ctrl Pts',(-1.55339129538237,-0.000825874200252562,
3.9559437743963));
#36200=CARTESIAN_POINT('Ctrl Pts',(-1.55438295724494,-0.206599346759669,
3.97063565542278));
#36201=CARTESIAN_POINT('Ctrl Pts',(-1.42062281789543,-0.929876204718288,
4.02236475327773));
#36202=CARTESIAN_POINT('Ctrl Pts',(-0.325213021862407,-1.80938005122649,
4.11113106796117));
#36203=CARTESIAN_POINT('Ctrl Pts',(1.34348911316817,-1.25485325124609,4.2222427184466));
#36204=CARTESIAN_POINT('Ctrl Pts',(1.78301209192838,0.447758371671112,4.33335436893204));
#36205=CARTESIAN_POINT('Ctrl Pts',(0.591229481908682,1.74070887258225,4.44446601941748));
#36206=CARTESIAN_POINT('Ctrl Pts',(-1.0856218085317,1.45071736103991,4.55199582123889));
#36207=CARTESIAN_POINT('Ctrl Pts',(-1.55437119708937,0.464594445617744,
4.62248840623184));
#36208=CARTESIAN_POINT('Ctrl Pts',(-1.55745492001379,-0.000856371120316864,
4.65594377439631));
#36209=CARTESIAN_POINT('Ctrl Pts',(-1.5573160577951,-0.000949523052659442,
4.0940562256037));
#36210=CARTESIAN_POINT('Ctrl Pts',(-1.55772052747877,-0.0572626470532979,
4.0981029141169));
#36211=CARTESIAN_POINT('Ctrl Pts',(-1.52938259291224,-0.628915705084586,
4.13921174257381));
#36212=CARTESIAN_POINT('Ctrl Pts',(-0.822616502622442,-1.64452261823584,
4.21738271097444));
#36213=CARTESIAN_POINT('Ctrl Pts',(0.936204134582059,-1.58261630557358,
4.3285691308056));
#36214=CARTESIAN_POINT('Ctrl Pts',(1.83742116834086,-0.0709647969689106,
4.43975555063676));
#36215=CARTESIAN_POINT('Ctrl Pts',(1.0554806974386,1.50569354438759,4.55094197046793));
#36216=CARTESIAN_POINT('Ctrl Pts',(-0.693325883166112,1.70307127625589,
4.66212839029909));
#36217=CARTESIAN_POINT('Ctrl Pts',(-1.50503746143118,0.709862178387775,
4.74316647534435));
#36218=CARTESIAN_POINT('Ctrl Pts',(-1.55710391061042,0.0977293375193425,
4.78714242044589));
#36219=CARTESIAN_POINT('Ctrl Pts',(-1.55622585425313,0.00134239099646029,
4.79405622560371));
#36220=CARTESIAN_POINT('Origin',(0.,0.,-1.29405622560369));
#36221=CARTESIAN_POINT('',(-1.55444674488022,0.00131742778884735,3.2559437743963));
#36222=CARTESIAN_POINT('',(-1.5533186684889,-0.000770198572060954,3.39405622560371));
#36223=CARTESIAN_POINT('',(-1.5555,-2.01987159101623E-13,-1.29405622560369));
#36224=CARTESIAN_POINT('Ctrl Pts',(-1.55444674488022,0.00131742778884739,
3.2559437743963));
#36225=CARTESIAN_POINT('Ctrl Pts',(-1.55154236665719,-0.359445316439912,
3.28174568778523));
#36226=CARTESIAN_POINT('Ctrl Pts',(-1.24691611905359,-1.24248704432008,
3.34458481800264));
#36227=CARTESIAN_POINT('Ctrl Pts',(0.222506403513669,-1.8248590575151,3.44446116504855));
#36228=CARTESIAN_POINT('Ctrl Pts',(1.65365282072159,-0.803151310699741,
3.55557281553397));
#36229=CARTESIAN_POINT('Ctrl Pts',(1.57184646516792,0.953372104320743,3.66668446601942));
#36230=CARTESIAN_POINT('Ctrl Pts',(0.0519332482321354,1.83764050268212,
3.77779611650485));
#36231=CARTESIAN_POINT('Ctrl Pts',(-1.30823935507303,1.14600960175539,3.87421588596382));
#36232=CARTESIAN_POINT('Ctrl Pts',(-1.55188304621527,0.312141358191517,
3.9335984385943));
#36233=CARTESIAN_POINT('Ctrl Pts',(-1.55339129538237,-0.000825874200252562,
3.9559437743963));
#36234=CARTESIAN_POINT('Ctrl Pts',(-1.5533186684889,-0.000770198572060919,
3.39405622560371));
#36235=CARTESIAN_POINT('Ctrl Pts',(-1.5542597194186,-0.210984061911746,
3.4090634077879));
#36236=CARTESIAN_POINT('Ctrl Pts',(-1.41654850766895,-0.939166341982764,
3.46113272991582));
#36237=CARTESIAN_POINT('Ctrl Pts',(-0.308692884081366,-1.81269447386996,
3.55026419198746));
#36238=CARTESIAN_POINT('Ctrl Pts',(1.35606994996762,-1.24186426112907,3.66145061181863));
#36239=CARTESIAN_POINT('Ctrl Pts',(1.77861387826841,0.466567491694538,3.77263703164979));
#36240=CARTESIAN_POINT('Ctrl Pts',(0.571870330903418,1.74760318061885,3.88382345148095));
#36241=CARTESIAN_POINT('Ctrl Pts',(-1.09574509035902,1.43939945308724,3.99096318279893));
#36242=CARTESIAN_POINT('Ctrl Pts',(-1.55401613758806,0.458488658137791,
4.06104077417318));
#36243=CARTESIAN_POINT('Ctrl Pts',(-1.5573160577951,-0.000949523052659442,
4.0940562256037));
#36244=CARTESIAN_POINT('Origin',(0.,0.,-1.29405622560369));
#36245=CARTESIAN_POINT('',(-1.55804712705668,3.25009013604671E-5,2.5559437743963));
#36246=CARTESIAN_POINT('',(-1.55449947323643,0.00133480041304715,2.69405622560371));
#36247=CARTESIAN_POINT('',(-1.5555,-2.01987159101623E-13,-1.29405622560369));
#36248=CARTESIAN_POINT('Ctrl Pts',(-1.55804712705668,3.25009013604029E-5,
2.5559437743963));
#36249=CARTESIAN_POINT('Ctrl Pts',(-1.55788927539753,-0.512989453804214,
2.59285572014769));
#36250=CARTESIAN_POINT('Ctrl Pts',(-1.0006227616332,-1.54106832868198,2.66680488272757));
#36251=CARTESIAN_POINT('Ctrl Pts',(0.750458968510211,-1.67822257683237,
2.77779126213592));
#36252=CARTESIAN_POINT('Ctrl Pts',(1.81691053470019,-0.280099604209337,
2.88890291262136));
#36253=CARTESIAN_POINT('Ctrl Pts',(1.22104229764526,1.37429086670804,3.0000145631068));
#36254=CARTESIAN_POINT('Ctrl Pts',(-0.491976593161155,1.77132117679823,
3.11112621359223));
#36255=CARTESIAN_POINT('Ctrl Pts',(-1.46161229246342,0.831876851886141,
3.19643595068874));
#36256=CARTESIAN_POINT('Ctrl Pts',(-1.55571144064704,0.158409610837222,
3.24470847095676));
#36257=CARTESIAN_POINT('Ctrl Pts',(-1.55444674488022,0.00131742778884739,
3.2559437743963));
#36258=CARTESIAN_POINT('Ctrl Pts',(-1.55449947323643,0.00133480041304701,
2.69405622560371));
#36259=CARTESIAN_POINT('Ctrl Pts',(-1.55153406972295,-0.361714100102126,
2.72002390145891));
#36260=CARTESIAN_POINT('Ctrl Pts',(-1.2437032104418,-1.24745277135715,2.78305371725784));
#36261=CARTESIAN_POINT('Ctrl Pts',(0.231926238140432,-1.82410602009977,
2.88314567300049));
#36262=CARTESIAN_POINT('Ctrl Pts',(1.65866396469461,-0.793716828903688,
2.99433209283165));
#36263=CARTESIAN_POINT('Ctrl Pts',(1.56599354026699,0.96375141196464,3.10551851266282));
#36264=CARTESIAN_POINT('Ctrl Pts',(0.0388050940998321,1.83838154825996,
3.21670493249398));
#36265=CARTESIAN_POINT('Ctrl Pts',(-1.31300314367493,1.13822266482633,3.31288417014094));
#36266=CARTESIAN_POINT('Ctrl Pts',(-1.55193567478298,0.308165737536199,
3.37200126784418));
#36267=CARTESIAN_POINT('Ctrl Pts',(-1.5533186684889,-0.000770198572060919,
3.39405622560371));
#36268=CARTESIAN_POINT('Origin',(0.,0.,-1.29405622560369));
#36269=CARTESIAN_POINT('',(-1.55454118234884,-0.00133834695600709,1.8559437743963));
#36270=CARTESIAN_POINT('',(-1.55805467550008,3.4854191793785E-5,1.9940562256037));
#36271=CARTESIAN_POINT('',(-1.5555,-2.01987159101623E-13,-1.29405622560369));
#36272=CARTESIAN_POINT('Ctrl Pts',(-1.55454118234884,-0.00133834695600729,
1.8559437743963));
#36273=CARTESIAN_POINT('Ctrl Pts',(-1.55580288786201,-0.154903851691022,
1.86692853568168));
#36274=CARTESIAN_POINT('Ctrl Pts',(-1.46436232298065,-0.824775316270878,
1.91495051379553));
#36275=CARTESIAN_POINT('Ctrl Pts',(-0.503915664640746,-1.76796168665343,
2.00000970873786));
#36276=CARTESIAN_POINT('Ctrl Pts',(1.21174280763407,-1.38249741391359,2.1111213592233));
#36277=CARTESIAN_POINT('Ctrl Pts',(1.81875888824183,0.267835396201195,2.22223300970874));
#36278=CARTESIAN_POINT('Ctrl Pts',(0.761764071097843,1.67312138149853,2.33334466019417));
#36279=CARTESIAN_POINT('Ctrl Pts',(-0.992180579104728,1.54764252547341,
2.44445631067961));
#36280=CARTESIAN_POINT('Ctrl Pts',(-1.55725669913861,0.518277207581445,
2.51865601541365));
#36281=CARTESIAN_POINT('Ctrl Pts',(-1.55804766277071,0.0017735852989955,
2.55581850331921));
#36282=CARTESIAN_POINT('Ctrl Pts',(-1.55804712705668,3.25009013604029E-5,
2.5559437743963));
#36283=CARTESIAN_POINT('Ctrl Pts',(-1.55805467550008,3.48541917938314E-5,
1.9940562256037));
#36284=CARTESIAN_POINT('Ctrl Pts',(-1.55788564535512,-0.513206116891616,
2.03098439512992));
#36285=CARTESIAN_POINT('Ctrl Pts',(-1.00003893378143,-1.54186484140614,
2.10497470459985));
#36286=CARTESIAN_POINT('Ctrl Pts',(0.752488571272716,-1.67777039880966,
2.21602715401351));
#36287=CARTESIAN_POINT('Ctrl Pts',(1.81781810074028,-0.276929424335053,
2.32721357384467));
#36288=CARTESIAN_POINT('Ctrl Pts',(1.21794738393109,1.37759091140133,2.43839999367584));
#36289=CARTESIAN_POINT('Ctrl Pts',(-0.497615974795104,1.77017821004958,
2.549586413507));
#36290=CARTESIAN_POINT('Ctrl Pts',(-1.46313162187878,0.828233020270418,
2.63480515748296));
#36291=CARTESIAN_POINT('Ctrl Pts',(-1.55576641614544,0.156444291597347,
2.68296176151519));
#36292=CARTESIAN_POINT('Ctrl Pts',(-1.55449947323643,0.00133480041304701,
2.69405622560371));
#36293=CARTESIAN_POINT('Origin',(0.,0.,-1.29405622560369));
#36294=CARTESIAN_POINT('',(-1.55333634177863,0.000779921548230329,1.1559437743963));
#36295=CARTESIAN_POINT('',(-1.55460191805193,-0.00135568056800359,1.2940562256037));
#36296=CARTESIAN_POINT('',(-1.5555,-2.01987159101623E-13,-1.29405622560369));
#36297=CARTESIAN_POINT('Ctrl Pts',(-1.55333634177863,0.000779921548230561,
1.1559437743963));
#36298=CARTESIAN_POINT('Ctrl Pts',(-1.55193438638927,-0.308706275100063,
1.17803856804414));
#36299=CARTESIAN_POINT('Ctrl Pts',(-1.31241956589738,-1.1389814578602,1.23717057852045));
#36300=CARTESIAN_POINT('Ctrl Pts',(0.0395347168138628,-1.83794704008407,
1.33333980582524));
#36301=CARTESIAN_POINT('Ctrl Pts',(1.56537855283131,-0.963955976349113,
1.44445145631068));
#36302=CARTESIAN_POINT('Ctrl Pts',(1.65903376979378,0.791977165381959,1.55556310679611));
#36303=CARTESIAN_POINT('Ctrl Pts',(0.234812759114929,1.82331608910266,1.66667475728155));
#36304=CARTESIAN_POINT('Ctrl Pts',(-1.24220109658982,1.24943524423025,1.76680164648161));
#36305=CARTESIAN_POINT('Ctrl Pts',(-1.55154880719052,0.362871523529771,
1.8298913188532));
#36306=CARTESIAN_POINT('Ctrl Pts',(-1.55454118234884,-0.00133834695600729,
1.8559437743963));
#36307=CARTESIAN_POINT('Ctrl Pts',(-1.55460191805193,-0.00135568056800364,
1.2940562256037));
#36308=CARTESIAN_POINT('Ctrl Pts',(-1.5558637635503,-0.152693971168416,
1.30488274885721));
#36309=CARTESIAN_POINT('Ctrl Pts',(-1.46605510259419,-0.820638709603335,
1.35277141205443));
#36310=CARTESIAN_POINT('Ctrl Pts',(-0.510374815939226,-1.76654153931159,
1.43772221519537));
#36311=CARTESIAN_POINT('Ctrl Pts',(1.20797626960931,-1.38634273102519,1.54890863502654));
#36312=CARTESIAN_POINT('Ctrl Pts',(1.81976886629041,0.263806680570579,1.6600950548577));
#36313=CARTESIAN_POINT('Ctrl Pts',(0.764574137846417,1.67229745635935,1.77128147468886));
#36314=CARTESIAN_POINT('Ctrl Pts',(-0.991003621173195,1.54889135395602,
1.88246789452002));
#36315=CARTESIAN_POINT('Ctrl Pts',(-1.5572087700955,0.518861158146894,1.95672614482497));
#36316=CARTESIAN_POINT('Ctrl Pts',(-1.55805528871865,0.00189682319971778,
1.9939222551862));
#36317=CARTESIAN_POINT('Ctrl Pts',(-1.55805467550008,3.48541917938314E-5,
1.9940562256037));
#36318=CARTESIAN_POINT('Origin',(0.,0.,-1.29405622560369));
#36319=CARTESIAN_POINT('',(-1.55735926886437,0.00101346774827271,0.455943774396301));
#36320=CARTESIAN_POINT('',(-1.55326046963413,0.000729270061605516,0.594056225603705));
#36321=CARTESIAN_POINT('',(-1.5555,-2.01987159101623E-13,-1.29405622560369));
#36322=CARTESIAN_POINT('Ctrl Pts',(-1.55735926886437,0.00101346774827265,
0.455943774396301));
#36323=CARTESIAN_POINT('Ctrl Pts',(-1.5541538777776,-0.460983628495037,
0.489148600406595));
#36324=CARTESIAN_POINT('Ctrl Pts',(-1.09151218308356,-1.44423481489054,
0.559390643245367));
#36325=CARTESIAN_POINT('Ctrl Pts',(0.579488995883613,-1.74456230311225,
0.666669902912619));
#36326=CARTESIAN_POINT('Ctrl Pts',(1.77994191588978,-0.459827600750814,
0.777781553398056));
#36327=CARTESIAN_POINT('Ctrl Pts',(1.35192905881154,1.24578720765632,0.888893203883492));
#36328=CARTESIAN_POINT('Ctrl Pts',(-0.313001003158473,1.81151906168851,
1.00000485436893));
#36329=CARTESIAN_POINT('Ctrl Pts',(-1.41742497137191,0.93698092273704,1.08902171120653));
#36330=CARTESIAN_POINT('Ctrl Pts',(-1.55428446607623,0.210081433596544,
1.14100135121566));
#36331=CARTESIAN_POINT('Ctrl Pts',(-1.55333634177863,0.000779921548230561,
1.1559437743963));
#36332=CARTESIAN_POINT('Ctrl Pts',(-1.55326046963413,0.000729270061605551,
0.594056225603705));
#36333=CARTESIAN_POINT('Ctrl Pts',(-1.55199262831984,-0.304485333833814,
0.615843242528215));
#36334=CARTESIAN_POINT('Ctrl Pts',(-1.31743653601245,-1.13071739766558,
0.674692399396446));
#36335=CARTESIAN_POINT('Ctrl Pts',(0.0255447675030308,-1.83860034663711,
0.770603696208398));
#36336=CARTESIAN_POINT('Ctrl Pts',(1.55899683301632,-0.975032021788082,
0.881790116039561));
#36337=CARTESIAN_POINT('Ctrl Pts',(1.66434877052597,0.781732535368643,0.992976535870723));
#36338=CARTESIAN_POINT('Ctrl Pts',(0.245080507541896,1.82238325373942,1.10416295570189));
#36339=CARTESIAN_POINT('Ctrl Pts',(-1.23863138927055,1.25487925833816,1.20452285227955));
#36340=CARTESIAN_POINT('Ctrl Pts',(-1.55154412248428,0.365378245899198,
1.26782060891349));
#36341=CARTESIAN_POINT('Ctrl Pts',(-1.55460191805193,-0.00135568056800364,
1.2940562256037));
#36342=CARTESIAN_POINT('Origin',(0.,0.,11.5));
#36343=CARTESIAN_POINT('',(-1.77892626630995,-0.0012009523392913,11.2223275485995));
#36344=CARTESIAN_POINT('Ctrl Pts',(1.55548765964692,0.00619602180104861,
11.4445));
#36345=CARTESIAN_POINT('Ctrl Pts',(1.55843889773201,-0.053546881811892,
11.4417867591843));
#36346=CARTESIAN_POINT('Ctrl Pts',(1.55766805736304,-0.113278156040886,
11.439086160746));
#36347=CARTESIAN_POINT('Ctrl Pts',(1.55338999746751,-0.172741258360748,
11.4363936568093));
#36348=CARTESIAN_POINT('Ctrl Pts',(1.54917978268939,-0.231261344159722,
11.4337438528932));
#36349=CARTESIAN_POINT('Ctrl Pts',(1.54157226362346,-0.289522447371128,
11.4311018887755));
#36350=CARTESIAN_POINT('Ctrl Pts',(1.5307259163647,-0.347284232316321,11.4284634295395));
#36351=CARTESIAN_POINT('Ctrl Pts',(1.52490021612,-0.37830876404678,11.427046282158));
#36352=CARTESIAN_POINT('Ctrl Pts',(1.51813939227042,-0.409189253639797,
11.4256301458963));
#36353=CARTESIAN_POINT('Ctrl Pts',(1.51046300038634,-0.439887833717896,
11.4242143490555));
#36354=CARTESIAN_POINT('Ctrl Pts',(1.50749771858011,-0.451746261786366,
11.4236674467248));
#36355=CARTESIAN_POINT('Ctrl Pts',(1.50439653465153,-0.463574222421597,
11.4231207471528));
#36356=CARTESIAN_POINT('Ctrl Pts',(1.50116353235453,-0.47535996619676,11.4225746575513));
#36357=CARTESIAN_POINT('Ctrl Pts',(1.48455611813741,-0.535901441503565,
11.4197694828629));
#36358=CARTESIAN_POINT('Ctrl Pts',(1.46445634965142,-0.595403551134085,
11.4169769764437));
#36359=CARTESIAN_POINT('Ctrl Pts',(1.4410621824655,-0.653580209875647,11.414192092755));
#36360=CARTESIAN_POINT('Ctrl Pts',(1.41747802435967,-0.712229338392404,
11.4113845922059));
#36361=CARTESIAN_POINT('Ctrl Pts',(1.39054537943373,-0.769532412755046,
11.4085848387028));
#36362=CARTESIAN_POINT('Ctrl Pts',(1.36041578548535,-0.825184282227088,
11.4057876627772));
#36363=CARTESIAN_POINT('Ctrl Pts',(1.35261592294621,-0.839591277975912,
11.4050635379265));
#36364=CARTESIAN_POINT('Ctrl Pts',(1.34460155997405,-0.853887506909652,
11.4043395858183));
#36365=CARTESIAN_POINT('Ctrl Pts',(1.33637481784576,-0.868067413704247,
11.4036157167661));
#36366=CARTESIAN_POINT('Ctrl Pts',(1.33123141939554,-0.87693275912219,11.4031631503791));
#36367=CARTESIAN_POINT('Ctrl Pts',(1.32600576325494,-0.885751206456736,
11.4027106878625));
#36368=CARTESIAN_POINT('Ctrl Pts',(1.32070341258855,-0.894513477947337,
11.4022587210796));
#36369=CARTESIAN_POINT('Ctrl Pts',(1.28755838481391,-0.949286492822766,
11.3994334738427));
#36370=CARTESIAN_POINT('Ctrl Pts',(1.25136992677528,-1.00195372283142,11.3966231054397));
#36371=CARTESIAN_POINT('Ctrl Pts',(1.21232687524415,-1.05222079285711,11.3938225048748));
#36372=CARTESIAN_POINT('Ctrl Pts',(1.17352218779371,-1.10218097437215,11.3910390024248));
#36373=CARTESIAN_POINT('Ctrl Pts',(1.13189715922074,-1.14977118940024,11.3882651489085));
#36374=CARTESIAN_POINT('Ctrl Pts',(1.08759128036108,-1.19468014867466,11.3854959263702));
#36375=CARTESIAN_POINT('Ctrl Pts',(1.05692354853581,-1.22576532190738,11.3835791203762));
#36376=CARTESIAN_POINT('Ctrl Pts',(1.0249704261144,-1.25556541150052,11.3816645331574));
#36377=CARTESIAN_POINT('Ctrl Pts',(0.991767007145199,-1.28396712328559,
11.379750500582));
#36378=CARTESIAN_POINT('Ctrl Pts',(0.971829282858114,-1.30102155672743,
11.378601177562));
#36379=CARTESIAN_POINT('Ctrl Pts',(0.951440575196337,-1.31757160665078,
11.3774520545279));
#36380=CARTESIAN_POINT('Ctrl Pts',(0.930607078503626,-1.33359088746794,
11.3763027711782));
#36381=CARTESIAN_POINT('Ctrl Pts',(0.921822018225176,-1.34034589118487,
11.3758181418501));
#36382=CARTESIAN_POINT('Ctrl Pts',(0.912957575551233,-1.34700657088378,
11.3753334724466));
#36383=CARTESIAN_POINT('Ctrl Pts',(0.904026617991894,-1.35356212132308,
11.3748494000991));
#36384=CARTESIAN_POINT('Ctrl Pts',(0.898865665597572,-1.35735039189889,
11.3745696681303));
#36385=CARTESIAN_POINT('Ctrl Pts',(0.893681522170691,-1.36110432047063,
11.3742900812105));
#36386=CARTESIAN_POINT('Ctrl Pts',(0.888474357058895,-1.36482361432558,
11.3740106343829));
#36387=CARTESIAN_POINT('Ctrl Pts',(0.838811308516624,-1.4002961732508,11.3713454257582));
#36388=CARTESIAN_POINT('Ctrl Pts',(0.787057395286918,-1.43262124116857,
11.368692960317));
#36389=CARTESIAN_POINT('Ctrl Pts',(0.733560484100527,-1.46184200007972,
11.3660489378073));
#36390=CARTESIAN_POINT('Ctrl Pts',(0.677705393253366,-1.49235082960671,
11.3632883650152));
#36391=CARTESIAN_POINT('Ctrl Pts',(0.619949541746925,-1.51947609806138,
11.3605369959002));
#36392=CARTESIAN_POINT('Ctrl Pts',(0.560651932851881,-1.54322365588157,
11.3577899361005));
#36393=CARTESIAN_POINT('Ctrl Pts',(0.511114145446654,-1.56306259192994,
11.3554950161722));
#36394=CARTESIAN_POINT('Ctrl Pts',(0.460499386969577,-1.58054347420583,
11.3532031037542));
#36395=CARTESIAN_POINT('Ctrl Pts',(0.409004561176526,-1.5956447160272,11.3509113452381));
#36396=CARTESIAN_POINT('Ctrl Pts',(0.394571471762801,-1.59987732717035,
11.3502690058367));
#36397=CARTESIAN_POINT('Ctrl Pts',(0.38006920116156,-1.60392285642947,11.3496266785255));
#36398=CARTESIAN_POINT('Ctrl Pts',(0.365502000908426,-1.60778049339754,
11.3489843004725));
#36399=CARTESIAN_POINT('Ctrl Pts',(0.352945849497182,-1.61110557117631,
11.3484306047756));
#36400=CARTESIAN_POINT('Ctrl Pts',(0.340339686983491,-1.61429135213649,
11.3478767954507));
#36401=CARTESIAN_POINT('Ctrl Pts',(0.327707338901135,-1.61733252206154,
11.3473237518226));
#36402=CARTESIAN_POINT('Ctrl Pts',(0.26442068399392,-1.63256844418037,11.3445530649309));
#36403=CARTESIAN_POINT('Ctrl Pts',(0.200363163100888,-1.64421053384351,
11.3417964693365));
#36404=CARTESIAN_POINT('Ctrl Pts',(0.135902532141567,-1.65227549235515,
11.3390491503551));
#36405=CARTESIAN_POINT('Ctrl Pts',(0.0706504004584388,-1.66043947907059,
11.3362680975283));
#36406=CARTESIAN_POINT('Ctrl Pts',(0.00498413291330568,-1.6649382180869,
11.333496550525));
#36407=CARTESIAN_POINT('Ctrl Pts',(-0.0607337043444866,-1.66573959706564,
11.3307295151184));
#36408=CARTESIAN_POINT('Ctrl Pts',(-0.114943810254912,-1.66640064802417,
11.3284470102656));
#36409=CARTESIAN_POINT('Ctrl Pts',(-0.169189647051337,-1.66454499730668,
11.326167575313));
#36410=CARTESIAN_POINT('Ctrl Pts',(-0.223269283792523,-1.66012780789457,
11.3238884070273));
#36411=CARTESIAN_POINT('Ctrl Pts',(-0.242921115785065,-1.65852265909112,
11.3230601871106));
#36412=CARTESIAN_POINT('Ctrl Pts',(-0.262550978640708,-1.65657902103982,
11.3222320024074));
#36413=CARTESIAN_POINT('Ctrl Pts',(-0.282149042864747,-1.65429391513469,
11.3214037184036));
#36414=CARTESIAN_POINT('Ctrl Pts',(-0.293822649715497,-1.65293278948249,
11.3209103501959));
#36415=CARTESIAN_POINT('Ctrl Pts',(-0.305486007024825,-1.65145026241138,
11.3204169024293));
#36416=CARTESIAN_POINT('Ctrl Pts',(-0.317120120921591,-1.64984824722041,
11.3199240638241));
#36417=CARTESIAN_POINT('Ctrl Pts',(-0.382649500838262,-1.64082486451904,
11.3171481404934));
#36418=CARTESIAN_POINT('Ctrl Pts',(-0.447374851901241,-1.62800143931766,
11.3143862955204));
#36419=CARTESIAN_POINT('Ctrl Pts',(-0.510936115769287,-1.6113566500933,
11.3116336908415));
#36420=CARTESIAN_POINT('Ctrl Pts',(-0.573549739883189,-1.59496001930709,
11.3089221249567));
#36421=CARTESIAN_POINT('Ctrl Pts',(-0.635034780101342,-1.57485515271455,
11.3062195258916));
#36422=CARTESIAN_POINT('Ctrl Pts',(-0.695044280650932,-1.55097228857054,
11.3035212687658));
#36423=CARTESIAN_POINT('Ctrl Pts',(-0.755213263935446,-1.52702595273528,
11.3008158406849));
#36424=CARTESIAN_POINT('Ctrl Pts',(-0.813899721511821,-1.49928127162975,
11.2981147776525));
#36425=CARTESIAN_POINT('Ctrl Pts',(-0.870916818143125,-1.46801413582731,
11.2954134178164));
#36426=CARTESIAN_POINT('Ctrl Pts',(-0.88517189274549,-1.46019691292752,
11.2947380399339));
#36427=CARTESIAN_POINT('Ctrl Pts',(-0.8993225020166,-1.4521592870016,11.294062643499));
#36428=CARTESIAN_POINT('Ctrl Pts',(-0.913365468395192,-1.44390514150358,
11.2933871556582));
#36429=CARTESIAN_POINT('Ctrl Pts',(-0.922789553247202,-1.43836587255875,
11.2929338429778));
#36430=CARTESIAN_POINT('Ctrl Pts',(-0.932156968408698,-1.43273389293101,
11.2924808828034));
#36431=CARTESIAN_POINT('Ctrl Pts',(-0.941465939330546,-1.42701150822941,
11.2920283046203));
#36432=CARTESIAN_POINT('Ctrl Pts',(-0.997258564244995,-1.39271482109252,
11.2893158109378));
#36433=CARTESIAN_POINT('Ctrl Pts',(-1.05096555773083,-1.35516769400791,
11.2866164406656));
#36434=CARTESIAN_POINT('Ctrl Pts',(-1.10242222381511,-1.31470157532149,
11.2839256753843));
#36435=CARTESIAN_POINT('Ctrl Pts',(-1.15490559840975,-1.27342804116106,
11.2811812215953));
#36436=CARTESIAN_POINT('Ctrl Pts',(-1.20504870548191,-1.22911724367845,
11.2784457196118));
#36437=CARTESIAN_POINT('Ctrl Pts',(-1.25265335579406,-1.18207076364008,
11.2757143751156));
#36438=CARTESIAN_POINT('Ctrl Pts',(-1.28397500867159,-1.15111636092502,
11.2739172770666));
#36439=CARTESIAN_POINT('Ctrl Pts',(-1.31419725536704,-1.11897666094205,
11.2721219788063));
#36440=CARTESIAN_POINT('Ctrl Pts',(-1.34325581778868,-1.08572815742637,
11.2703271147686));
#36441=CARTESIAN_POINT('Ctrl Pts',(-1.36209363901681,-1.06417411919684,
11.2691635565932));
#36442=CARTESIAN_POINT('Ctrl Pts',(-1.38044228251278,-1.04215395727969,
11.2680001809021));
#36443=CARTESIAN_POINT('Ctrl Pts',(-1.39828252264694,-1.01968718394611,
11.2668366156616));
#36444=CARTESIAN_POINT('Ctrl Pts',(-1.40805056143521,-1.00738598666853,
11.2661995306046));
#36445=CARTESIAN_POINT('Ctrl Pts',(-1.41766921695113,-0.994946604236495,
11.2655621759649));
#36446=CARTESIAN_POINT('Ctrl Pts',(-1.42711662985222,-0.982397385607975,
11.264925758661));
#36447=CARTESIAN_POINT('Ctrl Pts',(-1.46820629310292,-0.927817028752221,
11.262157786839));
#36448=CARTESIAN_POINT('Ctrl Pts',(-1.50612185513061,-0.871087521735772,
11.2594035844773));
#36449=CARTESIAN_POINT('Ctrl Pts',(-1.54066769776793,-0.812525394359864,
11.2566583590267));
#36450=CARTESIAN_POINT('Ctrl Pts',(-1.57505516312501,-0.754231748217875,
11.2539257192103));
#36451=CARTESIAN_POINT('Ctrl Pts',(-1.60610442219133,-0.694121381542228,
11.2512019741836));
#36452=CARTESIAN_POINT('Ctrl Pts',(-1.63358497140864,-0.632471603998023,
11.2484823970106));
#36453=CARTESIAN_POINT('Ctrl Pts',(-1.65966108961598,-0.573972522557314,
11.2459018075444));
#36454=CARTESIAN_POINT('Ctrl Pts',(-1.68252420078453,-0.514086499095208,
11.2433249708101));
#36455=CARTESIAN_POINT('Ctrl Pts',(-1.70193725006908,-0.453031690747441,
11.2407478481942));
#36456=CARTESIAN_POINT('Ctrl Pts',(-1.70639988231082,-0.438996535720931,
11.2401554244947));
#36457=CARTESIAN_POINT('Ctrl Pts',(-1.71068001578898,-0.424899564800969,
11.239562985688));
#36458=CARTESIAN_POINT('Ctrl Pts',(-1.71477442803653,-0.410743347710776,
11.2389704827146));
#36459=CARTESIAN_POINT('Ctrl Pts',(-1.7181060933816,-0.399224288308597,
11.238488356953));
#36460=CARTESIAN_POINT('Ctrl Pts',(-1.72131496051192,-0.387664952239154,
11.2380061462914));
#36461=CARTESIAN_POINT('Ctrl Pts',(-1.72439513423882,-0.376083269559728,
11.2375245092466));
#36462=CARTESIAN_POINT('Ctrl Pts',(-1.73399637264737,-0.339981897872015,
11.2360231938976));
#36463=CARTESIAN_POINT('Ctrl Pts',(-1.74235845090443,-0.303626928305512,
11.234525913273));
#36464=CARTESIAN_POINT('Ctrl Pts',(-1.74944665354966,-0.267065873422436,
11.2330319031487));
#36465=CARTESIAN_POINT('Ctrl Pts',(-1.76197449586933,-0.202447076028902,
11.2303913574139));
#36466=CARTESIAN_POINT('Ctrl Pts',(-1.77052625497235,-0.137185361680741,
11.227761027999));
#36467=CARTESIAN_POINT('Ctrl Pts',(-1.77528061829343,-0.0715870718432795,
11.2251366955952));
#36468=CARTESIAN_POINT('Ctrl Pts',(-1.77697828156189,-0.0481635764959884,
11.2241996126621));
#36469=CARTESIAN_POINT('Ctrl Pts',(-1.7781912975682,-0.0246970169190114,
11.2232632943623));
#36470=CARTESIAN_POINT('Ctrl Pts',(-1.77892626630995,-0.00120095233929127,
11.2223275485995));
#36471=CARTESIAN_POINT('',(1.88128289424299,-0.51655738433239,11.046));
#36472=CARTESIAN_POINT('Ctrl Pts',(1.88079991776263,-0.516378774142054,
11.046));
#36473=CARTESIAN_POINT('Ctrl Pts',(1.89035995045861,-0.445151004206684,
11.0555631104642));
#36474=CARTESIAN_POINT('Ctrl Pts',(1.8961423315859,-0.373654493774377,11.0651669654983));
#36475=CARTESIAN_POINT('Ctrl Pts',(1.89809144951916,-0.302224012343752,
11.0748303404806));
#36476=CARTESIAN_POINT('Ctrl Pts',(1.89999077178002,-0.23261842246626,11.0842468375051));
#36477=CARTESIAN_POINT('Ctrl Pts',(1.89824990827702,-0.163074621232238,
11.0937198521185));
#36478=CARTESIAN_POINT('Ctrl Pts',(1.89277099599951,-0.0939167257851171,
11.1032667571406));
#36479=CARTESIAN_POINT('Ctrl Pts',(1.88910201129244,-0.0476047485319078,
11.1096598962807));
#36480=CARTESIAN_POINT('Ctrl Pts',(1.8837557967888,-0.00146614169388357,
11.1160861707414));
#36481=CARTESIAN_POINT('Ctrl Pts',(1.87669176161129,0.0443950771863014,
11.1225507975725));
#36482=CARTESIAN_POINT('Ctrl Pts',(1.87063241478827,0.0837336455737761,
11.1280959874063));
#36483=CARTESIAN_POINT('Ctrl Pts',(1.8633089856103,0.122868068816038,11.1336693960131));
#36484=CARTESIAN_POINT('Ctrl Pts',(1.85469071090361,0.161728394728602,11.1392743160301));
#36485=CARTESIAN_POINT('Ctrl Pts',(1.85223436103037,0.172804226014781,11.1408718103131));
#36486=CARTESIAN_POINT('Ctrl Pts',(1.84967323324123,0.183855475695868,11.142471538338));
#36487=CARTESIAN_POINT('Ctrl Pts',(1.84700939076218,0.19487013146115,11.1440720571876));
#36488=CARTESIAN_POINT('Ctrl Pts',(1.83137216521354,0.259528105007685,11.1534673853433));
#36489=CARTESIAN_POINT('Ctrl Pts',(1.81217652429567,0.323030635926077,11.1629048835303));
#36490=CARTESIAN_POINT('Ctrl Pts',(1.78934255453511,0.385087390709459,11.1724028038701));
#36491=CARTESIAN_POINT('Ctrl Pts',(1.78198218565347,0.405090947322401,11.1754643914102));
#36492=CARTESIAN_POINT('Ctrl Pts',(1.77424343060636,0.424944079046285,11.1785322571122));
#36493=CARTESIAN_POINT('Ctrl Pts',(1.76612263817241,0.444636415640588,11.181607012295));
#36494=CARTESIAN_POINT('Ctrl Pts',(1.73919119835162,0.509943216945239,11.1918039955137));
#36495=CARTESIAN_POINT('Ctrl Pts',(1.70806080167302,0.573485248201441,11.2020767507448));
#36496=CARTESIAN_POINT('Ctrl Pts',(1.67301702698032,0.634984575310704,11.2124475752393));
#36497=CARTESIAN_POINT('Ctrl Pts',(1.64235372412421,0.688796486531309,11.2215220466721));
#36498=CARTESIAN_POINT('Ctrl Pts',(1.60869302252863,0.741044106677185,11.2306716023846));
#36499=CARTESIAN_POINT('Ctrl Pts',(1.57220891785208,0.791506873950779,11.239911179793));
#36500=CARTESIAN_POINT('Ctrl Pts',(1.56528521292053,0.801083354276364,11.2416646038728));
#36501=CARTESIAN_POINT('Ctrl Pts',(1.55825911602623,0.81059620160376,11.2434214216921));
#36502=CARTESIAN_POINT('Ctrl Pts',(1.55114206425445,0.820030590825838,11.2451792455347));
#36503=CARTESIAN_POINT('Ctrl Pts',(1.51163333781795,0.872403499555923,11.254937412757));
#36504=CARTESIAN_POINT('Ctrl Pts',(1.46925448012712,0.922460374176763,11.2647444648472));
#36505=CARTESIAN_POINT('Ctrl Pts',(1.42425895086728,0.969999034377404,11.2746213834588));
#36506=CARTESIAN_POINT('Ctrl Pts',(1.37955552976012,1.01722907657888,11.2844341817346));
#36507=CARTESIAN_POINT('Ctrl Pts',(1.33226826113497,1.06197396880102,11.2943159423384));
#36508=CARTESIAN_POINT('Ctrl Pts',(1.28262305484525,1.10398985376236,11.3042872409362));
#36509=CARTESIAN_POINT('Ctrl Pts',(1.23402945162958,1.14511574274852,11.3140473238087));
#36510=CARTESIAN_POINT('Ctrl Pts',(1.18317581682196,1.18362727550242,11.3238931915966));
#36511=CARTESIAN_POINT('Ctrl Pts',(1.13026675802768,1.2192467284131,11.3338441399431));
#36512=CARTESIAN_POINT('Ctrl Pts',(1.11612186853279,1.22876935528969,11.3365044606506));
#36513=CARTESIAN_POINT('Ctrl Pts',(1.1018300740637,1.23808499004259,11.3391722917297));
#36514=CARTESIAN_POINT('Ctrl Pts',(1.0873953214649,1.24718768011963,11.3418480018757));
#36515=CARTESIAN_POINT('Ctrl Pts',(1.07843141524914,1.25284040326838,11.3435096039465));
#36516=CARTESIAN_POINT('Ctrl Pts',(1.06941317684967,1.25841040829158,11.3451740914355));
#36517=CARTESIAN_POINT('Ctrl Pts',(1.06035226952456,1.2638900735973,11.346839603865));
#36518=CARTESIAN_POINT('Ctrl Pts',(1.00742079701965,1.29590085828569,11.3565690958694));
#36519=CARTESIAN_POINT('Ctrl Pts',(0.952938092487177,1.32489391547385,11.3663514013733));
#36520=CARTESIAN_POINT('Ctrl Pts',(0.897108858642945,1.35066478023243,11.3762079140514));
#36521=CARTESIAN_POINT('Ctrl Pts',(0.842238965806958,1.37599281162795,11.3858950574554));
#36522=CARTESIAN_POINT('Ctrl Pts',(0.78606756226141,1.39820862213323,11.3956538796688));
#36523=CARTESIAN_POINT('Ctrl Pts',(0.72878604220227,1.41706842320411,11.4055046903548));
#36524=CARTESIAN_POINT('Ctrl Pts',(0.67317444208947,1.43537840719681,11.4150683217683));
#36525=CARTESIAN_POINT('Ctrl Pts',(0.616515828164059,1.45052520284418,11.4247186563809));
#36526=CARTESIAN_POINT('Ctrl Pts',(0.558993687390787,1.46223733220615,11.4344742788813));
#36527=CARTESIAN_POINT('Ctrl Pts',(0.539362537898783,1.46623444634835,11.4378036765901));
#36528=CARTESIAN_POINT('Ctrl Pts',(0.519630929867265,1.46983109384517,11.4411453373854));
#36529=CARTESIAN_POINT('Ctrl Pts',(0.499806597877626,1.47301514408983,11.4445));
#36530=CARTESIAN_POINT('',(1.56060797133591,1.17265290216009,11.046));
#36531=CARTESIAN_POINT('Origin',(0.,0.,11.046));
#36532=CARTESIAN_POINT('Ctrl Pts',(-1.77892626630995,-0.00120095233929127,
11.2223275485995));
#36533=CARTESIAN_POINT('Ctrl Pts',(-1.78091222637221,0.0622877965358305,
11.2197990686688));
#36534=CARTESIAN_POINT('Ctrl Pts',(-1.77941067542291,0.125992016111799,
11.2172747683064));
#36535=CARTESIAN_POINT('Ctrl Pts',(-1.77452381634337,0.189646102027163,
11.2147508586347));
#36536=CARTESIAN_POINT('Ctrl Pts',(-1.77287868795546,0.211074823838332,
11.2139012013432));
#36537=CARTESIAN_POINT('Ctrl Pts',(-1.7708495726434,0.232497857027148,11.2130515883281));
#36538=CARTESIAN_POINT('Ctrl Pts',(-1.76843936997923,0.253904972833394,
11.2122018750387));
#36539=CARTESIAN_POINT('Ctrl Pts',(-1.76712267121633,0.265599725029338,
11.2117376748892));
#36540=CARTESIAN_POINT('Ctrl Pts',(-1.76569197102713,0.277291668505868,
11.2112733675823));
#36541=CARTESIAN_POINT('Ctrl Pts',(-1.7641484990815,0.288972974548762,11.2108091738099));
#36542=CARTESIAN_POINT('Ctrl Pts',(-1.75515036560026,0.357072658062498,
11.2081030167356));
#36543=CARTESIAN_POINT('Ctrl Pts',(-1.74235696629666,0.42456963250346,11.2054102736121));
#36544=CARTESIAN_POINT('Ctrl Pts',(-1.72594903242932,0.491138664005795,
11.2027264834948));
#36545=CARTESIAN_POINT('Ctrl Pts',(-1.70928395222888,0.558750970212142,
11.2000006328234));
#36546=CARTESIAN_POINT('Ctrl Pts',(-1.68888999030711,0.625407040269523,
11.1972840179815));
#36547=CARTESIAN_POINT('Ctrl Pts',(-1.66490278446929,0.690766734877331,
11.1945719649831));
#36548=CARTESIAN_POINT('Ctrl Pts',(-1.64112198461878,0.755564019991226,
11.1918832487577));
#36549=CARTESIAN_POINT('Ctrl Pts',(-1.61380916520598,0.81908815011939,11.1891990162058));
#36550=CARTESIAN_POINT('Ctrl Pts',(-1.5830482712126,0.880993120829078,11.186514712963));
#36551=CARTESIAN_POINT('Ctrl Pts',(-1.57216641681974,0.902892382846704,
11.1855651242728));
#36552=CARTESIAN_POINT('Ctrl Pts',(-1.56085264019442,0.92458881232314,11.1846155267362));
#36553=CARTESIAN_POINT('Ctrl Pts',(-1.54910931637308,0.946066284278751,
11.1836657187303));
#36554=CARTESIAN_POINT('Ctrl Pts',(-1.54396572241992,0.955473450134084,
11.1832497013582));
#36555=CARTESIAN_POINT('Ctrl Pts',(-1.53874121405367,0.964835754579395,
11.1828337685169));
#36556=CARTESIAN_POINT('Ctrl Pts',(-1.5334404792476,0.974144495398925,11.18241823656));
#36557=CARTESIAN_POINT('Ctrl Pts',(-1.49854818334159,1.03541964895223,11.179682981066));
#36558=CARTESIAN_POINT('Ctrl Pts',(-1.46030493742689,1.09447092650475,11.1769608571821));
#36559=CARTESIAN_POINT('Ctrl Pts',(-1.41884997832206,1.15095727599886,11.1742472453603));
#36560=CARTESIAN_POINT('Ctrl Pts',(-1.37811238995456,1.20646613920276,11.1715805921112));
#36561=CARTESIAN_POINT('Ctrl Pts',(-1.33427285188376,1.25949901944966,11.1689221588738));
#36562=CARTESIAN_POINT('Ctrl Pts',(-1.28741864153,1.30971119589593,11.166267561795));
#36563=CARTESIAN_POINT('Ctrl Pts',(-1.26549062822221,1.33321075474058,11.1650251966024));
#36564=CARTESIAN_POINT('Ctrl Pts',(-1.24290170835111,1.35609210845284,11.1637836716393));
#36565=CARTESIAN_POINT('Ctrl Pts',(-1.21965775424868,1.37831740927343,11.1625425375316));
#36566=CARTESIAN_POINT('Ctrl Pts',(-1.19165584264812,1.40509215276722,11.1610473475387));
#36567=CARTESIAN_POINT('Ctrl Pts',(-1.16270333140537,1.43091488294274,11.1595527247918));
#36568=CARTESIAN_POINT('Ctrl Pts',(-1.13285929301872,1.45577404177113,11.1580578836196));
#36569=CARTESIAN_POINT('Ctrl Pts',(-1.12175109882477,1.46502682318719,11.1575014915585));
#36570=CARTESIAN_POINT('Ctrl Pts',(-1.11051936159011,1.47414607111053,11.156945069237));
#36571=CARTESIAN_POINT('Ctrl Pts',(-1.09916702235175,1.48313103947397,11.1563885761416));
#36572=CARTESIAN_POINT('Ctrl Pts',(-1.0900493418525,1.49034735578674,11.1559416262983));
#36573=CARTESIAN_POINT('Ctrl Pts',(-1.08085382696811,1.49747696130526,11.1554946319594));
#36574=CARTESIAN_POINT('Ctrl Pts',(-1.07159363370462,1.50451093778695,11.1550481251347));
#36575=CARTESIAN_POINT('Ctrl Pts',(-1.01611106549685,1.54665509923293,11.152372873695));
#36576=CARTESIAN_POINT('Ctrl Pts',(-0.958209601759993,1.58545013781557,
11.1497101571816));
#36577=CARTESIAN_POINT('Ctrl Pts',(-0.898278760372612,1.62088563165273,
11.1470556568828));
#36578=CARTESIAN_POINT('Ctrl Pts',(-0.837571419107242,1.65678024897295,
11.1443667632881));
#36579=CARTESIAN_POINT('Ctrl Pts',(-0.774780874239298,1.6892280755481,11.1416863001956));
#36580=CARTESIAN_POINT('Ctrl Pts',(-0.71027313016202,1.71817742298682,11.1390097788418));
#36581=CARTESIAN_POINT('Ctrl Pts',(-0.66261429365752,1.73956543207362,11.13703234349));
#36582=CARTESIAN_POINT('Ctrl Pts',(-0.614017264977652,1.75904301818697,
11.135057059686));
#36583=CARTESIAN_POINT('Ctrl Pts',(-0.56462073685077,1.77657345707156,11.1330821172509));
#36584=CARTESIAN_POINT('Ctrl Pts',(-0.539231747042784,1.78558380964183,
11.1320670298498));
#36585=CARTESIAN_POINT('Ctrl Pts',(-0.513631449727103,1.79407954038564,
11.1310520326313));
#36586=CARTESIAN_POINT('Ctrl Pts',(-0.487838223654543,1.802054170041,11.1300368798027));
#36587=CARTESIAN_POINT('Ctrl Pts',(-0.475799003301229,1.80577640018727,
11.1295630480858));
#36588=CARTESIAN_POINT('Ctrl Pts',(-0.463717747565173,1.80938508638487,
11.129089182467));
#36589=CARTESIAN_POINT('Ctrl Pts',(-0.451596312388482,1.81287949077367,
11.1286152579519));
#36590=CARTESIAN_POINT('Ctrl Pts',(-0.439480899976025,1.81637215890158,
11.1281415689151));
#36591=CARTESIAN_POINT('Ctrl Pts',(-0.427332434103985,1.81974856717366,
11.1276680985874));
#36592=CARTESIAN_POINT('Ctrl Pts',(-0.415160020480683,1.8230065701324,11.1271950974533));
#36593=CARTESIAN_POINT('Ctrl Pts',(-0.345659931193023,1.8416085913534,11.1244944316633));
#36594=CARTESIAN_POINT('Ctrl Pts',(-0.275309825422015,1.85637496302517,
11.1218062647546));
#36595=CARTESIAN_POINT('Ctrl Pts',(-0.204481476884407,1.86725830113956,
11.1191261497819));
#36596=CARTESIAN_POINT('Ctrl Pts',(-0.133579826115251,1.87815290272383,
11.1164432610836));
#36597=CARTESIAN_POINT('Ctrl Pts',(-0.0621979169225611,1.88515673586772,
11.1137684409964));
#36598=CARTESIAN_POINT('Ctrl Pts',(0.00930939936232982,1.88817434312463,
11.111097228754));
#36599=CARTESIAN_POINT('Ctrl Pts',(0.0795378313902503,1.89113798149254,
11.1084737902425));
#36600=CARTESIAN_POINT('Ctrl Pts',(0.149888204683991,1.89025686041538,11.1058538316796));
#36601=CARTESIAN_POINT('Ctrl Pts',(0.220026910137412,1.88539116319202,11.1032331273822));
#36602=CARTESIAN_POINT('Ctrl Pts',(0.236366392955163,1.88425765244837,11.1026226092302));
#36603=CARTESIAN_POINT('Ctrl Pts',(0.252694364144288,1.88290767750495,11.102012050607));
#36604=CARTESIAN_POINT('Ctrl Pts',(0.269006539233807,1.88133906123029,11.1014013980884));
#36605=CARTESIAN_POINT('Ctrl Pts',(0.280730896030037,1.88021162011471,11.1009624923038));
#36606=CARTESIAN_POINT('Ctrl Pts',(0.292446914187848,1.8789711508204,11.1005235443156));
#36607=CARTESIAN_POINT('Ctrl Pts',(0.304138944100939,1.87761870427971,11.1000850620809));
#36608=CARTESIAN_POINT('Ctrl Pts',(0.375822773838615,1.86932685519343,11.0973967277121));
#36609=CARTESIAN_POINT('Ctrl Pts',(0.446738242932316,1.85681796775178,11.0947208906731));
#36610=CARTESIAN_POINT('Ctrl Pts',(0.516529562716851,1.84000805096474,11.0920531719144));
#36611=CARTESIAN_POINT('Ctrl Pts',(0.584847521294231,1.82355300752536,11.0894417712386));
#36612=CARTESIAN_POINT('Ctrl Pts',(0.652089317501138,1.80297695165361,11.0868381496919));
#36613=CARTESIAN_POINT('Ctrl Pts',(0.718036401553849,1.77856692481578,11.084238199749));
#36614=CARTESIAN_POINT('Ctrl Pts',(0.785323202313169,1.75366100765569,11.0815854317561));
#36615=CARTESIAN_POINT('Ctrl Pts',(0.851262956271168,1.7247633139281,11.0789364860598));
#36616=CARTESIAN_POINT('Ctrl Pts',(0.915607648721953,1.6921267735849,11.0762869996812));
#36617=CARTESIAN_POINT('Ctrl Pts',(0.930631108062465,1.68450666199239,11.0756683868732));
#36618=CARTESIAN_POINT('Ctrl Pts',(0.945567515715628,1.67668252571399,11.0750497445899));
#36619=CARTESIAN_POINT('Ctrl Pts',(0.960413518624615,1.6686572293506,11.074431017298));
#36620=CARTESIAN_POINT('Ctrl Pts',(0.975205360081844,1.66066121101609,11.073814547258));
#36621=CARTESIAN_POINT('Ctrl Pts',(0.989912270604597,1.65246257743845,11.0731977870787));
#36622=CARTESIAN_POINT('Ctrl Pts',(1.00450295029956,1.6440805277344,11.0725818668126));
#36623=CARTESIAN_POINT('Ctrl Pts',(1.06739734574523,1.60794897253934,11.0699268888682));
#36624=CARTESIAN_POINT('Ctrl Pts',(1.12821828188749,1.56837054324493,11.0672840147147));
#36625=CARTESIAN_POINT('Ctrl Pts',(1.18673956352194,1.52565231730803,11.0646490274931));
#36626=CARTESIAN_POINT('Ctrl Pts',(1.24608357911593,1.48233352805146,11.0619769957398));
#36627=CARTESIAN_POINT('Ctrl Pts',(1.30306365724006,1.43578546725283,11.0593130742375));
#36628=CARTESIAN_POINT('Ctrl Pts',(1.35742307425591,1.38627866511896,11.056652865764));
#36629=CARTESIAN_POINT('Ctrl Pts',(1.41159294455999,1.3369444890372,11.0540019332135));
#36630=CARTESIAN_POINT('Ctrl Pts',(1.4631611896777,1.28467147000892,11.0513546878431));
#36631=CARTESIAN_POINT('Ctrl Pts',(1.51184108762766,1.22968809505141,11.0487067782687));
#36632=CARTESIAN_POINT('Ctrl Pts',(1.52842600119773,1.21095562929319,11.0478046532996));
#36633=CARTESIAN_POINT('Ctrl Pts',(1.54467532477781,1.19190827830405,11.0469024512351));
#36634=CARTESIAN_POINT('Ctrl Pts',(1.56057659382849,1.17255425406029,11.046));
#36635=CARTESIAN_POINT('',(-0.999999999999999,-1.22464679914735E-16,12.));
#36636=CARTESIAN_POINT('',(-1.5,-1.83697019872103E-16,11.5));
#36637=CARTESIAN_POINT('Origin',(0.,0.,12.));
#36638=CARTESIAN_POINT('Ctrl Pts',(1.13509973994371,-1.59049193030953,-0.230074082272069));
#36639=CARTESIAN_POINT('Ctrl Pts',(1.66385127640631,-1.21313337847033,-0.19303686544359));
#36640=CARTESIAN_POINT('Ctrl Pts',(2.30633516687349,0.103782615975306,-0.118962431786632));
#36641=CARTESIAN_POINT('Ctrl Pts',(1.16188988078006,1.99753850566951,-0.00785078130119459));
#36642=CARTESIAN_POINT('Ctrl Pts',(-1.04655428901899,2.05782953697956,0.103260869184242));
#36643=CARTESIAN_POINT('Ctrl Pts',(-2.29698075471667,0.238333788527267,
0.214372519669679));
#36644=CARTESIAN_POINT('Ctrl Pts',(-1.44613108848303,-1.80075271725216,
0.325484170155115));
#36645=CARTESIAN_POINT('Ctrl Pts',(0.727946961077783,-2.19149774367173,
0.436595820640553));
#36646=CARTESIAN_POINT('Ctrl Pts',(2.2359411788162,-0.57762978583554,0.547707471125989));
#36647=CARTESIAN_POINT('Ctrl Pts',(1.69827668332871,1.56494259322429,0.658819121611427));
#36648=CARTESIAN_POINT('Ctrl Pts',(-0.393188016825179,2.27560800163251,
0.769930772096863));
#36649=CARTESIAN_POINT('Ctrl Pts',(-2.12490816724285,0.90434536960108,0.881042422582301));
#36650=CARTESIAN_POINT('Ctrl Pts',(-1.9125222930514,-1.29434912039326,0.992154073067737));
#36651=CARTESIAN_POINT('Ctrl Pts',(0.0496630258143332,-2.30880650358359,
1.10326572355317));
#36652=CARTESIAN_POINT('Ctrl Pts',(1.96640931676781,-1.21090966106477,1.21437737403861));
#36653=CARTESIAN_POINT('Ctrl Pts',(2.08405785032279,0.994871990457256,1.32548902452405));
#36654=CARTESIAN_POINT('Ctrl Pts',(0.294968904732024,2.29042728261432,1.43660067500948));
#36655=CARTESIAN_POINT('Ctrl Pts',(-1.76399147035948,1.49043619583305,1.54771232549492));
#36656=CARTESIAN_POINT('Ctrl Pts',(-2.20904863824581,-0.673178902258552,
1.65882397598036));
#36657=CARTESIAN_POINT('Ctrl Pts',(-0.633012670336293,-2.22089176195486,
1.7699356264658));
#36658=CARTESIAN_POINT('Ctrl Pts',(1.52217643594786,-1.73667627565877,1.88104727695123));
#36659=CARTESIAN_POINT('Ctrl Pts',(2.28470258285089,0.336451535954383,1.99215892743667));
#36660=CARTESIAN_POINT('Ctrl Pts',(0.956918672404541,2.10175453516431,2.10327057792211));
#36661=CARTESIAN_POINT('Ctrl Pts',(-1.24636506047609,1.94412953698174,2.21438222840754));
#36662=CARTESIAN_POINT('Ctrl Pts',(-2.30932995110325,0.00779007092406014,
2.32549387889298));
#36663=CARTESIAN_POINT('Ctrl Pts',(-1.2594528285163,-1.93567664513544,2.43660552937842));
#36664=CARTESIAN_POINT('Ctrl Pts',(0.942717341349318,-2.1081625941051,2.54771717986386));
#36665=CARTESIAN_POINT('Ctrl Pts',(2.28238070382781,-0.351857683462,2.65882883034929));
#36666=CARTESIAN_POINT('Ctrl Pts',(1.53385834111148,1.72636731182735,2.76994048083473));
#36667=CARTESIAN_POINT('Ctrl Pts',(-0.618014955343493,2.22511191222357,
2.88105213132016));
#36668=CARTESIAN_POINT('Ctrl Pts',(-2.20445672440028,0.68806689849701,2.99216378180561));
#36669=CARTESIAN_POINT('Ctrl Pts',(-1.77400663329184,-1.47850125855229,
3.10327543229104));
#36670=CARTESIAN_POINT('Ctrl Pts',(0.279509811935462,-2.29236554058792,
3.21438708277648));
#36671=CARTESIAN_POINT('Ctrl Pts',(2.07729836817097,-1.00890881459812,3.32549873326191));
#36672=CARTESIAN_POINT('Ctrl Pts',(1.97453422882556,1.1976143309821,3.43661038374735));
#36673=CARTESIAN_POINT('Ctrl Pts',(0.0652379087403971,2.30842143506323,
3.54772203423278));
#36674=CARTESIAN_POINT('Ctrl Pts',(-1.90374559216213,1.30721774273047,3.65883368471823));
#36675=CARTESIAN_POINT('Ctrl Pts',(-2.13096254074055,-0.889979863001003,
3.76994533520366));
#36676=CARTESIAN_POINT('Ctrl Pts',(-0.408528604769679,-2.27292100295502,
3.8810569856891));
#36677=CARTESIAN_POINT('Ctrl Pts',(1.6876745272456,-1.57633124585981,3.99216863617453));
#36678=CARTESIAN_POINT('Ctrl Pts',(2.23979789625721,0.562468568463683,4.10328028665997));
#36679=CARTESIAN_POINT('Ctrl Pts',(0.742695215461042,2.18665711155622,4.21439193714541));
#36680=CARTESIAN_POINT('Ctrl Pts',(-1.43391090854028,1.81023893808443,4.32550358763085));
#36681=CARTESIAN_POINT('Ctrl Pts',(-2.29860956455329,-0.222395090620434,
4.43661523811628));
#36682=CARTESIAN_POINT('Ctrl Pts',(-1.06027445761331,-2.05155638019547,
4.54772688860172));
#36683=CARTESIAN_POINT('Ctrl Pts',(1.14812229735204,-2.00371672072451,4.65883853908716));
#36684=CARTESIAN_POINT('Ctrl Pts',(2.30608404475241,-0.122645363248325,
4.76995018957259));
#36685=CARTESIAN_POINT('Ctrl Pts',(1.35417351061808,1.87063615108022,4.88106184005803));
#36686=CARTESIAN_POINT('Ctrl Pts',(-0.83669150175529,2.1524434574405,4.99217349054346));
#36687=CARTESIAN_POINT('Ctrl Pts',(-2.26205440167697,0.464946653328952,
5.10328514102891));
#36688=CARTESIAN_POINT('Ctrl Pts',(-1.61782842764492,-1.64793709991974,
5.21439679151433));
#36689=CARTESIAN_POINT('Ctrl Pts',(0.506574022840452,-2.25309748257175,
5.32550844199978));
#36690=CARTESIAN_POINT('Ctrl Pts',(2.1675039941815,-0.796863816342033,5.43662009248521));
#36691=CARTESIAN_POINT('Ctrl Pts',(1.84535073495005,1.38843299139974,5.54773174297065));
#36692=CARTESIAN_POINT('Ctrl Pts',(-0.1651427104253,2.30343078727826,5.65884339345609));
#36693=CARTESIAN_POINT('Ctrl Pts',(-2.024544512798,1.1109838082922,5.76995504394152));
#36694=CARTESIAN_POINT('Ctrl Pts',(-2.03165894515671,-1.09791959503082,
5.88106669442697));
#36695=CARTESIAN_POINT('Ctrl Pts',(-0.179976902307884,-2.30231922661119,
5.99217834491239));
#36696=CARTESIAN_POINT('Ctrl Pts',(1.83636881720094,-1.40029106752845,6.10328999539785));
#36697=CARTESIAN_POINT('Ctrl Pts',(2.17259204728728,0.782885242326115,6.21440164588326));
#36698=CARTESIAN_POINT('Ctrl Pts',(0.521076907609949,2.24978762618687,6.32551329636872));
#36699=CARTESIAN_POINT('Ctrl Pts',(-1.60717962682088,1.6583242004264,6.43662494685413));
#36700=CARTESIAN_POINT('Ctrl Pts',(-2.26500243885858,-0.450365916286509,
6.5477365973396));
#36701=CARTESIAN_POINT('Ctrl Pts',(-0.850539171717745,-2.14700922773088,
6.65884824782501));
#36702=CARTESIAN_POINT('Ctrl Pts',(1.34209565723166,-1.87932029027199,6.76995989831046));
#36703=CARTESIAN_POINT('Ctrl Pts',(2.30682622449346,0.107788109627418,6.8810715487959));
#36704=CARTESIAN_POINT('Ctrl Pts',(1.16100547839306,1.99627948587589,6.99218319928133));
#36705=CARTESIAN_POINT('Ctrl Pts',(-1.04703729866327,2.05834360634882,7.10329484976677));
#36706=CARTESIAN_POINT('Ctrl Pts',(-2.29712931099768,0.237197038645086,
7.21440650025221));
#36707=CARTESIAN_POINT('Ctrl Pts',(-1.44554186745893,-1.80096480143545,
7.32551815073763));
#36708=CARTESIAN_POINT('Ctrl Pts',(0.72859438989827,-2.19139583863915,7.43662980122308));
#36709=CARTESIAN_POINT('Ctrl Pts',(2.23612826941383,-0.576884623911715,
7.5477414517085));
#36710=CARTESIAN_POINT('Ctrl Pts',(1.6977934979946,1.56542733614398,7.65885310219396));
#36711=CARTESIAN_POINT('Ctrl Pts',(-0.393879040694563,2.27550539615811,
7.76996475267938));
#36712=CARTESIAN_POINT('Ctrl Pts',(-2.12518549811472,0.903688057410859,
7.88107640316484));
#36713=CARTESIAN_POINT('Ctrl Pts',(-1.91212657747833,-1.29492758803799,
7.99218805365025));
#36714=CARTESIAN_POINT('Ctrl Pts',(0.0503667898133586,-2.30879377455661,
8.1032997041357));
#36715=CARTESIAN_POINT('Ctrl Pts',(1.96677879493939,-1.21030850518371,8.21441135462113));
#36716=CARTESIAN_POINT('Ctrl Pts',(2.08375418707704,0.995506903268707,8.32552300510658));
#36717=CARTESIAN_POINT('Ctrl Pts',(0.294270353677539,2.29051751091564,8.436634655592));
#36718=CARTESIAN_POINT('Ctrl Pts',(-1.76444601777748,1.4898978999011,8.54774630607746));
#36719=CARTESIAN_POINT('Ctrl Pts',(-2.2088431932234,-0.673852547682493,
8.65885795656288));
#36720=CARTESIAN_POINT('Ctrl Pts',(-0.632335256349382,-2.2210847899434,
8.76996960704833));
#36721=CARTESIAN_POINT('Ctrl Pts',(1.52270606837662,-1.73621188252162,8.88108125753376));
#36722=CARTESIAN_POINT('Ctrl Pts',(2.28459985995541,0.337148347205355,8.99219290801919));
#36723=CARTESIAN_POINT('Ctrl Pts',(0.956277562497704,2.10204633917866,9.10330455850463));
#36724=CARTESIAN_POINT('Ctrl Pts',(-1.2469579560031,1.94374924182257,9.21441620899007));
#36725=CARTESIAN_POINT('Ctrl Pts',(-2.30933226540692,0.00708579792413808,
9.32552785947551));
#36726=CARTESIAN_POINT('Ctrl Pts',(-1.25886228368054,-1.93606087509586,
9.43663950996094));
#36727=CARTESIAN_POINT('Ctrl Pts',(0.943360139257667,-2.10787462610152,
9.54775116044639));
#36728=CARTESIAN_POINT('Ctrl Pts',(2.28248823506631,-0.351162152961091,
9.65886281093181));
#36729=CARTESIAN_POINT('Ctrl Pts',(1.53333110744206,1.72683627576032,9.76997446141726));
#36730=CARTESIAN_POINT('Ctrl Pts',(-0.618692454411617,2.22492101746939,
9.88108611190268));
#36731=CARTESIAN_POINT('Ctrl Pts',(-2.20466868021367,0.687398848825245,
9.99219776238814));
#36732=CARTESIAN_POINT('Ctrl Pts',(-1.7735514221838,-1.47905058047522,10.1033094128735));
#36733=CARTESIAN_POINT('Ctrl Pts',(0.280201048116106,-2.29226437530741,
10.214421063359));
#36734=CARTESIAN_POINT('Ctrl Pts',(2.07762111854432,-1.0083052618152,10.3255327138444));
#36735=CARTESIAN_POINT('Ctrl Pts',(1.97414006873683,1.19827380577986,10.4366443643299));
#36736=CARTESIAN_POINT('Ctrl Pts',(0.0645886152005097,2.30833217918201,
10.5477560148153));
#36737=CARTESIAN_POINT('Ctrl Pts',(-1.90424854748374,1.30684465150768,10.6588676653008));
#36738=CARTESIAN_POINT('Ctrl Pts',(-2.13049227679005,-0.891025387309722,
10.7699793157862));
#36739=CARTESIAN_POINT('Ctrl Pts',(-0.408214485225542,-2.27228942196666,
10.8810909662716));
#36740=CARTESIAN_POINT('Ctrl Pts',(1.68888461736298,-1.5772814986318,10.9922026167571));
#36741=CARTESIAN_POINT('Ctrl Pts',(2.23817187934597,0.566161966084782,11.1033142672425));
#36742=CARTESIAN_POINT('Ctrl Pts',(1.24300218570944,1.64165746435707,11.1773887008995));
#36743=CARTESIAN_POINT('Ctrl Pts',(0.627850911123727,1.850383536838,11.2144259177279));
#36744=CARTESIAN_POINT('Ctrl Pts',(1.05793541951254,-1.4823699524473,-0.153382721514713));
#36745=CARTESIAN_POINT('Ctrl Pts',(1.55074231467859,-1.13066431478549,-0.116345504686234));
#36746=CARTESIAN_POINT('Ctrl Pts',(2.14955001436596,0.0967274517879858,
-0.0422710710292769));
#36747=CARTESIAN_POINT('Ctrl Pts',(1.08290436090784,1.86174541551099,0.0688405794561606));
#36748=CARTESIAN_POINT('Ctrl Pts',(-0.975409307071879,1.91793784975909,
0.179952229941597));
#36749=CARTESIAN_POINT('Ctrl Pts',(-2.14083151712633,0.22213180716797,0.291063880427034));
#36750=CARTESIAN_POINT('Ctrl Pts',(-1.34782279118508,-1.67833716661673,
0.402175530912471));
#36751=CARTESIAN_POINT('Ctrl Pts',(0.678460972679723,-2.04251926348523,
0.513287181397908));
#36752=CARTESIAN_POINT('Ctrl Pts',(2.08394142450739,-0.538362390807298,
0.624398831883346));
#36753=CARTESIAN_POINT('Ctrl Pts',(1.58282747515632,1.45855746470163,0.735510482368781));
#36754=CARTESIAN_POINT('Ctrl Pts',(-0.366459012269607,2.12091168831785,
0.84662213285422));
#36755=CARTESIAN_POINT('Ctrl Pts',(-1.98045646054783,0.842867780077688,
0.957733783339656));
#36756=CARTESIAN_POINT('Ctrl Pts',(-1.78250862301028,-1.20635899339281,
1.06884543382509));
#36757=CARTESIAN_POINT('Ctrl Pts',(0.0462869228141735,-2.15185334908375,
1.17995708431053));
#36758=CARTESIAN_POINT('Ctrl Pts',(1.83273239545565,-1.12859176615955,1.29106873479597));
#36759=CARTESIAN_POINT('Ctrl Pts',(1.94238315681312,0.927240382098824,1.4021803852814));
#36760=CARTESIAN_POINT('Ctrl Pts',(0.274916856192995,2.13472355144377,1.51329203576684));
#36761=CARTESIAN_POINT('Ctrl Pts',(-1.64407495706399,1.38911602796551,1.62440368625228));
#36762=CARTESIAN_POINT('Ctrl Pts',(-2.0588770445336,-0.62741605808422,1.73551533673771));
#36763=CARTESIAN_POINT('Ctrl Pts',(-0.589980335104445,-2.06991507018771,
1.84662698722315));
#36764=CARTESIAN_POINT('Ctrl Pts',(1.41869855984326,-1.61861665507704,1.95773863770859));
#36765=CARTESIAN_POINT('Ctrl Pts',(2.1293880179812,0.313579489369987,2.06885028819403));
#36766=CARTESIAN_POINT('Ctrl Pts',(0.891867138635642,1.95887681727571,2.17996193867946));
#36767=CARTESIAN_POINT('Ctrl Pts',(-1.16163690001897,1.8119671998123,2.2910735891649));
#36768=CARTESIAN_POINT('Ctrl Pts',(-2.1523412125303,0.0072605002547781,
2.40218523965033));
#36769=CARTESIAN_POINT('Ctrl Pts',(-1.1738349588193,-1.80408893734178,2.51329689013577));
#36770=CARTESIAN_POINT('Ctrl Pts',(0.878631217069615,-1.96484925501419,
2.62440854062121));
#36771=CARTESIAN_POINT('Ctrl Pts',(2.12722398078527,-0.327938323711113,
2.73552019110664));
#36772=CARTESIAN_POINT('Ctrl Pts',(1.42958632662274,1.60900849678758,2.84663184159209));
#36773=CARTESIAN_POINT('Ctrl Pts',(-0.57600216794938,2.07384833374845,2.95774349207752));
#36774=CARTESIAN_POINT('Ctrl Pts',(-2.05459728996263,0.641291965189069,
3.06885514256296));
#36775=CARTESIAN_POINT('Ctrl Pts',(-1.65340928710165,-1.37799243024573,
3.17996679304839));
#36776=CARTESIAN_POINT('Ctrl Pts',(0.260508675794864,-2.13653004623031,
3.29107844353384));
#36777=CARTESIAN_POINT('Ctrl Pts',(1.93608318568785,-0.940322979965331,
3.40219009401926));
#36778=CARTESIAN_POINT('Ctrl Pts',(1.84030497427301,1.11620025542831,3.51330174450471));
#36779=CARTESIAN_POINT('Ctrl Pts',(0.0608030219043116,2.15149445760286,
3.62441339499014));
#36780=CARTESIAN_POINT('Ctrl Pts',(-1.77432856410404,1.21835280406139,3.73552504547559));
#36781=CARTESIAN_POINT('Ctrl Pts',(-1.98609925645444,-0.829478843655077,
3.84663669596101));
#36782=CARTESIAN_POINT('Ctrl Pts',(-0.380756743800589,-2.11840735237885,
3.95774834644646));
#36783=CARTESIAN_POINT('Ctrl Pts',(1.57294605588646,-1.4691719143219,4.06885999693188));
#36784=CARTESIAN_POINT('Ctrl Pts',(2.08753596148093,0.524231836199493,4.17997164741733));
#36785=CARTESIAN_POINT('Ctrl Pts',(0.692206637610257,2.03800769856489,4.29108329790276));
#36786=CARTESIAN_POINT('Ctrl Pts',(-1.33643334165982,1.68717851215016,4.4021949483882));
#36787=CARTESIAN_POINT('Ctrl Pts',(-2.1423496001257,-0.207276625316418,
4.51330659887364));
#36788=CARTESIAN_POINT('Ctrl Pts',(-0.988196775702872,-1.91209114350017,
4.62441824935908));
#36789=CARTESIAN_POINT('Ctrl Pts',(1.07007270071357,-1.86750363419964,4.73552989984451));
#36790=CARTESIAN_POINT('Ctrl Pts',(2.1493159635798,-0.11430790551128,4.84664155032995));
#36791=CARTESIAN_POINT('Ctrl Pts',(1.26211650891535,1.74346990983058,4.95775320081538));
#36792=CARTESIAN_POINT('Ctrl Pts',(-0.779813036479037,2.00611989589323,
5.06886485130082));
#36793=CARTESIAN_POINT('Ctrl Pts',(-2.1082794649543,0.433339481484583,5.17997650178626));
#36794=CARTESIAN_POINT('Ctrl Pts',(-1.50784810891129,-1.53590998727594,
5.29108815227169));
#36795=CARTESIAN_POINT('Ctrl Pts',(0.472137013611209,-2.09993143910453,
5.40219980275713));
#36796=CARTESIAN_POINT('Ctrl Pts',(2.02015661416081,-0.742692845544967,
5.51331145324257));
#36797=CARTESIAN_POINT('Ctrl Pts',(1.71990340163759,1.29404702294652,5.62442310372801));
#36798=CARTESIAN_POINT('Ctrl Pts',(-0.153916274037652,2.14684307510999,
5.73553475421344));
#36799=CARTESIAN_POINT('Ctrl Pts',(-1.88691554856225,1.03545889399597,5.84664640469888));
#36800=CARTESIAN_POINT('Ctrl Pts',(-1.89354634030427,-1.02328278871562,
5.95775805518432));
#36801=CARTESIAN_POINT('Ctrl Pts',(-0.167742034418123,-2.1458070785722,
6.06886970566975));
#36802=CARTESIAN_POINT('Ctrl Pts',(1.71153207655705,-1.30509898455162,6.1799813561552));
#36803=CARTESIAN_POINT('Ctrl Pts',(2.02489878034016,0.729664537947597,6.29109300664062));
#36804=CARTESIAN_POINT('Ctrl Pts',(0.485653989206222,2.09684658745684,6.40220465712607));
#36805=CARTESIAN_POINT('Ctrl Pts',(-1.49792321581985,1.54559097049293,6.5133163076115));
#36806=CARTESIAN_POINT('Ctrl Pts',(-2.11102709394471,-0.41974994603061,
6.62442795809694));
#36807=CARTESIAN_POINT('Ctrl Pts',(-0.79271933890819,-2.0010550862688,6.73553960858237));
#36808=CARTESIAN_POINT('Ctrl Pts',(1.25085971055702,-1.7515636994031,6.84665125906781));
#36809=CARTESIAN_POINT('Ctrl Pts',(2.15000768978506,0.100460651134341,6.95776290955325));
#36810=CARTESIAN_POINT('Ctrl Pts',(1.08208008038219,1.86057198414926,7.06887456003868));
#36811=CARTESIAN_POINT('Ctrl Pts',(-0.975859481618359,1.91841697258389,
7.17998621052413));
#36812=CARTESIAN_POINT('Ctrl Pts',(-2.14096997451993,0.221072333783236,
7.29109786100956));
#36813=CARTESIAN_POINT('Ctrl Pts',(-1.34727362553083,-1.67853483327237,
7.402209511495));
#36814=CARTESIAN_POINT('Ctrl Pts',(0.679064389152043,-2.04242428597833,
7.51332116198043));
#36815=CARTESIAN_POINT('Ctrl Pts',(2.08411579664662,-0.537667885148679,
7.62443281246587));
#36816=CARTESIAN_POINT('Ctrl Pts',(1.58237713686343,1.4590092546951,7.73554446295131));
#36817=CARTESIAN_POINT('Ctrl Pts',(-0.367103060190181,2.1208160579853,7.84665611343674));
#36818=CARTESIAN_POINT('Ctrl Pts',(-1.98071493840836,0.842255152109201,
7.95776776392219));
#36819=CARTESIAN_POINT('Ctrl Pts',(-1.78213980826558,-1.20689813668469,
8.0688794144076));
#36820=CARTESIAN_POINT('Ctrl Pts',(0.0469428447876819,-2.15184148537872,
8.17999106489306));
#36821=CARTESIAN_POINT('Ctrl Pts',(1.83307675642296,-1.12803147698245,8.29110271537848));
#36822=CARTESIAN_POINT('Ctrl Pts',(1.94210013665906,0.927832133403047,8.40221436586394));
#36823=CARTESIAN_POINT('Ctrl Pts',(0.274265792786954,2.13480764600607,8.51332601634936));
#36824=CARTESIAN_POINT('Ctrl Pts',(-1.64449860425235,1.38861432550488,8.6244376668348));
#36825=CARTESIAN_POINT('Ctrl Pts',(-2.05868556570727,-0.628043908949741,
8.73554931732024));
#36826=CARTESIAN_POINT('Ctrl Pts',(-0.589348971863656,-2.07009497609277,
8.84666096780567));
#36827=CARTESIAN_POINT('Ctrl Pts',(1.41919218774748,-1.61818383148359,8.95777261829112));
#36828=CARTESIAN_POINT('Ctrl Pts',(2.12929227820989,0.314228931244718,9.06888426877654));
#36829=CARTESIAN_POINT('Ctrl Pts',(0.891269611515884,1.95914878439144,9.179995919262));
#36830=CARTESIAN_POINT('Ctrl Pts',(-1.16218949038264,1.81161275719849,9.29110756974741));
#36831=CARTESIAN_POINT('Ctrl Pts',(-2.15234336950711,0.00660410388236847,
9.40221922023287));
#36832=CARTESIAN_POINT('Ctrl Pts',(-1.17328455934639,-1.80444704726821,
9.51333087071829));
#36833=CARTESIAN_POINT('Ctrl Pts',(0.879230317440182,-1.96458086313641,
9.62444252120374));
#36834=CARTESIAN_POINT('Ctrl Pts',(2.12732420202743,-0.327290075520782,
9.73555417168917));
#36835=CARTESIAN_POINT('Ctrl Pts',(1.42909493440969,1.60944558045319,9.8466658221746));
#36836=CARTESIAN_POINT('Ctrl Pts',(-0.576633610487541,2.07367041606005,
9.95777747266004));
#36837=CARTESIAN_POINT('Ctrl Pts',(-2.05479483697499,0.640669329675303,
10.0688891231455));
#36838=CARTESIAN_POINT('Ctrl Pts',(-1.65298502134104,-1.37850440914814,
10.1800007736309));
#36839=CARTESIAN_POINT('Ctrl Pts',(0.26115292159373,-2.13643575818697,10.2911124241164));
#36840=CARTESIAN_POINT('Ctrl Pts',(1.93638399542254,-0.939760456828254,
10.4022240746018));
#36841=CARTESIAN_POINT('Ctrl Pts',(1.83993760927049,1.11681489898982,10.5133357250872));
#36842=CARTESIAN_POINT('Ctrl Pts',(0.0601978674766102,2.15141126935532,
10.6244473755726));
#36843=CARTESIAN_POINT('Ctrl Pts',(-1.77479732841649,1.21800507565884,10.7355590260581));
#36844=CARTESIAN_POINT('Ctrl Pts',(-1.98566096114678,-0.830453293000129,
10.8466706765435));
#36845=CARTESIAN_POINT('Ctrl Pts',(-0.380463978169507,-2.11781870639967,
10.957782327029));
#36846=CARTESIAN_POINT('Ctrl Pts',(1.57407388382168,-1.47005756870945,11.0688939775144));
#36847=CARTESIAN_POINT('Ctrl Pts',(2.08602048154327,0.527674155869038,11.1800056279999));
#36848=CARTESIAN_POINT('Ctrl Pts',(1.15850263419028,1.53005724266717,11.2540800616568));
#36849=CARTESIAN_POINT('Ctrl Pts',(0.585169473375027,1.72459407258861,11.2911172784853));
#36850=CARTESIAN_POINT('Ctrl Pts',(0.980771099081375,-1.37424797458507,
-0.0766913607573581));
#36851=CARTESIAN_POINT('Ctrl Pts',(1.43763335295088,-1.04819525110066,-0.0396541439288791));
#36852=CARTESIAN_POINT('Ctrl Pts',(1.99276486185844,0.089672287600667,0.0344202897280782));
#36853=CARTESIAN_POINT('Ctrl Pts',(1.00391884103562,1.72595232535247,0.145531940213516));
#36854=CARTESIAN_POINT('Ctrl Pts',(-0.904264325124765,1.77804616253862,
0.256643590698952));
#36855=CARTESIAN_POINT('Ctrl Pts',(-1.98468227953599,0.20592982580867,0.36775524118439));
#36856=CARTESIAN_POINT('Ctrl Pts',(-1.24951449388714,-1.55592161598129,
0.478866891669827));
#36857=CARTESIAN_POINT('Ctrl Pts',(0.628974984281669,-1.89354078329874,
0.589978542155263));
#36858=CARTESIAN_POINT('Ctrl Pts',(1.93194167019859,-0.499094995779056,
0.7010901926407));
#36859=CARTESIAN_POINT('Ctrl Pts',(1.46737826698393,1.35217233617898,0.812201843126137));
#36860=CARTESIAN_POINT('Ctrl Pts',(-0.339730007714042,1.96621537500318,
0.923313493611574));
#36861=CARTESIAN_POINT('Ctrl Pts',(-1.8360047538528,0.7813901905543,1.03442514409701));
#36862=CARTESIAN_POINT('Ctrl Pts',(-1.65249495296916,-1.11836886639236,
1.14553679458245));
#36863=CARTESIAN_POINT('Ctrl Pts',(0.0429108198140191,-1.99490019458391,
1.25664844506789));
#36864=CARTESIAN_POINT('Ctrl Pts',(1.69905547414348,-1.04627387125433,1.36776009555332));
#36865=CARTESIAN_POINT('Ctrl Pts',(1.80070846330345,0.859608773740392,1.47887174603876));
#36866=CARTESIAN_POINT('Ctrl Pts',(0.254864807653961,1.97901982027321,1.5899833965242));
#36867=CARTESIAN_POINT('Ctrl Pts',(-1.52415844376849,1.28779586009797,1.70109504700963));
#36868=CARTESIAN_POINT('Ctrl Pts',(-1.90870545082139,-0.581653213909888,
1.81220669749507));
#36869=CARTESIAN_POINT('Ctrl Pts',(-0.546947999872595,-1.91893837842057,
1.92331834798051));
#36870=CARTESIAN_POINT('Ctrl Pts',(1.31522068373867,-1.50055703449532,2.03442999846594));
#36871=CARTESIAN_POINT('Ctrl Pts',(1.97407345311151,0.290707442785592,2.14554164895138));
#36872=CARTESIAN_POINT('Ctrl Pts',(0.826815604866742,1.81599909938712,2.25665329943681));
#36873=CARTESIAN_POINT('Ctrl Pts',(-1.07690873956185,1.67980486264285,2.36776494992226));
#36874=CARTESIAN_POINT('Ctrl Pts',(-1.99535247395734,0.00673092958549589,
2.47887660040769));
#36875=CARTESIAN_POINT('Ctrl Pts',(-1.0882170891223,-1.67250122954812,2.58998825089313));
#36876=CARTESIAN_POINT('Ctrl Pts',(0.814545092789914,-1.82153591592328,
2.70109990137857));
#36877=CARTESIAN_POINT('Ctrl Pts',(1.97206725774273,-0.304018963960226,
2.812211551864));
#36878=CARTESIAN_POINT('Ctrl Pts',(1.325314312134,1.49164968174781,2.92332320234944));
#36879=CARTESIAN_POINT('Ctrl Pts',(-0.533989380555266,1.92258475527334,
3.03443485283487));
#36880=CARTESIAN_POINT('Ctrl Pts',(-1.90473785552499,0.594517031881129,
3.14554650332031));
#36881=CARTESIAN_POINT('Ctrl Pts',(-1.53281194091147,-1.27748360193918,
3.25665815380575));
#36882=CARTESIAN_POINT('Ctrl Pts',(0.241507539654265,-1.98069455187271,
3.36776980429119));
#36883=CARTESIAN_POINT('Ctrl Pts',(1.79486800320472,-0.871737145332536,
3.47888145477662));
#36884=CARTESIAN_POINT('Ctrl Pts',(1.70607571972046,1.03478617987453,3.58999310526206));
#36885=CARTESIAN_POINT('Ctrl Pts',(0.0563681350682242,1.99456748014249,
3.7011047557475));
#36886=CARTESIAN_POINT('Ctrl Pts',(-1.64491153604594,1.1294878653923,3.81221640623293));
#36887=CARTESIAN_POINT('Ctrl Pts',(-1.84123597216834,-0.768977824309152,
3.92332805671837));
#36888=CARTESIAN_POINT('Ctrl Pts',(-0.352984882831497,-1.96389370180267,
4.03443970720381));
#36889=CARTESIAN_POINT('Ctrl Pts',(1.45821758452731,-1.36201258278399,4.14555135768924));
#36890=CARTESIAN_POINT('Ctrl Pts',(1.93527402670466,0.485995103935303,4.25666300817468));
#36891=CARTESIAN_POINT('Ctrl Pts',(0.641718059759468,1.88935828557357,4.36777465866012));
#36892=CARTESIAN_POINT('Ctrl Pts',(-1.23895577477937,1.56411808621589,4.47888630914555));
#36893=CARTESIAN_POINT('Ctrl Pts',(-1.98608963569812,-0.1921581600124,4.58999795963099));
#36894=CARTESIAN_POINT('Ctrl Pts',(-0.916119093792434,-1.77262590680487,
4.70110961011643));
#36895=CARTESIAN_POINT('Ctrl Pts',(0.992023104075105,-1.73129054767478,
4.81222126060186));
#36896=CARTESIAN_POINT('Ctrl Pts',(1.99254788240719,-0.105970447774237,
4.9233329110873));
#36897=CARTESIAN_POINT('Ctrl Pts',(1.17005950721263,1.61630366858093,5.03444456157274));
#36898=CARTESIAN_POINT('Ctrl Pts',(-0.722934571202785,1.85979633434597,
5.14555621205818));
#36899=CARTESIAN_POINT('Ctrl Pts',(-1.95450452823164,0.401732309640217,
5.25666786254361));
#36900=CARTESIAN_POINT('Ctrl Pts',(-1.39786779017765,-1.42388287463214,
5.36777951302905));
#36901=CARTESIAN_POINT('Ctrl Pts',(0.437700004381964,-1.9467653956373,5.47889116351449));
#36902=CARTESIAN_POINT('Ctrl Pts',(1.87280923414012,-0.688521874747905,
5.59000281399993));
#36903=CARTESIAN_POINT('Ctrl Pts',(1.59445606832513,1.19966105449332,5.70111446448536));
#36904=CARTESIAN_POINT('Ctrl Pts',(-0.142689837650004,1.99025536294172,
5.81222611497081));
#36905=CARTESIAN_POINT('Ctrl Pts',(-1.74928658432651,0.959933979699734,
5.92333776545623));
#36906=CARTESIAN_POINT('Ctrl Pts',(-1.75543373545183,-0.948645982400418,
6.03444941594168));
#36907=CARTESIAN_POINT('Ctrl Pts',(-0.155507166528361,-1.98929493053321,
6.1455610664271));
#36908=CARTESIAN_POINT('Ctrl Pts',(1.58669533591315,-1.20990690157479,6.25667271691256));
#36909=CARTESIAN_POINT('Ctrl Pts',(1.87720551339304,0.676443833569079,6.36778436739797));
#36910=CARTESIAN_POINT('Ctrl Pts',(0.450231070802491,1.94390554872681,6.47889601788343));
#36911=CARTESIAN_POINT('Ctrl Pts',(-1.38866680481881,1.43285774055946,6.59000766836885));
#36912=CARTESIAN_POINT('Ctrl Pts',(-1.95705174903083,-0.38913397577471,
6.7011193188543));
#36913=CARTESIAN_POINT('Ctrl Pts',(-0.734899506098636,-1.85510094480672,
6.81223096933973));
#36914=CARTESIAN_POINT('Ctrl Pts',(1.15962376388238,-1.62380710853421,6.92334261982516));
#36915=CARTESIAN_POINT('Ctrl Pts',(1.99318915507666,0.0931331926412601,
7.03445427031061));
#36916=CARTESIAN_POINT('Ctrl Pts',(1.00315468237132,1.72486448242263,7.14556592079604));
#36917=CARTESIAN_POINT('Ctrl Pts',(-0.904681664573454,1.77849033881895,
7.25667757128148));
#36918=CARTESIAN_POINT('Ctrl Pts',(-1.98481063804218,0.204947628921387,
7.36778922176691));
#36919=CARTESIAN_POINT('Ctrl Pts',(-1.24900538360275,-1.55610486510929,
7.47890087225236));
#36920=CARTESIAN_POINT('Ctrl Pts',(0.629534388405818,-1.89345273331751,
7.59001252273779));
#36921=CARTESIAN_POINT('Ctrl Pts',(1.93210332387941,-0.498451146385645,
7.70112417322323));
#36922=CARTESIAN_POINT('Ctrl Pts',(1.46696077573226,1.35259117324623,7.81223582370866));
#36923=CARTESIAN_POINT('Ctrl Pts',(-0.340327079685797,1.96612671981249,
7.9233474741941));
#36924=CARTESIAN_POINT('Ctrl Pts',(-1.836244378702,0.780822246807544,8.03445912467955));
#36925=CARTESIAN_POINT('Ctrl Pts',(-1.65215303905282,-1.11886868533138,
8.14557077516496));
#36926=CARTESIAN_POINT('Ctrl Pts',(0.0435188997620014,-1.99488919620082,
8.25668242565042));
#36927=CARTESIAN_POINT('Ctrl Pts',(1.69937471790653,-1.04575444878119,8.36779407613584));
#36928=CARTESIAN_POINT('Ctrl Pts',(1.80044608624107,0.860157363537389,8.47890572662129));
#36929=CARTESIAN_POINT('Ctrl Pts',(0.254261231896373,1.97909778109651,8.59001737710672));
#36930=CARTESIAN_POINT('Ctrl Pts',(-1.52455119072723,1.28733075110866,8.70112902759215));
#36931=CARTESIAN_POINT('Ctrl Pts',(-1.90852793819114,-0.58223527021699,
8.8122406780776));
#36932=CARTESIAN_POINT('Ctrl Pts',(-0.546362687377931,-1.91910516224214,
8.92335232856302));
#36933=CARTESIAN_POINT('Ctrl Pts',(1.31567830711834,-1.50015578044556,9.03446397904849));
#36934=CARTESIAN_POINT('Ctrl Pts',(1.97398469646436,0.291309515284085,9.14557562953389));
#36935=CARTESIAN_POINT('Ctrl Pts',(0.826261660534066,1.81625122960423,9.25668728001935));
#36936=CARTESIAN_POINT('Ctrl Pts',(-1.07742102476217,1.67947627257441,9.36779893050478));
#36937=CARTESIAN_POINT('Ctrl Pts',(-1.99535447360731,0.00612240984059651,
9.47891058099021));
#36938=CARTESIAN_POINT('Ctrl Pts',(-1.08770683501224,-1.67283321944057,
9.59002223147566));
#36939=CARTESIAN_POINT('Ctrl Pts',(0.815100495622697,-1.82128710017129,
9.70113388196108));
#36940=CARTESIAN_POINT('Ctrl Pts',(1.97216016898856,-0.303417998080474,
9.81224553244654));
#36941=CARTESIAN_POINT('Ctrl Pts',(1.32485876137733,1.49205488514605,9.92335718293196));
#36942=CARTESIAN_POINT('Ctrl Pts',(-0.534574766563464,1.9224198146507,10.0344688334174));
#36943=CARTESIAN_POINT('Ctrl Pts',(-1.90492099373632,0.593939810525364,
10.1455804839028));
#36944=CARTESIAN_POINT('Ctrl Pts',(-1.53241862049827,-1.27795823782107,
10.2566921343883));
#36945=CARTESIAN_POINT('Ctrl Pts',(0.242104795071353,-1.98060714106653,
10.3678037848737));
#36946=CARTESIAN_POINT('Ctrl Pts',(1.79514687230076,-0.871215651841315,
10.4789154353591));
#36947=CARTESIAN_POINT('Ctrl Pts',(1.70573514980415,1.03535599219979,10.5900270858446));
#36948=CARTESIAN_POINT('Ctrl Pts',(0.055807119752709,1.99449035952863,10.70113873633));
#36949=CARTESIAN_POINT('Ctrl Pts',(-1.64534610934924,1.12916549981001,10.8122503868155));
#36950=CARTESIAN_POINT('Ctrl Pts',(-1.84082964550351,-0.769881198690536,
10.9233620373009));
#36951=CARTESIAN_POINT('Ctrl Pts',(-0.352713471113472,-1.96334799083268,
11.0344736877863));
#36952=CARTESIAN_POINT('Ctrl Pts',(1.45926315028039,-1.36283363878709,11.1455853382718));
#36953=CARTESIAN_POINT('Ctrl Pts',(1.93386908374058,0.489186345653294,11.2566969887572));
#36954=CARTESIAN_POINT('Ctrl Pts',(1.07400308267113,1.41845702097726,11.3307714224142));
#36955=CARTESIAN_POINT('Ctrl Pts',(0.542488035626326,1.59880460833922,11.3678086392426));
#36956=CARTESIAN_POINT('Ctrl Pts',(0.903606778650208,-1.26612599672284,
-2.77555756156289E-15));
#36957=CARTESIAN_POINT('Ctrl Pts',(1.32452439122316,-0.965726187415828,
0.0370372168284762));
#36958=CARTESIAN_POINT('Ctrl Pts',(1.83597970935092,0.0826171234133487,
0.111111650485434));
#36959=CARTESIAN_POINT('Ctrl Pts',(0.924933321163406,1.59015923519395,0.222223300970871));
#36960=CARTESIAN_POINT('Ctrl Pts',(-0.833119343177651,1.63815447531815,
0.333334951456308));
#36961=CARTESIAN_POINT('Ctrl Pts',(-1.82853304194564,0.18972784444937,0.444446601941745));
#36962=CARTESIAN_POINT('Ctrl Pts',(-1.15120619658919,-1.43350606534586,
0.555558252427182));
#36963=CARTESIAN_POINT('Ctrl Pts',(0.579488995883613,-1.74456230311225,
0.666669902912619));
#36964=CARTESIAN_POINT('Ctrl Pts',(1.77994191588978,-0.459827600750814,
0.777781553398056));
#36965=CARTESIAN_POINT('Ctrl Pts',(1.35192905881154,1.24578720765632,0.888893203883492));
#36966=CARTESIAN_POINT('Ctrl Pts',(-0.313001003158473,1.81151906168851,
1.00000485436893));
#36967=CARTESIAN_POINT('Ctrl Pts',(-1.69155304715778,0.719912601030908,
1.11111650485437));
#36968=CARTESIAN_POINT('Ctrl Pts',(-1.52248128292804,-1.03037873939191,
1.2222281553398));
#36969=CARTESIAN_POINT('Ctrl Pts',(0.0395347168138628,-1.83794704008407,
1.33333980582524));
#36970=CARTESIAN_POINT('Ctrl Pts',(1.56537855283131,-0.963955976349113,
1.44445145631068));
#36971=CARTESIAN_POINT('Ctrl Pts',(1.65903376979378,0.791977165381959,1.55556310679611));
#36972=CARTESIAN_POINT('Ctrl Pts',(0.234812759114929,1.82331608910266,1.66667475728155));
#36973=CARTESIAN_POINT('Ctrl Pts',(-1.404241930473,1.18647569223042,1.77778640776699));
#36974=CARTESIAN_POINT('Ctrl Pts',(-1.75853385710917,-0.535890369735552,
1.88889805825242));
#36975=CARTESIAN_POINT('Ctrl Pts',(-0.503915664640746,-1.76796168665343,
2.00000970873786));
#36976=CARTESIAN_POINT('Ctrl Pts',(1.21174280763407,-1.38249741391359,2.1111213592233));
#36977=CARTESIAN_POINT('Ctrl Pts',(1.81875888824183,0.267835396201195,2.22223300970874));
#36978=CARTESIAN_POINT('Ctrl Pts',(0.761764071097843,1.67312138149853,2.33334466019417));
#36979=CARTESIAN_POINT('Ctrl Pts',(-0.992180579104728,1.54764252547341,
2.44445631067961));
#36980=CARTESIAN_POINT('Ctrl Pts',(-1.83836373538439,0.00620135891621234,
2.55556796116504));
#36981=CARTESIAN_POINT('Ctrl Pts',(-1.0025992194253,-1.54091352175446,2.66667961165049));
#36982=CARTESIAN_POINT('Ctrl Pts',(0.750458968510211,-1.67822257683237,
2.77779126213592));
#36983=CARTESIAN_POINT('Ctrl Pts',(1.81691053470019,-0.280099604209337,
2.88890291262136));
#36984=CARTESIAN_POINT('Ctrl Pts',(1.22104229764526,1.37429086670804,3.0000145631068));
#36985=CARTESIAN_POINT('Ctrl Pts',(-0.491976593161155,1.77132117679823,
3.11112621359223));
#36986=CARTESIAN_POINT('Ctrl Pts',(-1.75487842108734,0.547742098573187,
3.22223786407767));
#36987=CARTESIAN_POINT('Ctrl Pts',(-1.41221459472129,-1.17697477363263,
3.3333495145631));
#36988=CARTESIAN_POINT('Ctrl Pts',(0.222506403513669,-1.8248590575151,3.44446116504855));
#36989=CARTESIAN_POINT('Ctrl Pts',(1.65365282072159,-0.803151310699741,
3.55557281553397));
#36990=CARTESIAN_POINT('Ctrl Pts',(1.57184646516792,0.953372104320743,3.66668446601942));
#36991=CARTESIAN_POINT('Ctrl Pts',(0.0519332482321354,1.83764050268212,
3.77779611650485));
#36992=CARTESIAN_POINT('Ctrl Pts',(-1.51549450798785,1.04062292672322,3.88890776699029));
#36993=CARTESIAN_POINT('Ctrl Pts',(-1.69637268788223,-0.708476804963227,
4.00001941747572));
#36994=CARTESIAN_POINT('Ctrl Pts',(-0.325213021862407,-1.80938005122649,
4.11113106796117));
#36995=CARTESIAN_POINT('Ctrl Pts',(1.34348911316817,-1.25485325124609,4.2222427184466));
#36996=CARTESIAN_POINT('Ctrl Pts',(1.78301209192838,0.447758371671112,4.33335436893204));
#36997=CARTESIAN_POINT('Ctrl Pts',(0.591229481908682,1.74070887258225,4.44446601941748));
#36998=CARTESIAN_POINT('Ctrl Pts',(-1.14147820789891,1.44105766028162,4.55557766990291));
#36999=CARTESIAN_POINT('Ctrl Pts',(-1.82982967127054,-0.177039694708382,
4.66668932038835));
#37000=CARTESIAN_POINT('Ctrl Pts',(-0.844041411881997,-1.63316067010957,
4.77780097087378));
#37001=CARTESIAN_POINT('Ctrl Pts',(0.913973507436636,-1.59507746114991,
4.88891262135923));
#37002=CARTESIAN_POINT('Ctrl Pts',(1.83577980123458,-0.0976329900371924,
5.00002427184466));
#37003=CARTESIAN_POINT('Ctrl Pts',(1.0780025055099,1.48913742733129,5.1111359223301));
#37004=CARTESIAN_POINT('Ctrl Pts',(-0.666056105926533,1.7134727727987,5.22224757281553));
#37005=CARTESIAN_POINT('Ctrl Pts',(-1.80072959150898,0.37012513779585,5.33335922330097));
#37006=CARTESIAN_POINT('Ctrl Pts',(-1.28788747144402,-1.31185576198834,
5.44447087378641));
#37007=CARTESIAN_POINT('Ctrl Pts',(0.403262995152723,-1.79359935217008,
5.55558252427184));
#37008=CARTESIAN_POINT('Ctrl Pts',(1.72546185411942,-0.634350903950841,
5.66669417475728));
#37009=CARTESIAN_POINT('Ctrl Pts',(1.46900873501267,1.1052750860401,5.77780582524271));
#37010=CARTESIAN_POINT('Ctrl Pts',(-0.13146340126236,1.83366765077345,5.88891747572816));
#37011=CARTESIAN_POINT('Ctrl Pts',(-1.61165762009075,0.884409065403499,
6.00002912621358));
#37012=CARTESIAN_POINT('Ctrl Pts',(-1.6173211305994,-0.87400917608522,6.11114077669903));
#37013=CARTESIAN_POINT('Ctrl Pts',(-0.143272298638598,-1.83278278249422,
6.22225242718446));
#37014=CARTESIAN_POINT('Ctrl Pts',(1.46185859526926,-1.11471481859797,6.33336407766989));
#37015=CARTESIAN_POINT('Ctrl Pts',(1.72951224644592,0.623223129190563,6.44447572815534));
#37016=CARTESIAN_POINT('Ctrl Pts',(0.414808152398764,1.79096450999678,6.55558737864077));
#37017=CARTESIAN_POINT('Ctrl Pts',(-1.27941039381778,1.320124510626,6.66669902912621));
#37018=CARTESIAN_POINT('Ctrl Pts',(-1.80307640411694,-0.358518005518811,
6.77781067961165));
#37019=CARTESIAN_POINT('Ctrl Pts',(-0.677079673289082,-1.70914680334463,
6.8889223300971));
#37020=CARTESIAN_POINT('Ctrl Pts',(1.06838781720774,-1.49605051766532,7.00003398058251));
#37021=CARTESIAN_POINT('Ctrl Pts',(1.83637062036826,0.0858057341481814,
7.11114563106797));
#37022=CARTESIAN_POINT('Ctrl Pts',(0.924229284360448,1.589156980696,7.22225728155339));
#37023=CARTESIAN_POINT('Ctrl Pts',(-0.833503847528551,1.63856370505402,
7.33336893203883));
#37024=CARTESIAN_POINT('Ctrl Pts',(-1.82865130156443,0.188822924059537,
7.44448058252428));
#37025=CARTESIAN_POINT('Ctrl Pts',(-1.15073714167466,-1.43367489694622,
7.5555922330097));
#37026=CARTESIAN_POINT('Ctrl Pts',(0.580004387659595,-1.74448118065669,
7.66670388349515));
#37027=CARTESIAN_POINT('Ctrl Pts',(1.7800908511122,-0.459234407622611,7.77781553398057));
#37028=CARTESIAN_POINT('Ctrl Pts',(1.35154441460109,1.24617309179735,7.88892718446602));
#37029=CARTESIAN_POINT('Ctrl Pts',(-0.313551099181417,1.81143738163968,
8.00003883495145));
#37030=CARTESIAN_POINT('Ctrl Pts',(-1.69177381899564,0.719389341505889,
8.11115048543689));
#37031=CARTESIAN_POINT('Ctrl Pts',(-1.52216626984007,-1.03083923397808,
8.22226213592232));
#37032=CARTESIAN_POINT('Ctrl Pts',(0.0400949547363229,-1.83793690702293,
8.33337378640777));
#37033=CARTESIAN_POINT('Ctrl Pts',(1.56567267939011,-0.963477420579929,
8.44448543689319));
#37034=CARTESIAN_POINT('Ctrl Pts',(1.65879203582308,0.792482593671729,8.55559708737864));
#37035=CARTESIAN_POINT('Ctrl Pts',(0.234256671005791,1.82338791618694,8.66670873786407));
#37036=CARTESIAN_POINT('Ctrl Pts',(-1.40460377720211,1.18604717671243,8.77782038834951));
#37037=CARTESIAN_POINT('Ctrl Pts',(-1.75837031067501,-0.536426631484242,
8.88893203883495));
#37038=CARTESIAN_POINT('Ctrl Pts',(-0.503376402892206,-1.7681153483915,
9.00004368932038));
#37039=CARTESIAN_POINT('Ctrl Pts',(1.2121644264892,-1.38212772940753,9.11115533980582));
#37040=CARTESIAN_POINT('Ctrl Pts',(1.81867711471885,0.26839009932345,9.22226699029127));
#37041=CARTESIAN_POINT('Ctrl Pts',(0.761253709552246,1.67335367481701,9.33337864077668));
#37042=CARTESIAN_POINT('Ctrl Pts',(-0.99265255914171,1.54733978795034,9.44449029126215));
#37043=CARTESIAN_POINT('Ctrl Pts',(-1.8383655777075,0.00564071579882353,
9.55560194174756));
#37044=CARTESIAN_POINT('Ctrl Pts',(-1.00212911067809,-1.54121939161292,
9.66671359223301));
#37045=CARTESIAN_POINT('Ctrl Pts',(0.750970673805211,-1.67799333720618,
9.77782524271844));
#37046=CARTESIAN_POINT('Ctrl Pts',(1.81699613594968,-0.279545920640164,
9.88893689320389));
#37047=CARTESIAN_POINT('Ctrl Pts',(1.22062258834496,1.37466418983892,10.0000485436893));
#37048=CARTESIAN_POINT('Ctrl Pts',(-0.492515922639386,1.77116921324136,
10.1111601941748));
#37049=CARTESIAN_POINT('Ctrl Pts',(-1.75504715049764,0.547210291375423,
10.2222718446602));
#37050=CARTESIAN_POINT('Ctrl Pts',(-1.4118522196555,-1.177412066494,10.3333834951456));
#37051=CARTESIAN_POINT('Ctrl Pts',(0.223056668548975,-1.82477852394609,
10.4444951456311));
#37052=CARTESIAN_POINT('Ctrl Pts',(1.65390974917898,-0.802670846854376,
10.5556067961165));
#37053=CARTESIAN_POINT('Ctrl Pts',(1.57153269033781,0.953897085409752,10.6667184466019));
#37054=CARTESIAN_POINT('Ctrl Pts',(0.0514163720288116,1.83756944970195,
10.7778300970874));
#37055=CARTESIAN_POINT('Ctrl Pts',(-1.51589489028199,1.04032592396117,10.8889417475728));
#37056=CARTESIAN_POINT('Ctrl Pts',(-1.69599832986023,-0.709309104380943,
11.0000533980583));
#37057=CARTESIAN_POINT('Ctrl Pts',(-0.324962964057439,-1.80887727526569,
11.1111650485437));
#37058=CARTESIAN_POINT('Ctrl Pts',(1.34445241673909,-1.25560970886474,11.2222766990291));
#37059=CARTESIAN_POINT('Ctrl Pts',(1.78171768593789,0.450698535437549,11.3333883495146));
#37060=CARTESIAN_POINT('Ctrl Pts',(0.989503531151977,1.30685679928735,11.4074627831715));
#37061=CARTESIAN_POINT('Ctrl Pts',(0.499806597877626,1.47301514408983,11.4445));
#37062=CARTESIAN_POINT('',(0.903606778650206,-1.26612599672284,0.));
#37063=CARTESIAN_POINT('Ctrl Pts',(0.903606778650208,-1.26612599672284,
-2.77555756156289E-15));
#37064=CARTESIAN_POINT('Ctrl Pts',(1.32452439122316,-0.965726187415828,
0.0370372168284762));
#37065=CARTESIAN_POINT('Ctrl Pts',(1.83597970935092,0.0826171234133487,
0.111111650485434));
#37066=CARTESIAN_POINT('Ctrl Pts',(0.924933321163406,1.59015923519395,0.222223300970871));
#37067=CARTESIAN_POINT('Ctrl Pts',(-0.833119343177651,1.63815447531815,
0.333334951456308));
#37068=CARTESIAN_POINT('Ctrl Pts',(-1.5310616378989,0.622578531632503,0.411241775931451));
#37069=CARTESIAN_POINT('Ctrl Pts',(-1.55772922446558,0.0543356393242454,
0.452111383578116));
#37070=CARTESIAN_POINT('Ctrl Pts',(-1.55735926886437,0.00101346774827265,
0.455943774396301));
#37071=CARTESIAN_POINT('Ctrl Pts',(0.863567639152676,1.75641488315944,2.28983498828939E-16));
#37072=CARTESIAN_POINT('Ctrl Pts',(0.902605506355985,1.73244147111074,2.48310810971475E-16));
#37073=CARTESIAN_POINT('Ctrl Pts',(0.940681517855526,1.70703362163956,1.53446104133306E-16));
#37074=CARTESIAN_POINT('Ctrl Pts',(0.977705169885396,1.68018661523996,1.12757025938492E-16));
#37075=CARTESIAN_POINT('Ctrl Pts',(1.0358643592122,1.63801357064694,3.49621561433049E-17));
#37076=CARTESIAN_POINT('Ctrl Pts',(1.09142895154027,1.59229038852923,-3.14041157591089E-18));
#37077=CARTESIAN_POINT('Ctrl Pts',(1.14423757319707,1.54335784953327,-1.00613961606655E-16));
#37078=CARTESIAN_POINT('Ctrl Pts',(1.16947625472704,1.51997165369202,-1.47199231391008E-16));
#37079=CARTESIAN_POINT('Ctrl Pts',(1.19408480623982,1.49585194230134,-1.44940981238328E-16));
#37080=CARTESIAN_POINT('Ctrl Pts',(1.21804196717247,1.47103398018765,-1.04083408558608E-16));
#37081=CARTESIAN_POINT('Ctrl Pts',(1.23020142841566,1.45843761915368,-8.33461403619852E-17));
#37082=CARTESIAN_POINT('Ctrl Pts',(1.24219304748387,1.44566136836505,-3.17714931440926E-16));
#37083=CARTESIAN_POINT('Ctrl Pts',(1.25401379483509,1.43270976178997,-3.05311331771918E-16));
#37084=CARTESIAN_POINT('Ctrl Pts',(1.26389181876557,1.42188673377951,-2.94946246493115E-16));
#37085=CARTESIAN_POINT('Ctrl Pts',(1.27364380619492,1.41094858444086,-5.46603369369435E-16));
#37086=CARTESIAN_POINT('Ctrl Pts',(1.28326720497828,1.3998998522991,-5.34294830600857E-16));
#37087=CARTESIAN_POINT('Ctrl Pts',(1.330154786252,1.3460676940429,-4.74324582576826E-16));
#37088=CARTESIAN_POINT('Ctrl Pts',(1.37400431756963,1.2896005558432,-2.78813144032988E-17));
#37089=CARTESIAN_POINT('Ctrl Pts',(1.41465239664765,1.2308327382907,1.45716771982052E-16));
#37090=CARTESIAN_POINT('Ctrl Pts',(1.44369336478921,1.18884614615641,2.69743702909727E-16));
#37091=CARTESIAN_POINT('Ctrl Pts',(1.47109927736379,1.14568453076923,1.23340209484872E-16));
#37092=CARTESIAN_POINT('Ctrl Pts',(1.4967949674738,1.10146499100096,1.52655665885959E-16));
#37093=CARTESIAN_POINT('Ctrl Pts',(1.51164370962241,1.07591189080641,1.69596158676961E-16));
#37094=CARTESIAN_POINT('Ctrl Pts',(1.5259211042574,1.05000546373499,-2.47389032972511E-16));
#37095=CARTESIAN_POINT('Ctrl Pts',(1.53961051084784,1.0237681518455,-2.63677968348475E-16));
#37096=CARTESIAN_POINT('Ctrl Pts',(1.5453767175419,1.01271655786648,-2.70539139983884E-16));
#37097=CARTESIAN_POINT('Ctrl Pts',(1.55103417937643,1.00161467257822,6.72528652799515E-17));
#37098=CARTESIAN_POINT('Ctrl Pts',(1.55658137030158,0.990465869694384,6.24500451351651E-17));
#37099=CARTESIAN_POINT('Ctrl Pts',(1.58759523113096,0.928133884781808,3.5597896440648E-17));
#37100=CARTESIAN_POINT('Ctrl Pts',(1.61517455934254,0.864320573166324,-1.32844578099872E-16));
#37101=CARTESIAN_POINT('Ctrl Pts',(1.639165272121,0.799334213601843,-1.80411241501588E-16));
#37102=CARTESIAN_POINT('Ctrl Pts',(1.66256479067373,0.735949288762567,-2.26805737281603E-16));
#37103=CARTESIAN_POINT('Ctrl Pts',(1.68255047093124,0.671447445488438,-3.92048207771591E-16));
#37104=CARTESIAN_POINT('Ctrl Pts',(1.69893099532196,0.606109731061441,-4.30211422042248E-16));
#37105=CARTESIAN_POINT('Ctrl Pts',(1.70969999791506,0.563154939181291,-4.55300957861645E-16));
#37106=CARTESIAN_POINT('Ctrl Pts',(1.71890982821634,0.519838805550124,-3.77882014063636E-16));
#37107=CARTESIAN_POINT('Ctrl Pts',(1.72649398406889,0.476242912678102,-4.71844785465692E-16));
#37108=CARTESIAN_POINT('Ctrl Pts',(1.73287054571603,0.439588616027976,-5.50846247992205E-16));
#37109=CARTESIAN_POINT('Ctrl Pts',(1.73809775889755,0.402736552578244,-9.42921937940892E-17));
#37110=CARTESIAN_POINT('Ctrl Pts',(1.74213052178609,0.36573694696249,-1.2490009027033E-16));
#37111=CARTESIAN_POINT('Ctrl Pts',(1.74338539139703,0.354223827548557,-1.34424309820125E-16));
#37112=CARTESIAN_POINT('Ctrl Pts',(1.74452450777523,0.342696049837886,-3.03274465566551E-16));
#37113=CARTESIAN_POINT('Ctrl Pts',(1.74554535151306,0.331170337018761,-2.91433543964104E-16));
#37114=CARTESIAN_POINT('Ctrl Pts',(1.75129431083391,0.266262406759456,-2.24750491415529E-16));
#37115=CARTESIAN_POINT('Ctrl Pts',(1.75331011127704,0.201301920292928,9.80627071070611E-17));
#37116=CARTESIAN_POINT('Ctrl Pts',(1.75142561531544,0.136549272921142,2.77555756156289E-17));
#37117=CARTESIAN_POINT('Ctrl Pts',(1.75088296778463,0.11790351037964,7.510378979319E-18));
#37118=CARTESIAN_POINT('Ctrl Pts',(1.75001659332986,0.099275023041261,-5.08054903583662E-16));
#37119=CARTESIAN_POINT('Ctrl Pts',(1.74882170147482,0.0806701752180915,
-4.85722573273506E-16));
#37120=CARTESIAN_POINT('Ctrl Pts',(1.74442082328573,0.0121470962041962,
-4.16579971360731E-16));
#37121=CARTESIAN_POINT('Ctrl Pts',(1.73556771390717,-0.056057442313777,
-1.52368272571946E-16));
#37122=CARTESIAN_POINT('Ctrl Pts',(1.72245534586321,-0.123606275893366,
-5.55111512312578E-17));
#37123=CARTESIAN_POINT('Ctrl Pts',(1.71065390208195,-0.184401836184713,
3.16625666268892E-17));
#37124=CARTESIAN_POINT('Ctrl Pts',(1.69540107690307,-0.244666544752314,
-5.10914177950054E-16));
#37125=CARTESIAN_POINT('Ctrl Pts',(1.67680493801022,-0.304129401844208,
-5.82867087928207E-16));
#37126=CARTESIAN_POINT('Ctrl Pts',(1.67349552259788,-0.314711560692091,
-5.95672007842828E-16));
#37127=CARTESIAN_POINT('Ctrl Pts',(1.67008173945308,-0.325263020743978,
-2.82234476894323E-16));
#37128=CARTESIAN_POINT('Ctrl Pts',(1.66656691458475,-0.335775244456298,
-2.77555756156289E-16));
#37129=CARTESIAN_POINT('Ctrl Pts',(1.64601434320315,-0.39724437487395,-2.5019742521657E-16));
#37130=CARTESIAN_POINT('Ctrl Pts',(1.6219871213203,-0.457449913435399,-1.49651752513019E-16));
#37131=CARTESIAN_POINT('Ctrl Pts',(1.59467186427628,-0.5161179062652,-1.94289029309402E-16));
#37132=CARTESIAN_POINT('Ctrl Pts',(1.56746479951959,-0.57455352257637,-2.38749503483388E-16));
#37133=CARTESIAN_POINT('Ctrl Pts',(1.53699493854014,-0.631464584970275,
-4.11608014004163E-16));
#37134=CARTESIAN_POINT('Ctrl Pts',(1.50340708769257,-0.686547887629179,
-4.71844785465692E-16));
#37135=CARTESIAN_POINT('Ctrl Pts',(1.47050686756616,-0.740503491725204,
-5.30848353445754E-16));
#37136=CARTESIAN_POINT('Ctrl Pts',(1.43461427022078,-0.792706028859038,
8.26037042042841E-17));
#37137=CARTESIAN_POINT('Ctrl Pts',(1.39583852741916,-0.842828743497358,
1.94289029309402E-16));
#37138=CARTESIAN_POINT('Ctrl Pts',(1.38891448399703,-0.851778974428235,
2.14232271779286E-16));
#37139=CARTESIAN_POINT('Ctrl Pts',(1.38189845475662,-0.860662765012678,
1.05754276149716E-16));
#37140=CARTESIAN_POINT('Ctrl Pts',(1.3747909965488,-0.869478087839508,1.11022302462516E-16));
#37141=CARTESIAN_POINT('Ctrl Pts',(1.36801000346398,-0.877888498619479,
1.1604835382339E-16));
#37142=CARTESIAN_POINT('Ctrl Pts',(1.36114891147745,-0.8862326313589,4.78426519390645E-16));
#37143=CARTESIAN_POINT('Ctrl Pts',(1.35421355798306,-0.894502968665375,
4.71844785465692E-16));
#37144=CARTESIAN_POINT('Ctrl Pts',(1.3143417576089,-0.942049678199007,4.34005967100638E-16));
#37145=CARTESIAN_POINT('Ctrl Pts',(1.27196760499602,-0.987223303029092,
-4.84873724376989E-16));
#37146=CARTESIAN_POINT('Ctrl Pts',(1.22722986402911,-1.02975664627632,-3.05311331771918E-16));
#37147=CARTESIAN_POINT('Ctrl Pts',(1.18329662429212,-1.07152512911229,-1.2897793916942E-16));
#37148=CARTESIAN_POINT('Ctrl Pts',(1.13708333146208,-1.1107479710078,1.42267300457324E-16));
#37149=CARTESIAN_POINT('Ctrl Pts',(1.08869802628341,-1.14712822354107,1.94289029309402E-16));
#37150=CARTESIAN_POINT('Ctrl Pts',(1.04185702701945,-1.1823473334721,2.44650389103912E-16));
#37151=CARTESIAN_POINT('Ctrl Pts',(0.99297984330778,-1.21490270865201,1.66616011326585E-16));
#37152=CARTESIAN_POINT('Ctrl Pts',(0.942151955941521,-1.24447758118399,
1.11022302462516E-16));
#37153=CARTESIAN_POINT('Ctrl Pts',(0.929425469464971,-1.25188265416315,
9.71025308430195E-17));
#37154=CARTESIAN_POINT('Ctrl Pts',(0.916576650468056,-1.25910062269163,
1.9641793555709E-16));
#37155=CARTESIAN_POINT('Ctrl Pts',(0.903606778650242,-1.26612599672281,
1.94289029309402E-16));
#37156=CARTESIAN_POINT('Ctrl Pts',(1.88079991776263,-0.516378774142081,
11.046));
#37157=CARTESIAN_POINT('Ctrl Pts',(1.79754570390634,-0.821182550519846,
11.028067538919));
#37158=CARTESIAN_POINT('Ctrl Pts',(1.64446793279769,-1.10682480125595,11.010135077838));
#37159=CARTESIAN_POINT('Ctrl Pts',(1.43091597726206,-1.33587557506818,10.9922026167571));
#37160=CARTESIAN_POINT('Ctrl Pts',(0.9898515831668,-1.80895080641009,10.9551653999286));
#37161=CARTESIAN_POINT('Ctrl Pts',(0.290818548970629,-2.04062011418838,
10.9181281831001));
#37162=CARTESIAN_POINT('Ctrl Pts',(-0.345744266721549,-1.9262440956347,
10.8810909662716));
#37163=CARTESIAN_POINT('Ctrl Pts',(-0.982307082413709,-1.81186807708102,
10.8440537494431));
#37164=CARTESIAN_POINT('Ctrl Pts',(-1.55639967960188,-1.35144673219537,
10.8070165326147));
#37165=CARTESIAN_POINT('Ctrl Pts',(-1.80573868997825,-0.754924386616321,
10.7699793157862));
#37166=CARTESIAN_POINT('Ctrl Pts',(-1.90472245868201,-0.518114150655666,
10.7552761078989));
#37167=CARTESIAN_POINT('Ctrl Pts',(-1.95252608806662,-0.259854826956367,
10.7405729000116));
#37168=CARTESIAN_POINT('Ctrl Pts',(-1.95129684289216,-0.00113636086278679,
10.7258696921242));
#37169=CARTESIAN_POINT('Origin',(0.,0.,-1.29405622560369));
#37170=CARTESIAN_POINT('',(-0.903606778650172,-1.26612599672286,0.));
#37171=CARTESIAN_POINT('Ctrl Pts',(-0.905549614304886,-1.26792015305981,
1.24276674021151E-15));
#37172=CARTESIAN_POINT('Ctrl Pts',(-0.513706458239086,-1.54472437079514,
0.0344950590738082));
#37173=CARTESIAN_POINT('Ctrl Pts',(0.587535178885047,-1.72169358136003,
0.106052258091336));
#37174=CARTESIAN_POINT('Ctrl Pts',(1.77508460417327,-0.479721809770191,
0.214671597052585));
#37175=CARTESIAN_POINT('Ctrl Pts',(1.3650560094313,1.23222299189869,0.325858016883748));
#37176=CARTESIAN_POINT('Ctrl Pts',(-0.295638381403906,1.81478253869214,
0.43704443671491));
#37177=CARTESIAN_POINT('Ctrl Pts',(-1.41307745535963,0.946781319192958,
0.526443839621562));
#37178=CARTESIAN_POINT('Ctrl Pts',(-1.55414936746312,0.214718667413076,
0.578781102584494));
#37179=CARTESIAN_POINT('Ctrl Pts',(-1.55326046963413,0.000729270061605551,
0.594056225603705));
#37180=CARTESIAN_POINT('Origin',(0.,0.,0.));
#37181=CARTESIAN_POINT('Ctrl Pts',(-0.685825729128748,1.39614588036674,
-0.230074082272066));
#37182=CARTESIAN_POINT('Ctrl Pts',(-1.15028016933624,1.16799292759742,-0.193011942328345));
#37183=CARTESIAN_POINT('Ctrl Pts',(-1.82555218707277,0.215691441263552,
-0.118887662440903));
#37184=CARTESIAN_POINT('Ctrl Pts',(-1.16942936218886,-1.42059634545264,
-0.00770124260974049));
#37185=CARTESIAN_POINT('Ctrl Pts',(0.559468948314244,-1.75104601534012,
0.103485177221422));
#37186=CARTESIAN_POINT('Ctrl Pts',(1.77508460417327,-0.479721809770191,
0.214671597052585));
#37187=CARTESIAN_POINT('Ctrl Pts',(1.3650560094313,1.23222299189869,0.325858016883748));
#37188=CARTESIAN_POINT('Ctrl Pts',(-0.295638381403906,1.81478253869214,
0.43704443671491));
#37189=CARTESIAN_POINT('Ctrl Pts',(-1.68540213790592,0.735245708832444,
0.548230856546073));
#37190=CARTESIAN_POINT('Ctrl Pts',(-1.53132379752993,-1.01797781965797,
0.659417276377235));
#37191=CARTESIAN_POINT('Ctrl Pts',(0.0255447675030308,-1.83860034663711,
0.770603696208398));
#37192=CARTESIAN_POINT('Ctrl Pts',(1.55899683301632,-0.975032021788082,
0.881790116039561));
#37193=CARTESIAN_POINT('Ctrl Pts',(1.66434877052597,0.781732535368643,0.992976535870723));
#37194=CARTESIAN_POINT('Ctrl Pts',(0.245080507541896,1.82238325373942,1.10416295570189));
#37195=CARTESIAN_POINT('Ctrl Pts',(-1.39868975820189,1.19365863723167,1.21534937553305));
#37196=CARTESIAN_POINT('Ctrl Pts',(-1.76120077222934,-0.528512641939849,
1.32653579536421));
#37197=CARTESIAN_POINT('Ctrl Pts',(-0.510374815939226,-1.76654153931159,
1.43772221519537));
#37198=CARTESIAN_POINT('Ctrl Pts',(1.20797626960931,-1.38634273102519,1.54890863502654));
#37199=CARTESIAN_POINT('Ctrl Pts',(1.81976886629041,0.263806680570579,1.6600950548577));
#37200=CARTESIAN_POINT('Ctrl Pts',(0.764574137846417,1.67229745635935,1.77128147468886));
#37201=CARTESIAN_POINT('Ctrl Pts',(-0.991003621173195,1.54889135395602,
1.88246789452002));
#37202=CARTESIAN_POINT('Ctrl Pts',(-1.83877909581896,0.00663349951290586,
1.99365431435119));
#37203=CARTESIAN_POINT('Ctrl Pts',(-1.00215313155719,-1.54170088892816,
2.10484073418235));
#37204=CARTESIAN_POINT('Ctrl Pts',(0.752488571272716,-1.67777039880966,
2.21602715401351));
#37205=CARTESIAN_POINT('Ctrl Pts',(1.81781810074028,-0.276929424335053,
2.32721357384467));
#37206=CARTESIAN_POINT('Ctrl Pts',(1.21794738393109,1.37759091140133,2.43839999367584));
#37207=CARTESIAN_POINT('Ctrl Pts',(-0.497615974795104,1.77017821004958,
2.549586413507));
#37208=CARTESIAN_POINT('Ctrl Pts',(-1.75734151264734,0.541205469518692,
2.66077283333817));
#37209=CARTESIAN_POINT('Ctrl Pts',(-1.40726598433086,-1.1835349598584,2.77195925316932));
#37210=CARTESIAN_POINT('Ctrl Pts',(0.231926238140432,-1.82410602009977,
2.88314567300049));
#37211=CARTESIAN_POINT('Ctrl Pts',(1.65866396469461,-0.793716828903688,
2.99433209283165));
#37212=CARTESIAN_POINT('Ctrl Pts',(1.56599354026699,0.96375141196464,3.10551851266282));
#37213=CARTESIAN_POINT('Ctrl Pts',(0.0388050940998321,1.83838154825996,
3.21670493249398));
#37214=CARTESIAN_POINT('Ctrl Pts',(-1.52393050178991,1.02897443019027,3.32789135232514));
#37215=CARTESIAN_POINT('Ctrl Pts',(-1.69067964401488,-0.723017906820314,
3.4390777721563));
#37216=CARTESIAN_POINT('Ctrl Pts',(-0.308692884081366,-1.81269447386996,
3.55026419198746));
#37217=CARTESIAN_POINT('Ctrl Pts',(1.35606994996762,-1.24186426112907,3.66145061181863));
#37218=CARTESIAN_POINT('Ctrl Pts',(1.77861387826841,0.466567491694538,3.77263703164979));
#37219=CARTESIAN_POINT('Ctrl Pts',(0.571870330903418,1.74760318061885,3.88382345148095));
#37220=CARTESIAN_POINT('Ctrl Pts',(-1.15873124952358,1.42775853828764,3.99500987131212));
#37221=CARTESIAN_POINT('Ctrl Pts',(-1.82788473512851,-0.199974866820836,
4.10619629114327));
#37222=CARTESIAN_POINT('Ctrl Pts',(-0.822616502622442,-1.64452261823584,
4.21738271097444));
#37223=CARTESIAN_POINT('Ctrl Pts',(0.936204134582059,-1.58261630557358,
4.3285691308056));
#37224=CARTESIAN_POINT('Ctrl Pts',(1.83742116834086,-0.0709647969689106,
4.43975555063676));
#37225=CARTESIAN_POINT('Ctrl Pts',(1.0554806974386,1.50569354438759,4.55094197046793));
#37226=CARTESIAN_POINT('Ctrl Pts',(-0.693325883166112,1.70307127625589,
4.66212839029909));
#37227=CARTESIAN_POINT('Ctrl Pts',(-1.80701587562324,0.340361833232659,
4.77331481013025));
#37228=CARTESIAN_POINT('Ctrl Pts',(-1.26540093064824,-1.33413381524886,
4.88450122996142));
#37229=CARTESIAN_POINT('Ctrl Pts',(0.435376164803608,-1.7865050090601,4.99568764979258));
#37230=CARTESIAN_POINT('Ctrl Pts',(1.73732980498774,-0.602360109052031,
5.10687406962374));
#37231=CARTESIAN_POINT('Ctrl Pts',(1.44781397169404,1.13357278356683,5.21806048945491));
#37232=CARTESIAN_POINT('Ctrl Pts',(-0.167962271460079,1.83110382765203,
5.32924690928607));
#37233=CARTESIAN_POINT('Ctrl Pts',(-1.62987778710162,0.851264325217889,
5.44043332911723));
#37234=CARTESIAN_POINT('Ctrl Pts',(-1.59875453933454,-0.908370230265797,
5.55161974894839));
#37235=CARTESIAN_POINT('Ctrl Pts',(-0.103102773360761,-1.83589824620028,
5.66280616877956));
#37236=CARTESIAN_POINT('Ctrl Pts',(1.4869956060099,-1.08166382022474,5.77399258861071));
#37237=CARTESIAN_POINT('Ctrl Pts',(1.71494149863546,0.663421591850831,5.88517900844189));
#37238=CARTESIAN_POINT('Ctrl Pts',(0.371926577693494,1.80078404398782,5.99636542827304));
#37239=CARTESIAN_POINT('Ctrl Pts',(-1.311789224034,1.28855018683177,6.10755184810421));
#37240=CARTESIAN_POINT('Ctrl Pts',(-1.79384918603911,-0.404051543769803,
6.21873826793537));
#37241=CARTESIAN_POINT('Ctrl Pts',(-0.632665469493242,-1.72652453095426,
6.32992468776653));
#37242=CARTESIAN_POINT('Ctrl Pts',(1.10806726459172,-1.46742614445027,6.44111110759769));
#37243=CARTESIAN_POINT('Ctrl Pts',(1.83376231205259,0.135898253011021,6.55229752742886));
#37244=CARTESIAN_POINT('Ctrl Pts',(0.879651525947856,1.61473395492061,6.66348394726001));
#37245=CARTESIAN_POINT('Ctrl Pts',(-0.880258220622017,1.61440330069759,
6.77467036709119));
#37246=CARTESIAN_POINT('Ctrl Pts',(-1.83381324808445,0.13520918395534,6.88585678692234));
#37247=CARTESIAN_POINT('Ctrl Pts',(-1.1075157823663,-1.46784241118916,6.99704320675351));
#37248=CARTESIAN_POINT('Ctrl Pts',(0.633314188332071,-1.72628667698419,
7.10822962658467));
#37249=CARTESIAN_POINT('Ctrl Pts',(1.7940008868909,-0.403377453646542,7.21941604641583));
#37250=CARTESIAN_POINT('Ctrl Pts',(1.31130494233742,1.28904301731096,7.33060246624699));
#37251=CARTESIAN_POINT('Ctrl Pts',(-0.372603218894873,1.80064416072257,
7.44178888607816));
#37252=CARTESIAN_POINT('Ctrl Pts',(-1.71519066664489,0.662777133981789,
7.55297530590932));
#37253=CARTESIAN_POINT('Ctrl Pts',(-1.48658905212271,-1.08222250133236,
7.66416172574049));
#37254=CARTESIAN_POINT('Ctrl Pts',(0.103792628149562,-1.8358593744105,7.77534814557165));
#37255=CARTESIAN_POINT('Ctrl Pts',(1.59909575810308,-0.907769413831382,
7.8865345654028));
#37256=CARTESIAN_POINT('Ctrl Pts',(1.62955779866738,0.851876712390422,7.99772098523398));
#37257=CARTESIAN_POINT('Ctrl Pts',(0.167274199086701,1.83116681231986,8.10890740506512));
#37258=CARTESIAN_POINT('Ctrl Pts',(-1.44823982381472,1.1330286690894,8.2200938248963));
#37259=CARTESIAN_POINT('Ctrl Pts',(-1.73710333792674,-0.603012890298399,
8.33128024472746));
#37260=CARTESIAN_POINT('Ctrl Pts',(-0.434704832044991,-1.78666848096071,
8.44246666455862));
#37261=CARTESIAN_POINT('Ctrl Pts',(1.26590215885116,-1.33365823077974,8.55365308438979));
#37262=CARTESIAN_POINT('Ctrl Pts',(1.8068878531032,0.341040818691465,8.66483950422094));
#37263=CARTESIAN_POINT('Ctrl Pts',(0.69268588294083,1.70333168137465,8.77602592405212));
#37264=CARTESIAN_POINT('Ctrl Pts',(-1.05604640517969,1.5052968290502,8.88721234388326));
#37265=CARTESIAN_POINT('Ctrl Pts',(-1.83739437498563,-0.0716552286239433,
8.99839876371444));
#37266=CARTESIAN_POINT('Ctrl Pts',(-0.935609375970031,-1.5829679799695,
9.1095851835456));
#37267=CARTESIAN_POINT('Ctrl Pts',(0.823234386500799,-1.64421340203127,
9.22077160337675));
#37268=CARTESIAN_POINT('Ctrl Pts',(1.82795976495949,-0.199287985657338,
9.33195802320793));
#37269=CARTESIAN_POINT('Ctrl Pts',(1.15819463928053,1.42819381470141,9.44314444303908));
#37270=CARTESIAN_POINT('Ctrl Pts',(-0.572526917402423,1.74738822826618,
9.55433086287024));
#37271=CARTESIAN_POINT('Ctrl Pts',(-1.77878918025408,0.46589901053406,9.66551728270142));
#37272=CARTESIAN_POINT('Ctrl Pts',(-1.35560300066214,-1.24237352171324,
9.77670370253256));
#37273=CARTESIAN_POINT('Ctrl Pts',(0.309373610575528,-1.81257875466721,
9.88789012236375));
#37274=CARTESIAN_POINT('Ctrl Pts',(1.69095195914933,-0.722381792257861,
9.99907654219489));
#37275=CARTESIAN_POINT('Ctrl Pts',(1.52354231364944,1.0295455294481,10.1102629620261));
#37276=CARTESIAN_POINT('Ctrl Pts',(-0.0394931635484403,1.83836962465064,
10.2214493818572));
#37277=CARTESIAN_POINT('Ctrl Pts',(-1.56636075542215,0.963157594965877,
10.3326358016884));
#37278=CARTESIAN_POINT('Ctrl Pts',(-1.65835572967195,-0.794329933758677,
10.4438222215196));
#37279=CARTESIAN_POINT('Ctrl Pts',(-0.231259578302998,-1.82421227428175,
10.5550086413507));
#37280=CARTESIAN_POINT('Ctrl Pts',(1.40774638007895,-1.1829694620695,10.6661950611819));
#37281=CARTESIAN_POINT('Ctrl Pts',(1.75706993010233,0.541796064983141,10.7773814810131));
#37282=CARTESIAN_POINT('Ctrl Pts',(0.497080432048737,1.77049779856472,10.8885679008442));
#37283=CARTESIAN_POINT('Ctrl Pts',(-1.21871201614337,1.37688031013954,10.9997543206754));
#37284=CARTESIAN_POINT('Ctrl Pts',(-1.81724153253684,-0.27712968875509,
11.1109407405065));
#37285=CARTESIAN_POINT('Ctrl Pts',(-0.75277483453787,-1.67898453189698,
11.2221271603377));
#37286=CARTESIAN_POINT('Ctrl Pts',(1.00462758039806,-1.53944373403644,11.3333135801688));
#37287=CARTESIAN_POINT('Ctrl Pts',(1.55754888396286,-0.511266487217653,
11.4074378600563));
#37288=CARTESIAN_POINT('Ctrl Pts',(1.55548765964692,0.00619602180124784,
11.4445));
#37289=CARTESIAN_POINT('Ctrl Pts',(-0.74439243930934,1.51537102412034,-0.153382721514711));
#37290=CARTESIAN_POINT('Ctrl Pts',(-1.24850938769699,1.26773474301532,-0.11632058157099));
#37291=CARTESIAN_POINT('Ctrl Pts',(-1.98144687185762,0.234110607521693,
-0.042196301683548));
#37292=CARTESIAN_POINT('Ctrl Pts',(-1.26929384324154,-1.54190945884872,
0.0689901181476148));
#37293=CARTESIAN_POINT('Ctrl Pts',(0.607245306591998,-1.90057817801302,
0.180176537978778));
#37294=CARTESIAN_POINT('Ctrl Pts',(1.92666956394248,-0.520688088821623,
0.29136295780994));
#37295=CARTESIAN_POINT('Ctrl Pts',(1.48162620545796,1.33744979191402,0.402549377641103));
#37296=CARTESIAN_POINT('Ctrl Pts',(-0.320884689126903,1.9697575395855,0.513735797472264));
#37297=CARTESIAN_POINT('Ctrl Pts',(-1.82932858212653,0.798032683003624,
0.624922217303428));
#37298=CARTESIAN_POINT('Ctrl Pts',(-1.66209258212561,-1.10490895887015,
0.736108637134591));
#37299=CARTESIAN_POINT('Ctrl Pts',(0.0277261860929502,-1.99560929084259,
0.847295056965753));
#37300=CARTESIAN_POINT('Ctrl Pts',(1.69212878157669,-1.0582957656395,0.958481476796916));
#37301=CARTESIAN_POINT('Ctrl Pts',(1.80647734334385,0.848489294255244,1.06966789662808));
#37302=CARTESIAN_POINT('Ctrl Pts',(0.266009379770665,1.97800732458805,1.18085431645924));
#37303=CARTESIAN_POINT('Ctrl Pts',(-1.51813213871049,1.2955921992025,1.29204073629041));
#37304=CARTESIAN_POINT('Ctrl Pts',(-1.91160010957712,-0.573645458357494,
1.40322715612156));
#37305=CARTESIAN_POINT('Ctrl Pts',(-0.553958736254638,-1.91739695630841,
1.51441357595273));
#37306=CARTESIAN_POINT('Ctrl Pts',(1.31113249878304,-1.50473072594935,1.62559999578389));
#37307=CARTESIAN_POINT('Ctrl Pts',(1.9751696791516,0.286334691329668,1.73678641561505));
#37308=CARTESIAN_POINT('Ctrl Pts',(0.829865639814035,1.81510481441338,1.84797283544622));
#37309=CARTESIAN_POINT('Ctrl Pts',(-1.07563127424026,1.68116033596642,1.95915925527738));
#37310=CARTESIAN_POINT('Ctrl Pts',(-1.99580330447296,0.00719997322039096,
2.07034567510854));
#37311=CARTESIAN_POINT('Ctrl Pts',(-1.08773290717609,-1.67335583465575,
2.18153209493971));
#37312=CARTESIAN_POINT('Ctrl Pts',(0.816748015321165,-1.82104512374819,
2.29271851477087));
#37313=CARTESIAN_POINT('Ctrl Pts',(1.97305232620797,-0.300578063700233,
2.40390493460203));
#37314=CARTESIAN_POINT('Ctrl Pts',(1.32195510545613,1.49523153675082,2.51509135443319));
#37315=CARTESIAN_POINT('Ctrl Pts',(-0.54011034229875,1.92134418384253,2.62627777426435));
#37316=CARTESIAN_POINT('Ctrl Pts',(-1.90741128502276,0.587422201459822,
2.73746419409552));
#37317=CARTESIAN_POINT('Ctrl Pts',(-1.52744073944838,-1.28460400121777,
2.84865061392668));
#37318=CARTESIAN_POINT('Ctrl Pts',(0.251731789602741,-1.9798772081443,2.95983703375785));
#37319=CARTESIAN_POINT('Ctrl Pts',(1.80030707836241,-0.861496997406464,
3.071023453589));
#37320=CARTESIAN_POINT('Ctrl Pts',(1.69972297898904,1.04605183790867,3.18220987342017));
#37321=CARTESIAN_POINT('Ctrl Pts',(0.0421188903066005,1.99537180797957,
3.29339629325133));
#37322=CARTESIAN_POINT('Ctrl Pts',(-1.65406792919015,1.11684463493277,3.4045827130825));
#37323=CARTESIAN_POINT('Ctrl Pts',(-1.83505676565636,-0.784760676748056,
3.51576913291366));
#37324=CARTESIAN_POINT('Ctrl Pts',(-0.335053992900935,-1.96749116257395,
3.62695555274482));
#37325=CARTESIAN_POINT('Ctrl Pts',(1.47187277329603,-1.34791438607496,3.73814197257599));
#37326=CARTESIAN_POINT('Ctrl Pts',(1.93050022360002,0.506410445822938,3.84932839240714));
#37327=CARTESIAN_POINT('Ctrl Pts',(0.620705716495424,1.89684133929807,3.96051481223831));
#37328=CARTESIAN_POINT('Ctrl Pts',(-1.25768215554202,1.54968327363698,4.07170123206947));
#37329=CARTESIAN_POINT('Ctrl Pts',(-1.9839786099702,-0.217051901949521,
4.18288765190064));
#37330=CARTESIAN_POINT('Ctrl Pts',(-0.892864584974339,-1.78495811879663,
4.29407407173179));
#37331=CARTESIAN_POINT('Ctrl Pts',(1.01615213578872,-1.71776526041577,4.40526049156296));
#37332=CARTESIAN_POINT('Ctrl Pts',(1.99432941554622,-0.0770249001709277,
4.51644691139412));
#37333=CARTESIAN_POINT('Ctrl Pts',(1.14561442891388,1.6342736102696,4.62763333122529));
#37334=CARTESIAN_POINT('Ctrl Pts',(-0.752533075803338,1.84850659257176,
4.73881975105645));
#37335=CARTESIAN_POINT('Ctrl Pts',(-1.96132763527948,0.369427340688636,
4.85000617088761));
#37336=CARTESIAN_POINT('Ctrl Pts',(-1.3734609908354,-1.44806338245697,4.96119259071877));
#37337=CARTESIAN_POINT('Ctrl Pts',(0.472555507281729,-1.9390652246629,5.07237901054994));
#37338=CARTESIAN_POINT('Ctrl Pts',(1.88569065943703,-0.653799196903168,
5.1835654303811));
#37339=CARTESIAN_POINT('Ctrl Pts',(1.57145135896933,1.23037525956625,5.29475185021226));
#37340=CARTESIAN_POINT('Ctrl Pts',(-0.182305561972616,1.98747259981946,
5.40593827004342));
#37341=CARTESIAN_POINT('Ctrl Pts',(-1.76906267902489,0.923958814363803,
5.51712468987459));
#37342=CARTESIAN_POINT('Ctrl Pts',(-1.73528163328608,-0.985941329968107,
5.62831110970574));
#37343=CARTESIAN_POINT('Ctrl Pts',(-0.111907328205795,-1.99267644208816,
5.73949752953692));
#37344=CARTESIAN_POINT('Ctrl Pts',(1.61397894448518,-1.17403348321834,5.85068394936807));
#37345=CARTESIAN_POINT('Ctrl Pts',(1.86139048335769,0.720075080408093,5.96187036919923));
#37346=CARTESIAN_POINT('Ctrl Pts',(0.403687585131819,1.9545636307293,6.0730567890304));
#37347=CARTESIAN_POINT('Ctrl Pts',(-1.42381065460884,1.39858709874703,6.18424320886156));
#37348=CARTESIAN_POINT('Ctrl Pts',(-1.94703656429618,-0.438555891823412,
6.29542962869273));
#37349=CARTESIAN_POINT('Ctrl Pts',(-0.686692511086116,-1.87396265922711,
6.40661604852388));
#37350=CARTESIAN_POINT('Ctrl Pts',(1.20269167366484,-1.59273833100625,6.51780246835505));
#37351=CARTESIAN_POINT('Ctrl Pts',(1.99035810790665,0.147503407586138,6.62898888818621));
#37352=CARTESIAN_POINT('Ctrl Pts',(0.954770165847204,1.75262562555938,6.74017530801738));
#37353=CARTESIAN_POINT('Ctrl Pts',(-0.9554286697633,1.7522667348191,6.85136172784854));
#37354=CARTESIAN_POINT('Ctrl Pts',(-1.99041339366714,0.146755494853507,
6.9625481476797));
#37355=CARTESIAN_POINT('Ctrl Pts',(-1.20209309711463,-1.59319014522084,
7.07373456751086));
#37356=CARTESIAN_POINT('Ctrl Pts',(0.687396627858533,-1.87370449350154,
7.18492098734203));
#37357=CARTESIAN_POINT('Ctrl Pts',(1.94720121977979,-0.437824237162718,
7.29610740717318));
#37358=CARTESIAN_POINT('Ctrl Pts',(1.42328501723757,1.39912201493195,7.40729382700435));
#37359=CARTESIAN_POINT('Ctrl Pts',(-0.404422008722263,1.95441180200575,
7.51848024683551));
#37360=CARTESIAN_POINT('Ctrl Pts',(-1.86166092929526,0.719375588474842,
7.62966666666667));
#37361=CARTESIAN_POINT('Ctrl Pts',(-1.61353767256008,-1.17463987340584,
7.74085308649784));
#37362=CARTESIAN_POINT('Ctrl Pts',(0.112656093769942,-1.99263425080664,
7.852039506329));
#37363=CARTESIAN_POINT('Ctrl Pts',(1.73565199074082,-0.985289206269375,
7.96322592616017));
#37364=CARTESIAN_POINT('Ctrl Pts',(1.76871536488809,0.924623496894334,8.07441234599133));
#37365=CARTESIAN_POINT('Ctrl Pts',(0.181558731034875,1.98754096312013,8.18559876582249));
#37366=CARTESIAN_POINT('Ctrl Pts',(-1.57191357711808,1.22978467993954,8.29678518565365));
#37367=CARTESIAN_POINT('Ctrl Pts',(-1.88544485301595,-0.6545077229961,8.40797160548482));
#37368=CARTESIAN_POINT('Ctrl Pts',(-0.471826845453332,-1.93924265639472,
8.51915802531597));
#37369=CARTESIAN_POINT('Ctrl Pts',(1.37400502187529,-1.44754718502077,8.63034444514714));
#37370=CARTESIAN_POINT('Ctrl Pts',(1.96118868016023,0.370164308726493,8.7415308649783));
#37371=CARTESIAN_POINT('Ctrl Pts',(0.751838422178375,1.84878923522181,8.85271728480947));
#37372=CARTESIAN_POINT('Ctrl Pts',(-1.14622844578058,1.63384301706618,8.96390370464062));
#37373=CARTESIAN_POINT('Ctrl Pts',(-1.99430033414812,-0.077774291863319,
9.0750901244718));
#37374=CARTESIAN_POINT('Ctrl Pts',(-1.01550658722561,-1.71814696636568,
9.18627654430294));
#37375=CARTESIAN_POINT('Ctrl Pts',(0.893535233606871,-1.78462249679383,
9.29746296413412));
#37376=CARTESIAN_POINT('Ctrl Pts',(1.98406004704164,-0.216306363946107,
9.40864938396527));
#37377=CARTESIAN_POINT('Ctrl Pts',(1.2570997209806,1.55015572087487,9.51983580379645));
#37378=CARTESIAN_POINT('Ctrl Pts',(-0.621418372793996,1.8966080308943,9.63102222362759));
#37379=CARTESIAN_POINT('Ctrl Pts',(-1.93069049565776,0.50568487910749,9.74220864345877));
#37380=CARTESIAN_POINT('Ctrl Pts',(-1.47136594843111,-1.34846713542859,
9.85339506328992));
#37381=CARTESIAN_POINT('Ctrl Pts',(0.335792850651442,-1.96736556142493,
9.9645814831211));
#37382=CARTESIAN_POINT('Ctrl Pts',(1.83535233538869,-0.784070240605622,
10.0757679029522));
#37383=CARTESIAN_POINT('Ctrl Pts',(1.65364659137136,1.11746450372967,10.1869543227834));
#37384=CARTESIAN_POINT('Ctrl Pts',(-0.0428657180698079,1.99535886614283,
10.2981407426146));
#37385=CARTESIAN_POINT('Ctrl Pts',(-1.70012155281541,1.04540731136874,10.4093271624457));
#37386=CARTESIAN_POINT('Ctrl Pts',(-1.79997252133044,-0.862162458906591,
10.5205135822769));
#37387=CARTESIAN_POINT('Ctrl Pts',(-0.251008199743871,-1.97999253599851,
10.6317000021081));
#37388=CARTESIAN_POINT('Ctrl Pts',(1.52796215902707,-1.28399021223231,10.7428864219392));
#37389=CARTESIAN_POINT('Ctrl Pts',(1.90711651044001,0.588063231359589,10.8540728417704));
#37390=CARTESIAN_POINT('Ctrl Pts',(0.539529066393858,1.92169106390877,10.9652592616015));
#37391=CARTESIAN_POINT('Ctrl Pts',(-1.32278503412967,1.49446025304978,11.0764456814327));
#37392=CARTESIAN_POINT('Ctrl Pts',(-1.97242652143987,-0.300795429882017,
11.1876321012639));
#37393=CARTESIAN_POINT('Ctrl Pts',(-0.817058724297523,-1.82236293883171,
11.2988185210951));
#37394=CARTESIAN_POINT('Ctrl Pts',(1.09041866382002,-1.67090592797485,11.4100049409262));
#37395=CARTESIAN_POINT('Ctrl Pts',(1.69055718360052,-0.554926552610627,
11.4841292208136));
#37396=CARTESIAN_POINT('Ctrl Pts',(1.6883199391646,0.00672513670271936,
11.5211913607574));
#37397=CARTESIAN_POINT('Ctrl Pts',(-0.802959149489932,1.63459616787394,
-0.0766913607573554));
#37398=CARTESIAN_POINT('Ctrl Pts',(-1.34673860605774,1.36747655843322,-0.0396292208136346));
#37399=CARTESIAN_POINT('Ctrl Pts',(-2.13734155664247,0.252529773779836,
0.0344950590738073));
#37400=CARTESIAN_POINT('Ctrl Pts',(-1.36915832429422,-1.66322257224481,
0.14568147890497));
#37401=CARTESIAN_POINT('Ctrl Pts',(0.655021664869751,-2.05011034068591,
0.256867898736133));
#37402=CARTESIAN_POINT('Ctrl Pts',(2.0782545237117,-0.561654367873057,0.368054318567295));
#37403=CARTESIAN_POINT('Ctrl Pts',(1.59819640148463,1.44267659192936,0.479240738398458));
#37404=CARTESIAN_POINT('Ctrl Pts',(-0.346130996849898,2.12473254047885,
0.590427158229621));
#37405=CARTESIAN_POINT('Ctrl Pts',(-1.97325502634714,0.860819657174806,
0.701613578060782));
#37406=CARTESIAN_POINT('Ctrl Pts',(-1.79286136672128,-1.19184009808233,
0.812799997891947));
#37407=CARTESIAN_POINT('Ctrl Pts',(0.0299076046828686,-2.15261823504807,
0.923986417723108));
#37408=CARTESIAN_POINT('Ctrl Pts',(1.82526073013706,-1.14155950949091,1.03517283755427));
#37409=CARTESIAN_POINT('Ctrl Pts',(1.94860591616173,0.915246053141843,1.14635925738543));
#37410=CARTESIAN_POINT('Ctrl Pts',(0.286938251999433,2.13363139543668,1.2575456772166));
#37411=CARTESIAN_POINT('Ctrl Pts',(-1.63757451921909,1.39752576117334,1.36873209704776));
#37412=CARTESIAN_POINT('Ctrl Pts',(-2.0619994469249,-0.618778274775138,
1.47991851687892));
#37413=CARTESIAN_POINT('Ctrl Pts',(-0.597542656570052,-2.06825237330522,
1.59110493671008));
#37414=CARTESIAN_POINT('Ctrl Pts',(1.41428872795678,-1.62311872087351,1.70229135654125));
#37415=CARTESIAN_POINT('Ctrl Pts',(2.13057049201279,0.308862702088754,1.81347777637241));
#37416=CARTESIAN_POINT('Ctrl Pts',(0.895157141781652,1.95791217246742,1.92466419620357));
#37417=CARTESIAN_POINT('Ctrl Pts',(-1.16025892730732,1.81342931797682,2.03585061603473));
#37418=CARTESIAN_POINT('Ctrl Pts',(-2.15282751312695,0.00776644692787891,
2.1470370358659));
#37419=CARTESIAN_POINT('Ctrl Pts',(-1.173312682795,-1.80501078038335,2.25822345569706));
#37420=CARTESIAN_POINT('Ctrl Pts',(0.881007459369614,-1.96431984868673,
2.36940987552822));
#37421=CARTESIAN_POINT('Ctrl Pts',(2.12828655167567,-0.324226703065412,
2.48059629535939));
#37422=CARTESIAN_POINT('Ctrl Pts',(1.42596282698117,1.6128721621003,2.59178271519055));
#37423=CARTESIAN_POINT('Ctrl Pts',(-0.582604709802392,2.07251015763547,
2.70296913502171));
#37424=CARTESIAN_POINT('Ctrl Pts',(-2.05748105739819,0.633638933400953,
2.81415555485287));
#37425=CARTESIAN_POINT('Ctrl Pts',(-1.6476154945659,-1.38567304257714,2.92534197468403));
#37426=CARTESIAN_POINT('Ctrl Pts',(0.271537341065049,-2.13564839618882,
3.0365283945152));
#37427=CARTESIAN_POINT('Ctrl Pts',(1.9419501920302,-0.92927716590924,3.14771481434636));
#37428=CARTESIAN_POINT('Ctrl Pts',(1.83345241771109,1.12835226385271,3.25890123417753));
#37429=CARTESIAN_POINT('Ctrl Pts',(0.045432686513366,2.15236206769919,3.37008765400868));
#37430=CARTESIAN_POINT('Ctrl Pts',(-1.78420535659039,1.20471483967528,3.48127407383985));
#37431=CARTESIAN_POINT('Ctrl Pts',(-1.97943388729784,-0.8465034466758,3.59246049367101));
#37432=CARTESIAN_POINT('Ctrl Pts',(-0.361415101720502,-2.12228785127793,
3.70364691350217));
#37433=CARTESIAN_POINT('Ctrl Pts',(1.58767559662444,-1.45396451102085,3.81483333333334));
#37434=CARTESIAN_POINT('Ctrl Pts',(2.08238656893164,0.546253399951339,3.9260197531645));
#37435=CARTESIAN_POINT('Ctrl Pts',(0.669541102087431,2.04607949797729,4.03720617299566));
#37436=CARTESIAN_POINT('Ctrl Pts',(-1.35663306156047,1.67160800898631,4.14839259282683));
#37437=CARTESIAN_POINT('Ctrl Pts',(-2.14007248481188,-0.234128937078206,
4.25957901265799));
#37438=CARTESIAN_POINT('Ctrl Pts',(-0.963112667326238,-1.92539361935742,
4.37076543248915));
#37439=CARTESIAN_POINT('Ctrl Pts',(1.09610013699538,-1.85291421525797,4.48195185232032));
#37440=CARTESIAN_POINT('Ctrl Pts',(2.15123766275159,-0.0830850033729405,
4.59313827215147));
#37441=CARTESIAN_POINT('Ctrl Pts',(1.23574816038915,1.76285367615161,4.70432469198265));
#37442=CARTESIAN_POINT('Ctrl Pts',(-0.811740268440561,1.99394190888763,
4.8155111118138));
#37443=CARTESIAN_POINT('Ctrl Pts',(-2.11563939493572,0.398492848144611,
4.92669753164497));
#37444=CARTESIAN_POINT('Ctrl Pts',(-1.48152105102257,-1.56199294966507,
5.03788395147612));
#37445=CARTESIAN_POINT('Ctrl Pts',(0.509734849759847,-2.0916254402657,5.1490703713073));
#37446=CARTESIAN_POINT('Ctrl Pts',(2.03405151388631,-0.705238284754304,
5.26025679113844));
#37447=CARTESIAN_POINT('Ctrl Pts',(1.69508874624462,1.32717773556567,5.37144321096963));
#37448=CARTESIAN_POINT('Ctrl Pts',(-0.19664885248515,2.1438413719869,5.48262963080077));
#37449=CARTESIAN_POINT('Ctrl Pts',(-1.90824757094816,0.996653303509719,
5.59381605063195));
#37450=CARTESIAN_POINT('Ctrl Pts',(-1.87180872723762,-1.06351242967042,
5.70500247046309));
#37451=CARTESIAN_POINT('Ctrl Pts',(-0.12071188305083,-2.14945463797604,
5.81618889029427));
#37452=CARTESIAN_POINT('Ctrl Pts',(1.74096228296046,-1.26640314621194,5.92737531012542));
#37453=CARTESIAN_POINT('Ctrl Pts',(2.00783946807991,0.776728568965356,6.0385617299566));
#37454=CARTESIAN_POINT('Ctrl Pts',(0.435448592570146,2.10834321747079,6.14974814978775));
#37455=CARTESIAN_POINT('Ctrl Pts',(-1.53583208518367,1.50862401066228,6.26093456961893));
#37456=CARTESIAN_POINT('Ctrl Pts',(-2.10022394255324,-0.473060239877022,
6.37212098945007));
#37457=CARTESIAN_POINT('Ctrl Pts',(-0.74071955267899,-2.02140078749996,
6.48330740928124));
#37458=CARTESIAN_POINT('Ctrl Pts',(1.29731608273796,-1.71805051756223,6.5944938291124));
#37459=CARTESIAN_POINT('Ctrl Pts',(2.14695390376071,0.15910856216126,6.70568024894357));
#37460=CARTESIAN_POINT('Ctrl Pts',(1.02988880574655,1.89051729619815,6.81686666877473));
#37461=CARTESIAN_POINT('Ctrl Pts',(-1.03059911890458,1.89013016894061,6.92805308860589));
#37462=CARTESIAN_POINT('Ctrl Pts',(-2.14701353924984,0.158301805751674,
7.03923950843705));
#37463=CARTESIAN_POINT('Ctrl Pts',(-1.29667041186295,-1.71853787925252,
7.15042592826822));
#37464=CARTESIAN_POINT('Ctrl Pts',(0.741479067384996,-2.0211223100189,7.26161234809938));
#37465=CARTESIAN_POINT('Ctrl Pts',(2.10040155266868,-0.472271020678894,
7.37279876793055));
#37466=CARTESIAN_POINT('Ctrl Pts',(1.53526509213771,1.50920101255294,7.48398518776171));
#37467=CARTESIAN_POINT('Ctrl Pts',(-0.436240798549652,2.10817944328893,
7.59517160759286));
#37468=CARTESIAN_POINT('Ctrl Pts',(-2.00813119194563,0.775974042967894,
7.70635802742404));
#37469=CARTESIAN_POINT('Ctrl Pts',(-1.74048629299744,-1.26705724547931,
7.81754444725519));
#37470=CARTESIAN_POINT('Ctrl Pts',(0.121519559390324,-2.14940912720278,
7.92873086708636));
#37471=CARTESIAN_POINT('Ctrl Pts',(1.87220822337856,-1.06280899870737,8.03991728691751));
#37472=CARTESIAN_POINT('Ctrl Pts',(1.90787293110882,0.997370281398245,8.15110370674869));
#37473=CARTESIAN_POINT('Ctrl Pts',(0.195843262983046,2.1439151139204,8.26229012657984));
#37474=CARTESIAN_POINT('Ctrl Pts',(-1.69558733042143,1.32654069078969,8.37347654641101));
#37475=CARTESIAN_POINT('Ctrl Pts',(-2.03378636810517,-0.706002555693802,
8.48466296624217));
#37476=CARTESIAN_POINT('Ctrl Pts',(-0.508948858861673,-2.09181683182873,
8.59584938607333));
#37477=CARTESIAN_POINT('Ctrl Pts',(1.48210788489943,-1.56143613926181,8.70703580590451));
#37478=CARTESIAN_POINT('Ctrl Pts',(2.11548950721726,0.399287798761521,8.81822222573564));
#37479=CARTESIAN_POINT('Ctrl Pts',(0.810990961415923,1.99424678906897,8.92940864556684));
#37480=CARTESIAN_POINT('Ctrl Pts',(-1.23641048638147,1.76238920508216,9.04059506539797));
#37481=CARTESIAN_POINT('Ctrl Pts',(-2.15120629331062,-0.0838933551026959,
9.15178148522916));
#37482=CARTESIAN_POINT('Ctrl Pts',(-1.09540379848118,-1.85332595276186,
9.26296790506031));
#37483=CARTESIAN_POINT('Ctrl Pts',(0.963836080712942,-1.9250315915564,9.37415432489147));
#37484=CARTESIAN_POINT('Ctrl Pts',(2.14016032912378,-0.233324742234878,
9.48534074472264));
#37485=CARTESIAN_POINT('Ctrl Pts',(1.35600480268067,1.67211762704833,9.5965271645538));
#37486=CARTESIAN_POINT('Ctrl Pts',(-0.67030982818557,2.04582783352242,9.70771358438496));
#37487=CARTESIAN_POINT('Ctrl Pts',(-2.08259181106143,0.545470747680921,
9.81890000421612));
#37488=CARTESIAN_POINT('Ctrl Pts',(-1.58712889620009,-1.45456074914393,
9.93008642404728));
#37489=CARTESIAN_POINT('Ctrl Pts',(0.362212090727357,-2.12215236818265,
10.0412728438785));
#37490=CARTESIAN_POINT('Ctrl Pts',(1.97975271162804,-0.845758688953388,
10.1524592637096));
#37491=CARTESIAN_POINT('Ctrl Pts',(1.78375086909329,1.20538347801125,10.2636456835408));
#37492=CARTESIAN_POINT('Ctrl Pts',(-0.0462382725911752,2.15234810763501,
10.3748321033719));
#37493=CARTESIAN_POINT('Ctrl Pts',(-1.83388235020868,1.12765702777161,10.4860185232031));
#37494=CARTESIAN_POINT('Ctrl Pts',(-1.94158931298892,-0.929994984054507,
10.5972049430343));
#37495=CARTESIAN_POINT('Ctrl Pts',(-0.270756821184746,-2.13577279771527,
10.7083913628654));
#37496=CARTESIAN_POINT('Ctrl Pts',(1.64817793797518,-1.38501096239512,10.8195777826966));
#37497=CARTESIAN_POINT('Ctrl Pts',(2.0571630907777,0.634330397736036,10.9307642025277));
#37498=CARTESIAN_POINT('Ctrl Pts',(0.58197770073898,2.07288432925282,11.0419506223589));
#37499=CARTESIAN_POINT('Ctrl Pts',(-1.42685805211597,1.61204019596003,11.1531370421901));
#37500=CARTESIAN_POINT('Ctrl Pts',(-2.12761151034289,-0.324461171008946,
11.2643234620212));
#37501=CARTESIAN_POINT('Ctrl Pts',(-0.881342614057178,-1.96574134576644,
11.3755098818524));
#37502=CARTESIAN_POINT('Ctrl Pts',(1.17620974724197,-1.80236812191326,11.4866963016836));
#37503=CARTESIAN_POINT('Ctrl Pts',(1.82356548323819,-0.598586618003602,
11.560820581571));
#37504=CARTESIAN_POINT('Ctrl Pts',(1.82115221868229,0.00725425160419088,
11.5978827215147));
#37505=CARTESIAN_POINT('Ctrl Pts',(-0.861525859670525,1.75382131162755,
-1.38777878078145E-16));
#37506=CARTESIAN_POINT('Ctrl Pts',(-1.44496782441849,1.46721837385112,0.0370621399437207));
#37507=CARTESIAN_POINT('Ctrl Pts',(-2.29323624142731,0.270948940037977,
0.111186419831162));
#37508=CARTESIAN_POINT('Ctrl Pts',(-1.4690228053469,-1.78453568564088,0.222372839662325));
#37509=CARTESIAN_POINT('Ctrl Pts',(0.702798023147504,-2.19964250335881,
0.333559259493488));
#37510=CARTESIAN_POINT('Ctrl Pts',(2.22983948348091,-0.602620646924488,
0.44474567932465));
#37511=CARTESIAN_POINT('Ctrl Pts',(1.71476659751129,1.54790339194469,0.555932099155814));
#37512=CARTESIAN_POINT('Ctrl Pts',(-0.371377304572895,2.2797075413722,0.667118518986976));
#37513=CARTESIAN_POINT('Ctrl Pts',(-2.11718147056775,0.923606631345987,
0.778304938818138));
#37514=CARTESIAN_POINT('Ctrl Pts',(-1.92363015131696,-1.2787712372945,0.889491358649302));
#37515=CARTESIAN_POINT('Ctrl Pts',(0.0320890232727887,-2.30962717925356,
1.00067777848046));
#37516=CARTESIAN_POINT('Ctrl Pts',(1.95839267869742,-1.22482325334233,1.11186419831163));
#37517=CARTESIAN_POINT('Ctrl Pts',(2.09073448897961,0.982002812028443,1.22305061814279));
#37518=CARTESIAN_POINT('Ctrl Pts',(0.3078671242282,2.28925546628532,1.33423703797395));
#37519=CARTESIAN_POINT('Ctrl Pts',(-1.75701689972769,1.49945932314417,1.44542345780511));
#37520=CARTESIAN_POINT('Ctrl Pts',(-2.21239878427269,-0.663911091192784,
1.55660987763628));
#37521=CARTESIAN_POINT('Ctrl Pts',(-0.641126576885465,-2.21910779030204,
1.66779629746744));
#37522=CARTESIAN_POINT('Ctrl Pts',(1.51744495713052,-1.74150671579767,1.7789827172986));
#37523=CARTESIAN_POINT('Ctrl Pts',(2.28597130487397,0.331390712847842,1.89016913712977));
#37524=CARTESIAN_POINT('Ctrl Pts',(0.960448643749269,2.10071953052146,2.00135555696093));
#37525=CARTESIAN_POINT('Ctrl Pts',(-1.24488658037438,1.94569829998722,2.11254197679209));
#37526=CARTESIAN_POINT('Ctrl Pts',(-2.30985172178094,0.00833292063536468,
2.22372839662325));
#37527=CARTESIAN_POINT('Ctrl Pts',(-1.2588924584139,-1.93666572611094,2.33491481645442));
#37528=CARTESIAN_POINT('Ctrl Pts',(0.945266903418065,-2.10759457362527,
2.44610123628558));
#37529=CARTESIAN_POINT('Ctrl Pts',(2.28352077714336,-0.347875342430591,
2.55728765611674));
#37530=CARTESIAN_POINT('Ctrl Pts',(1.52997054850621,1.73051278744978,2.6684740759479));
#37531=CARTESIAN_POINT('Ctrl Pts',(-0.625099077306038,2.22367613142842,
2.77966049577907));
#37532=CARTESIAN_POINT('Ctrl Pts',(-2.20755082977362,0.679855665342084,
2.89084691561023));
#37533=CARTESIAN_POINT('Ctrl Pts',(-1.76779024968342,-1.48674208393651,
3.00203333544139));
#37534=CARTESIAN_POINT('Ctrl Pts',(0.291342892527361,-2.29141958423335,
3.11321975527256));
#37535=CARTESIAN_POINT('Ctrl Pts',(2.08359330569799,-0.997057334412016,
3.22440617510372));
#37536=CARTESIAN_POINT('Ctrl Pts',(1.96718185643314,1.21065268979674,3.33559259493488));
#37537=CARTESIAN_POINT('Ctrl Pts',(0.0487464827201324,2.30935232741881,
3.44677901476604));
#37538=CARTESIAN_POINT('Ctrl Pts',(-1.91434278399063,1.29258504441778,3.55796543459721));
#37539=CARTESIAN_POINT('Ctrl Pts',(-2.12381100893932,-0.908246216603541,
3.66915185442837));
#37540=CARTESIAN_POINT('Ctrl Pts',(-0.38777621054007,-2.27708453998192,
3.78033827425954));
#37541=CARTESIAN_POINT('Ctrl Pts',(1.70347841995286,-1.56001463596674,3.89152469409069));
#37542=CARTESIAN_POINT('Ctrl Pts',(2.23427291426326,0.58609635407974,4.00271111392186));
#37543=CARTESIAN_POINT('Ctrl Pts',(0.718376487679439,2.19531765665651,4.11389753375301));
#37544=CARTESIAN_POINT('Ctrl Pts',(-1.45558396757891,1.79353274433565,4.22508395358419));
#37545=CARTESIAN_POINT('Ctrl Pts',(-2.29616635965357,-0.251205972206891,
4.33627037341534));
#37546=CARTESIAN_POINT('Ctrl Pts',(-1.03336074967814,-2.06582911991821,
4.44745679324651));
#37547=CARTESIAN_POINT('Ctrl Pts',(1.17604813820203,-1.98806317010017,4.55864321307767));
#37548=CARTESIAN_POINT('Ctrl Pts',(2.30814590995695,-0.0891451065749571,
4.66982963290884));
#37549=CARTESIAN_POINT('Ctrl Pts',(1.32588189186442,1.89143374203362,4.78101605273999));
#37550=CARTESIAN_POINT('Ctrl Pts',(-0.870947461077787,2.1393772252035,4.89220247257116));
#37551=CARTESIAN_POINT('Ctrl Pts',(-2.26995115459196,0.427558355600586,
5.00338889240232));
#37552=CARTESIAN_POINT('Ctrl Pts',(-1.58958111120973,-1.67592251687317,
5.11457531223348));
#37553=CARTESIAN_POINT('Ctrl Pts',(0.546914192237968,-2.24418565586851,
5.22576173206465));
#37554=CARTESIAN_POINT('Ctrl Pts',(2.1824123683356,-0.756677372605439,5.33694815189581));
#37555=CARTESIAN_POINT('Ctrl Pts',(1.81872613351991,1.4239802115651,5.44813457172697));
#37556=CARTESIAN_POINT('Ctrl Pts',(-0.210992142997687,2.30021014415434,
5.55932099155813));
#37557=CARTESIAN_POINT('Ctrl Pts',(-2.04743246287144,1.06934779265563,5.67050741138931));
#37558=CARTESIAN_POINT('Ctrl Pts',(-2.00833582118916,-1.14108352937273,
5.78169383122044));
#37559=CARTESIAN_POINT('Ctrl Pts',(-0.129516437895867,-2.30623283386393,
5.89288025105164));
#37560=CARTESIAN_POINT('Ctrl Pts',(1.86794562143574,-1.35877280920554,6.00406667088277));
#37561=CARTESIAN_POINT('Ctrl Pts',(2.15428845280213,0.83338205752262,6.11525309071395));
#37562=CARTESIAN_POINT('Ctrl Pts',(0.467209600008474,2.26212280421227,6.22643951054511));
#37563=CARTESIAN_POINT('Ctrl Pts',(-1.64785351575852,1.61866092257753,6.33762593037627));
#37564=CARTESIAN_POINT('Ctrl Pts',(-2.25341132081031,-0.507564587930634,
6.44881235020743));
#37565=CARTESIAN_POINT('Ctrl Pts',(-0.794746594271866,-2.1688389157728,
6.55999877003859));
#37566=CARTESIAN_POINT('Ctrl Pts',(1.39194049181108,-1.84336270411821,6.67118518986976));
#37567=CARTESIAN_POINT('Ctrl Pts',(2.30354969961477,0.170713716736379,6.78237160970093));
#37568=CARTESIAN_POINT('Ctrl Pts',(1.1050074456459,2.02840896683692,6.89355802953208));
#37569=CARTESIAN_POINT('Ctrl Pts',(-1.10576956804586,2.02799360306213,7.00474444936325));
#37570=CARTESIAN_POINT('Ctrl Pts',(-2.30361368483253,0.169848116649841,
7.11593086919441));
#37571=CARTESIAN_POINT('Ctrl Pts',(-1.39124772661127,-1.84388561328419,
7.22711728902557));
#37572=CARTESIAN_POINT('Ctrl Pts',(0.795561506911461,-2.16854012653626,
7.33830370885674));
#37573=CARTESIAN_POINT('Ctrl Pts',(2.25360188555757,-0.506717804195071,
7.44949012868789));
#37574=CARTESIAN_POINT('Ctrl Pts',(1.64724516703786,1.61928001017393,7.56067654851907));
#37575=CARTESIAN_POINT('Ctrl Pts',(-0.468059588377044,2.26194708457211,
7.67186296835021));
#37576=CARTESIAN_POINT('Ctrl Pts',(-2.154601454596,0.832572497460946,7.78304938818139));
#37577=CARTESIAN_POINT('Ctrl Pts',(-1.8674349134348,-1.35947461755279,7.89423580801255));
#37578=CARTESIAN_POINT('Ctrl Pts',(0.130383025010703,-2.30618400359892,
8.00542222784371));
#37579=CARTESIAN_POINT('Ctrl Pts',(2.00876445601631,-1.14032879114536,8.11660864767487));
#37580=CARTESIAN_POINT('Ctrl Pts',(2.04703049732954,1.07011706590215,8.22779506750604));
#37581=CARTESIAN_POINT('Ctrl Pts',(0.210127794931219,2.30028926472067,8.3389814873372));
#37582=CARTESIAN_POINT('Ctrl Pts',(-1.81926108372479,1.42329670163983,8.45016790716836));
#37583=CARTESIAN_POINT('Ctrl Pts',(-2.18212788319439,-0.757497388391501,
8.56135432699953));
#37584=CARTESIAN_POINT('Ctrl Pts',(-0.546070872270014,-2.24439100726275,
8.67254074683069));
#37585=CARTESIAN_POINT('Ctrl Pts',(1.59021074792356,-1.67532509350284,8.78372716666185));
#37586=CARTESIAN_POINT('Ctrl Pts',(2.26979033427429,0.428411288796547,8.89491358649301));
#37587=CARTESIAN_POINT('Ctrl Pts',(0.870143500653468,2.13970434291613,9.00610000632417));
#37588=CARTESIAN_POINT('Ctrl Pts',(-1.32659252698235,1.89093539309814,9.11728642615534));
#37589=CARTESIAN_POINT('Ctrl Pts',(-2.30811225247311,-0.0900124183420705,
9.2284728459865));
#37590=CARTESIAN_POINT('Ctrl Pts',(-1.17530100973675,-1.98850493915805,
9.33965926581767));
#37591=CARTESIAN_POINT('Ctrl Pts',(1.03413692781901,-2.06544068631896,9.45084568564882));
#37592=CARTESIAN_POINT('Ctrl Pts',(2.29626061120593,-0.250343120523647,
9.56203210547999));
#37593=CARTESIAN_POINT('Ctrl Pts',(1.45490988438074,1.79407953322179,9.67321852531115));
#37594=CARTESIAN_POINT('Ctrl Pts',(-0.719201283577143,2.19504763615053,
9.78440494514231));
#37595=CARTESIAN_POINT('Ctrl Pts',(-2.2344931264651,0.585256616254353,9.89559136497349));
#37596=CARTESIAN_POINT('Ctrl Pts',(-1.70289184396906,-1.56065436285928,
10.0067777848046));
#37597=CARTESIAN_POINT('Ctrl Pts',(0.388631330803272,-2.27693917494037,
10.1179642046358));
#37598=CARTESIAN_POINT('Ctrl Pts',(2.1241530878674,-0.907447137301155,10.229150624467));
#37599=CARTESIAN_POINT('Ctrl Pts',(1.91385514681521,1.29330245229283,10.3403370442981));
#37600=CARTESIAN_POINT('Ctrl Pts',(-0.0496108271125438,2.30933734912719,
10.4515234641293));
#37601=CARTESIAN_POINT('Ctrl Pts',(-1.96764314760194,1.20990674417448,10.5627098839605));
#37602=CARTESIAN_POINT('Ctrl Pts',(-2.08320610464741,-0.997827509202423,
10.6738963037916));
#37603=CARTESIAN_POINT('Ctrl Pts',(-0.290505442625618,-2.29155305943203,
10.7850827236228));
#37604=CARTESIAN_POINT('Ctrl Pts',(1.7683937169233,-1.48603171255794,10.8962691434539));
#37605=CARTESIAN_POINT('Ctrl Pts',(2.20720967111538,0.680597564112484,11.0074555632851));
#37606=CARTESIAN_POINT('Ctrl Pts',(0.624426335084105,2.22407759459687,11.1186419831163));
#37607=CARTESIAN_POINT('Ctrl Pts',(-1.53093107010227,1.72962013887028,11.2298284029474));
#37608=CARTESIAN_POINT('Ctrl Pts',(-2.28279649924591,-0.348126912135875,
11.3410148227786));
#37609=CARTESIAN_POINT('Ctrl Pts',(-0.945626503816835,-2.10911975270116,
11.4522012426097));
#37610=CARTESIAN_POINT('Ctrl Pts',(1.26200083066393,-1.93383031585166,11.5633876624409));
#37611=CARTESIAN_POINT('Ctrl Pts',(1.95657378287586,-0.642246683396576,
11.6375119423284));
#37612=CARTESIAN_POINT('Ctrl Pts',(1.95398449819998,0.0077833665056624,
11.6745740822721));
#37613=CARTESIAN_POINT('Ctrl Pts',(-1.95093054978418,-0.000550606481354719,
10.6241303078758));
#37614=CARTESIAN_POINT('Ctrl Pts',(-1.95166977968097,-0.292567552961119,
10.640718973181));
#37615=CARTESIAN_POINT('Ctrl Pts',(-1.89027401228485,-0.584289311968449,
10.6573076384863));
#37616=CARTESIAN_POINT('Ctrl Pts',(-1.7651621681362,-0.845492725344543,
10.6738963037916));
#37617=CARTESIAN_POINT('Ctrl Pts',(-1.48563921730681,-1.42906935927896,
10.7109584437353));
#37618=CARTESIAN_POINT('Ctrl Pts',(-0.888072329966215,-1.8603112093555,
10.7480205836791));
#37619=CARTESIAN_POINT('Ctrl Pts',(-0.246139026371096,-1.94167857658142,
10.7850827236228));
#37620=CARTESIAN_POINT('Ctrl Pts',(0.395794277224022,-2.02304594380734,
10.8221448635665));
#37621=CARTESIAN_POINT('Ctrl Pts',(1.08209399707366,-1.75453882818264,10.8592070035102));
#37622=CARTESIAN_POINT('Ctrl Pts',(1.49837984936383,-1.25918039092522,10.8962691434539));
#37623=CARTESIAN_POINT('Ctrl Pts',(1.91466570165399,-0.763821953667804,
10.9333312833977));
#37624=CARTESIAN_POINT('Ctrl Pts',(2.06093768638468,-0.041612194777677,
10.9703934233414));
#37625=CARTESIAN_POINT('Ctrl Pts',(1.87027645607817,0.576739356414784,11.0074555632851));
#37626=CARTESIAN_POINT('Ctrl Pts',(1.80418088670294,0.791100177355746,11.0203037088567));
#37627=CARTESIAN_POINT('Ctrl Pts',(1.69759382901609,0.992979671982257,11.0331518544284));
#37628=CARTESIAN_POINT('Ctrl Pts',(1.56057659382855,1.17255425406022,11.046));
#37629=CARTESIAN_POINT('Ctrl Pts',(-0.9055496143049,-1.2679201530598,4.59701721133854E-17));
#37630=CARTESIAN_POINT('Ctrl Pts',(-0.937460871048188,-1.25085822491965,
4.11134559556874E-17));
#37631=CARTESIAN_POINT('Ctrl Pts',(-0.968677330061127,-1.23263760516135,
2.44937731663795E-16));
#37632=CARTESIAN_POINT('Ctrl Pts',(-0.999128467894991,-1.21327242330634,
1.95156391047391E-16));
#37633=CARTESIAN_POINT('Ctrl Pts',(-1.04916478169554,-1.18145218981002,
1.19833509668E-16));
#37634=CARTESIAN_POINT('Ctrl Pts',(-1.09713600671012,-1.14654455097205,
1.20483738925504E-16));
#37635=CARTESIAN_POINT('Ctrl Pts',(-1.14296368523792,-1.10887020140839,
3.46944695195361E-17));
#37636=CARTESIAN_POINT('Ctrl Pts',(-1.1691715546085,-1.08732504652154,-1.4366579135275E-17));
#37637=CARTESIAN_POINT('Ctrl Pts',(-1.19467812556179,-1.06487409533188,
1.54611493479508E-16));
#37638=CARTESIAN_POINT('Ctrl Pts',(-1.21946596262297,-1.04157045589269,
1.28369537222284E-16));
#37639=CARTESIAN_POINT('Ctrl Pts',(-1.23288807387334,-1.02895200756582,
1.14160049906282E-16));
#37640=CARTESIAN_POINT('Ctrl Pts',(-1.24610308792281,-1.01607950194371,
2.35779340588765E-16));
#37641=CARTESIAN_POINT('Ctrl Pts',(-1.25908578368524,-1.0029839550804,2.28983498828939E-16));
#37642=CARTESIAN_POINT('Ctrl Pts',(-1.30296735026586,-0.95872095130156,
2.06013524941215E-16));
#37643=CARTESIAN_POINT('Ctrl Pts',(-1.34424080059494,-0.911874911049719,
3.41092537496216E-16));
#37644=CARTESIAN_POINT('Ctrl Pts',(-1.3828175432908,-0.862794893107178,
2.15105711021124E-16));
#37645=CARTESIAN_POINT('Ctrl Pts',(-1.41246270387874,-0.825078255778903,
1.18288316865636E-16));
#37646=CARTESIAN_POINT('Ctrl Pts',(-1.44051505756546,-0.786041114269597,
-3.41744083773187E-17));
#37647=CARTESIAN_POINT('Ctrl Pts',(-1.46692433972057,-0.745823635123971,
-2.77555756156289E-17));
#37648=CARTESIAN_POINT('Ctrl Pts',(-1.479951210132,-0.725985614308893,-2.45893667770833E-17));
#37649=CARTESIAN_POINT('Ctrl Pts',(-1.49257814628919,-0.705860181165347,
1.12314029669873E-16));
#37650=CARTESIAN_POINT('Ctrl Pts',(-1.50479813274716,-0.685463000140721,
1.31838984174237E-16));
#37651=CARTESIAN_POINT('Ctrl Pts',(-1.51107691151866,-0.674982678607113,
1.41871145034493E-16));
#37652=CARTESIAN_POINT('Ctrl Pts',(-1.51724344631134,-0.664438579506566,
2.39743182585592E-16));
#37653=CARTESIAN_POINT('Ctrl Pts',(-1.52329612440982,-0.653835068968427,
2.42861286636753E-16));
#37654=CARTESIAN_POINT('Ctrl Pts',(-1.55541704658302,-0.597563360607725,
2.59408734877987E-16));
#37655=CARTESIAN_POINT('Ctrl Pts',(-1.58434358367058,-0.539605423501723,
2.32306933354682E-17));
#37656=CARTESIAN_POINT('Ctrl Pts',(-1.60998194797531,-0.480314579840224,
1.38777878078145E-17));
#37657=CARTESIAN_POINT('Ctrl Pts',(-1.63611695660561,-0.419875204988797,
4.34370584461709E-18));
#37658=CARTESIAN_POINT('Ctrl Pts',(-1.65883591999594,-0.358049987819819,
-3.99522282745635E-16));
#37659=CARTESIAN_POINT('Ctrl Pts',(-1.67800508733892,-0.295172269836945,
-4.02455846426619E-16));
#37660=CARTESIAN_POINT('Ctrl Pts',(-1.69036857863681,-0.254618180804147,
-4.04347899868101E-16));
#37661=CARTESIAN_POINT('Ctrl Pts',(-1.70125468815875,-0.21362546632645,
2.10692284276142E-16));
#37662=CARTESIAN_POINT('Ctrl Pts',(-1.71061789501208,-0.172277279535232,
2.22044604925031E-16));
#37663=CARTESIAN_POINT('Ctrl Pts',(-1.71585060492304,-0.149169484288187,
2.28388948449886E-16));
#37664=CARTESIAN_POINT('Ctrl Pts',(-1.72060753217063,-0.125950592727189,
-7.81124113857471E-17));
#37665=CARTESIAN_POINT('Ctrl Pts',(-1.72487954070067,-0.102634681883505,
-6.93889390390723E-17));
#37666=CARTESIAN_POINT('Ctrl Pts',(-1.72700542719079,-0.0910319475914671,
-6.50478634353357E-17));
#37667=CARTESIAN_POINT('Ctrl Pts',(-1.7290114810898,-0.0794035343790101,
3.2530658909822E-16));
#37668=CARTESIAN_POINT('Ctrl Pts',(-1.73089565945358,-0.0677563287869385,
3.05311331771918E-16));
#37669=CARTESIAN_POINT('Ctrl Pts',(-1.74172479313661,-0.000815136373784872,
1.90390516006322E-16));
#37670=CARTESIAN_POINT('Ctrl Pts',(-1.74848828323664,0.0664709663887247,
1.66332759660732E-17));
#37671=CARTESIAN_POINT('Ctrl Pts',(-1.75106678678907,0.133744024330042,
0.));
#37672=CARTESIAN_POINT('Ctrl Pts',(-1.75197767455289,0.157509050853062,
-5.87590718476407E-18));
#37673=CARTESIAN_POINT('Ctrl Pts',(-1.75236592486458,0.181272742240003,
-1.43574718418596E-16));
#37674=CARTESIAN_POINT('Ctrl Pts',(-1.75222496230419,0.20502014676713,-1.52655665885959E-16));
#37675=CARTESIAN_POINT('Ctrl Pts',(-1.75184009030703,0.269858008556557,
-1.89868827307373E-16));
#37676=CARTESIAN_POINT('Ctrl Pts',(-1.74751402866387,0.334573792851957,
-3.30194805135327E-16));
#37677=CARTESIAN_POINT('Ctrl Pts',(-1.7394637798186,0.398932034828451,-3.60822483003176E-16));
#37678=CARTESIAN_POINT('Ctrl Pts',(-1.73512917103287,0.433585348839861,
-3.77313774654407E-16));
#37679=CARTESIAN_POINT('Ctrl Pts',(-1.72971393872322,0.468135193807322,
-2.30290250750647E-16));
#37680=CARTESIAN_POINT('Ctrl Pts',(-1.72324590502527,0.502545438383202,
-2.22044604925031E-16));
#37681=CARTESIAN_POINT('Ctrl Pts',(-1.71875224847293,0.526451903350239,
-2.16315955056648E-16));
#37682=CARTESIAN_POINT('Ctrl Pts',(-1.71375034317529,0.550290993458765,
-1.09112752506388E-16));
#37683=CARTESIAN_POINT('Ctrl Pts',(-1.70824837476028,0.574050543226345,
-1.11022302462516E-16));
#37684=CARTESIAN_POINT('Ctrl Pts',(-1.70556019910987,0.585659087356796,
-1.11955278682682E-16));
#37685=CARTESIAN_POINT('Ctrl Pts',(-1.70275214211861,0.597250589985584,
-1.86923780482983E-17));
#37686=CARTESIAN_POINT('Ctrl Pts',(-1.69982665236451,0.608817432227434,
-2.77555756156289E-17));
#37687=CARTESIAN_POINT('Ctrl Pts',(-1.68323412399998,0.674421202576402,
-7.91594003935956E-17));
#37688=CARTESIAN_POINT('Ctrl Pts',(-1.6629277813761,0.739001412074313,-4.05964646411352E-16));
#37689=CARTESIAN_POINT('Ctrl Pts',(-1.63916833994428,0.802303176749866,
-3.88578058618805E-16));
#37690=CARTESIAN_POINT('Ctrl Pts',(-1.61488642929252,0.866996944840365,
-3.70809140417215E-16));
#37691=CARTESIAN_POINT('Ctrl Pts',(-1.58699772603761,0.930356288581554,
-4.09457680297508E-17));
#37692=CARTESIAN_POINT('Ctrl Pts',(-1.55572518982035,0.992113582996803,
0.));
#37693=CARTESIAN_POINT('Ctrl Pts',(-1.52416508821539,1.05443876420538,4.13222832434933E-17));
#37694=CARTESIAN_POINT('Ctrl Pts',(-1.48915832892389,1.11513327578217,-2.91589739144645E-16));
#37695=CARTESIAN_POINT('Ctrl Pts',(-1.45088203376165,1.17391247934435,-2.77555756156289E-16));
#37696=CARTESIAN_POINT('Ctrl Pts',(-1.43586030613212,1.19698067814596,-2.72048047818399E-16));
#37697=CARTESIAN_POINT('Ctrl Pts',(-1.42033446520901,1.21975369583959,-2.46829292445535E-16));
#37698=CARTESIAN_POINT('Ctrl Pts',(-1.40431321996707,1.24221341255695,-2.22044604925031E-16));
#37699=CARTESIAN_POINT('Ctrl Pts',(-1.39827097600966,1.25068385824148,-2.12697320981403E-16));
#37700=CARTESIAN_POINT('Ctrl Pts',(-1.39215941512485,1.25910802930607,-2.5395452896005E-16));
#37701=CARTESIAN_POINT('Ctrl Pts',(-1.38598454691313,1.26747777400967,-2.4980018054066E-16));
#37702=CARTESIAN_POINT('Ctrl Pts',(-1.3431243018081,1.32557282918544,-2.20964521964367E-16));
#37703=CARTESIAN_POINT('Ctrl Pts',(-1.29714727100707,1.38114651172693,8.67497813555755E-17));
#37704=CARTESIAN_POINT('Ctrl Pts',(-1.24829449348075,1.43391808714502,5.55111512312578E-17));
#37705=CARTESIAN_POINT('Ctrl Pts',(-1.19933005104754,1.48681028483588,2.42011176187261E-17));
#37706=CARTESIAN_POINT('Ctrl Pts',(-1.14747626839011,1.53688856046327,-1.29713890200027E-16));
#37707=CARTESIAN_POINT('Ctrl Pts',(-1.09292624810297,1.58385401467225,-2.77555756156289E-17));
#37708=CARTESIAN_POINT('Ctrl Pts',(-1.03954323648884,1.62981471962349,7.20215071969156E-17));
#37709=CARTESIAN_POINT('Ctrl Pts',(-0.983577547054738,1.67279522220595,
1.33536308196711E-16));
#37710=CARTESIAN_POINT('Ctrl Pts',(-0.92517040004714,1.71248622994896,1.66533453693773E-16));
#37711=CARTESIAN_POINT('Ctrl Pts',(-0.904266808925204,1.72669141954621,
1.78342947445829E-16));
#37712=CARTESIAN_POINT('Ctrl Pts',(-0.883050159709791,1.74047492561567,
-1.31748417511445E-16));
#37713=CARTESIAN_POINT('Ctrl Pts',(-0.861525859670525,1.75382131162755,
-1.38777878078145E-16));
#37714=CARTESIAN_POINT('Origin',(0.,0.,0.));
#37715=CARTESIAN_POINT('Origin',(-0.866025403784439,-1.5,-4.));
#37716=CARTESIAN_POINT('',(-0.866025403784439,-1.5,-4.));
#37717=CARTESIAN_POINT('',(0.866025403784439,-1.5,-4.));
#37718=CARTESIAN_POINT('',(-0.43301270189222,-1.5,-4.));
#37719=CARTESIAN_POINT('',(-0.866025403784439,-1.5,-2.));
#37720=CARTESIAN_POINT('',(-0.866025403784439,-1.5,-4.));
#37721=CARTESIAN_POINT('',(0.866025403784439,-1.5,-2.));
#37722=CARTESIAN_POINT('',(-0.866025403784439,-1.5,-2.));
#37723=CARTESIAN_POINT('',(0.866025403784439,-1.5,-4.));
#37724=CARTESIAN_POINT('Origin',(-1.73205080756888,2.12115047744981E-16,
-4.));
#37725=CARTESIAN_POINT('',(-1.73205080756888,2.12115047744981E-16,-4.));
#37726=CARTESIAN_POINT('',(-1.51554445662277,-0.375,-4.));
#37727=CARTESIAN_POINT('',(-1.73205080756888,2.77555756156289E-16,-2.));
#37728=CARTESIAN_POINT('',(-1.73205080756888,2.12115047744981E-16,-4.));
#37729=CARTESIAN_POINT('',(-1.73205080756888,2.12115047744981E-16,-2.));
#37730=CARTESIAN_POINT('Origin',(-0.866025403784438,1.5,-4.));
#37731=CARTESIAN_POINT('',(-0.866025403784438,1.5,-4.));
#37732=CARTESIAN_POINT('',(-1.08253175473055,1.125,-4.));
#37733=CARTESIAN_POINT('',(-0.866025403784438,1.5,-2.));
#37734=CARTESIAN_POINT('',(-0.866025403784438,1.5,-4.));
#37735=CARTESIAN_POINT('',(-0.866025403784438,1.5,-2.));
#37736=CARTESIAN_POINT('Origin',(0.866025403784439,1.5,-4.));
#37737=CARTESIAN_POINT('',(0.866025403784439,1.5,-4.));
#37738=CARTESIAN_POINT('',(0.43301270189222,1.5,-4.));
#37739=CARTESIAN_POINT('',(0.866025403784439,1.5,-2.));
#37740=CARTESIAN_POINT('',(0.866025403784439,1.5,-4.));
#37741=CARTESIAN_POINT('',(0.866025403784439,1.5,-2.));
#37742=CARTESIAN_POINT('Origin',(1.73205080756888,0.,-4.));
#37743=CARTESIAN_POINT('',(1.73205080756888,0.,-4.));
#37744=CARTESIAN_POINT('',(1.51554445662277,0.375,-4.));
#37745=CARTESIAN_POINT('',(1.73205080756888,0.,-2.));
#37746=CARTESIAN_POINT('',(1.73205080756888,0.,-4.));
#37747=CARTESIAN_POINT('',(1.73205080756888,0.,-2.));
#37748=CARTESIAN_POINT('Origin',(0.866025403784439,-1.5,-4.));
#37749=CARTESIAN_POINT('',(1.08253175473055,-1.125,-4.));
#37750=CARTESIAN_POINT('',(0.866025403784439,-1.5,-2.));
#37751=CARTESIAN_POINT('Origin',(0.,2.77555756156289E-16,-2.));
#37752=CARTESIAN_POINT('Origin',(0.,0.,0.));
#37753=CARTESIAN_POINT('',(-3.5,-4.28626379701574E-16,0.));
#37754=CARTESIAN_POINT('Origin',(0.,0.,0.));
#37755=CARTESIAN_POINT('Origin',(0.,0.,-4.));
#37756=CARTESIAN_POINT('',(-3.5,-4.28626379701574E-16,-4.));
#37757=CARTESIAN_POINT('',(-3.5,-4.28626379701574E-16,-4.));
#37758=CARTESIAN_POINT('Origin',(0.,0.,-4.));
#37759=CARTESIAN_POINT('Origin',(0.,0.,-4.));
#37760=CARTESIAN_POINT('Origin',(0.,0.,12.));
#42604=UNCERTAINTY_MEASURE_WITH_UNIT(LENGTH_MEASURE(0.01),#42621,
'DISTANCE_ACCURACY_VALUE',
'Maximum model space distance between geometric entities at asserted c
onnectivities');
#42608=UNCERTAINTY_MEASURE_WITH_UNIT(LENGTH_MEASURE(0.01),#42621,
'DISTANCE_ACCURACY_VALUE',
'Maximum model space distance between geometric entities at asserted c
onnectivities');
#42616=(
GEOMETRIC_REPRESENTATION_CONTEXT(3)
GLOBAL_UNCERTAINTY_ASSIGNED_CONTEXT((#42604))
GLOBAL_UNIT_ASSIGNED_CONTEXT((#42621,#42623,#42624))
REPRESENTATION_CONTEXT('','3D')
);
#42620=(
GEOMETRIC_REPRESENTATION_CONTEXT(3)
GLOBAL_UNCERTAINTY_ASSIGNED_CONTEXT((#42608))
GLOBAL_UNIT_ASSIGNED_CONTEXT((#42621,#42623,#42624))
REPRESENTATION_CONTEXT('','3D')
);
#42621=(
LENGTH_UNIT()
NAMED_UNIT(*)
SI_UNIT(.MILLI.,.METRE.)
);
#42623=(
NAMED_UNIT(*)
PLANE_ANGLE_UNIT()
SI_UNIT($,.RADIAN.)
);
#42624=(
NAMED_UNIT(*)
SI_UNIT($,.STERADIAN.)
SOLID_ANGLE_UNIT()
);
#42632=SHAPE_DEFINITION_REPRESENTATION(#42643,#42729);
#42643=PRODUCT_DEFINITION_SHAPE('',$,#42741);
#42729=SHAPE_REPRESENTATION('',(#11061),#42616);
#42733=PRODUCT_DEFINITION_CONTEXT('part definition',#42768,'design');
#42741=PRODUCT_DEFINITION('Socket head cap screw M4x12',
'Socket head cap screw M4x12',#42752,#42733);
#42752=PRODUCT_DEFINITION_FORMATION('',$,#42777);
#42768=APPLICATION_CONTEXT(
'Core Data for Automotive Mechanical Design Process');
#42769=PRODUCT_CONTEXT('part definition',#42768,'mechanical');
#42777=PRODUCT('Socket head cap screw M4x12',
'Socket head cap screw M4x12',$,(#42769));
#42784=PRESENTATION_STYLE_ASSIGNMENT((#42792));
#42792=SURFACE_STYLE_USAGE(.BOTH.,#42800);
#42800=SURFACE_SIDE_STYLE('',(#42808));
#42808=SURFACE_STYLE_FILL_AREA(#42816);
#42816=FILL_AREA_STYLE('Dark gray',(#42824));
#42824=FILL_AREA_STYLE_COLOUR('Dark gray',#42832);
#42832=COLOUR_RGB('Dark gray',0.250980392156863,0.282352941176471,0.32156862745098);
ENDSEC;
END-ISO-10303-21;
